ISO-10303-21;
HEADER;
FILE_DESCRIPTION (('STEP AP214'),
    '1' );
FILE_NAME ('SAWC-0630-60S_wagen.step',
    '2026-10-09T16:01:55',
    ( '' ),
    ( '' ),
    'SwSTEP 2.0',
    'SolidWorks 2024',
    '' );
FILE_SCHEMA (( 'AUTOMOTIVE_DESIGN' ));
ENDSEC;

DATA;
#10=VERTEX_POINT ( 'NONE', #4255 ) ;
#19=ADVANCED_FACE ( 'NONE', ( #47367 ), #45971, .F. ) ;
#21=ORIENTED_EDGE ( 'NONE', *, *, #32727, .F. ) ;
#22=EDGE_CURVE ( 'NONE', #35164, #51205, #22753, .T. ) ;
#39=ORIENTED_EDGE ( 'NONE', *, *, #40166, .F. ) ;
#56=ORIENTED_EDGE ( 'NONE', *, *, #20714, .T. ) ;
#58=DIRECTION ( 'NONE',  ( 0.000000000000000000, 0.7096009616570518874, -0.7046037717862339012 ) ) ;
#62=CARTESIAN_POINT ( 'NONE',  ( 30.00000000000000000, -14.04000000000000092, 17.04524521594300523 ) ) ;
#64=VERTEX_POINT ( 'NONE', #42415 ) ;
#73=DIRECTION ( 'NONE',  ( 0.000000000000000000, 0.000000000000000000, 1.000000000000000000 ) ) ;
#76=CARTESIAN_POINT ( 'NONE',  ( 11.00000000000000000, -17.14999999999900027, 26.64999999999900027 ) ) ;
#81=PLANE ( 'NONE',  #14890 ) ;
#84=CARTESIAN_POINT ( 'NONE',  ( 30.00000000000000000, -5.599999999999999645, -9.400000000000000355 ) ) ;
#91=DIRECTION ( 'NONE',  ( 0.000000000000000000, -0.9938079899998859545, 0.1111111111112941946 ) ) ;
#93=ORIENTED_EDGE ( 'NONE', *, *, #1630, .F. ) ;
#109=CARTESIAN_POINT ( 'NONE',  ( 11.00000000000000000, -17.00000000000000000, 15.70499999999969809 ) ) ;
#115=CIRCLE ( 'NONE', #62160, 1.620999999999997332 ) ;
#117=ORIENTED_EDGE ( 'NONE', *, *, #12680, .F. ) ;
#121=FACE_OUTER_BOUND ( 'NONE', #43409, .T. ) ;
#122=VERTEX_POINT ( 'NONE', #47717 ) ;
#125=CARTESIAN_POINT ( 'NONE',  ( -11.00000000000000000, -9.200000000000120082, 17.64999999999993108 ) ) ;
#131=DIRECTION ( 'NONE',  ( 0.8660254037844482555, 0.000000000000000000, -0.4999999999999831801 ) ) ;
#139=CARTESIAN_POINT ( 'NONE',  ( 29.50000000000000355, -12.00000000000000000, 10.69999999999999929 ) ) ;
#146=CIRCLE ( 'NONE', #27251, 2.000000000000001776 ) ;
#147=DIRECTION ( 'NONE',  ( 1.000000000000000000, 0.000000000000000000, 0.000000000000000000 ) ) ;
#156=EDGE_CURVE ( 'NONE', #48024, #52249, #59027, .T. ) ;
#170=AXIS2_PLACEMENT_3D ( 'NONE', #9286, #3635, #67983 ) ;
#171=CIRCLE ( 'NONE', #58872, 0.4999999999991850963 ) ;
#173=CYLINDRICAL_SURFACE ( 'NONE', #39140, 3.499999999999850342 ) ;
#183=CARTESIAN_POINT ( 'NONE',  ( 11.50000000000000000, -11.50000000000100009, -10.50000000000065903 ) ) ;
#185=EDGE_CURVE ( 'NONE', #36958, #12401, #20004, .T. ) ;
#206=VECTOR ( 'NONE', #26081, 1000.000000000000000 ) ;
#210=ORIENTED_EDGE ( 'NONE', *, *, #15362, .F. ) ;
#212=DIRECTION ( 'NONE',  ( 0.000000000000000000, -0.1249999999999996531, -0.9921567416492215186 ) ) ;
#218=DIRECTION ( 'NONE',  ( 0.000000000000000000, 0.000000000000000000, 1.000000000000000000 ) ) ;
#223=PLANE ( 'NONE',  #58243 ) ;
#225=CARTESIAN_POINT ( 'NONE',  ( -29.50000000000000355, -15.46862696659690073, 14.50000000000000000 ) ) ;
#233=CARTESIAN_POINT ( 'NONE',  ( 30.00000000000000000, -5.599999999999999645, 9.400000000000000355 ) ) ;
#238=CARTESIAN_POINT ( 'NONE',  ( -11.00000000000000000, -9.199999999999999289, -12.34999999999989839 ) ) ;
#240=VECTOR ( 'NONE', #33249, 1000.000000000000000 ) ;
#251=CARTESIAN_POINT ( 'NONE',  ( -11.00000000000000000, -11.50000000000000000, -11.00000000000000000 ) ) ;
#258=DIRECTION ( 'NONE',  ( 0.000000000000000000, 0.000000000000000000, -1.000000000000000000 ) ) ;
#263=DIRECTION ( 'NONE',  ( 0.000000000000000000, 0.000000000000000000, -1.000000000000000000 ) ) ;
#265=DIRECTION ( 'NONE',  ( -1.000000000000000000, 0.000000000000000000, 0.000000000000000000 ) ) ;
#269=LINE ( 'NONE', #54368, #39000 ) ;
#276=ORIENTED_EDGE ( 'NONE', *, *, #51497, .T. ) ;
#278=VERTEX_POINT ( 'NONE', #3022 ) ;
#286=EDGE_CURVE ( 'NONE', #67917, #37432, #33951, .T. ) ;
#289=EDGE_CURVE ( 'NONE', #31751, #6775, #9008, .T. ) ;
#298=FACE_OUTER_BOUND ( 'NONE', #42957, .T. ) ;
#299=DIRECTION ( 'NONE',  ( 0.000000000000000000, -1.000000000000000000, 0.000000000000000000 ) ) ;
#301=ORIENTED_EDGE ( 'NONE', *, *, #36059, .F. ) ;
#302=LINE ( 'NONE', #38144, #67419 ) ;
#307=CYLINDRICAL_SURFACE ( 'NONE', #50491, 0.5000000000079367624 ) ;
#311=VECTOR ( 'NONE', #59625, 1000.000000000000000 ) ;
#312=DIRECTION ( 'NONE',  ( 1.000000000000000000, 0.000000000000000000, 0.000000000000000000 ) ) ;
#315=CARTESIAN_POINT ( 'NONE',  ( -14.25000000000000000, -0.2038245569916330158, 21.77831216351300014 ) ) ;
#328=ORIENTED_EDGE ( 'NONE', *, *, #56971, .F. ) ;
#331=DIRECTION ( 'NONE',  ( 0.000000000000000000, 0.000000000000000000, 1.000000000000000000 ) ) ;
#337=EDGE_LOOP ( 'NONE', ( #22411, #3438, #18951, #7458 ) ) ;
#342=CARTESIAN_POINT ( 'NONE',  ( 11.75000000000000000, -5.000000000000000000, 23.89194109070750471 ) ) ;
#346=ORIENTED_EDGE ( 'NONE', *, *, #49780, .F. ) ;
#351=ORIENTED_EDGE ( 'NONE', *, *, #10046, .F. ) ;
#359=ADVANCED_FACE ( 'NONE', ( #19615 ), #63466, .F. ) ;
#369=VECTOR ( 'NONE', #9157, 1000.000000000000000 ) ;
#370=AXIS2_PLACEMENT_3D ( 'NONE', #47263, #51866, #52935 ) ;
#373=VERTEX_POINT ( 'NONE', #52152 ) ;
#375=AXIS2_PLACEMENT_3D ( 'NONE', #48813, #22962, #60097 ) ;
#386=PLANE ( 'NONE',  #21114 ) ;
#394=ORIENTED_EDGE ( 'NONE', *, *, #68255, .T. ) ;
#401=CARTESIAN_POINT ( 'NONE',  ( -11.00000000000000000, -12.00000000000000000, -12.20000000000000107 ) ) ;
#404=CARTESIAN_POINT ( 'NONE',  ( -11.00000000000000000, -17.14999999999999858, -27.00000000000000000 ) ) ;
#406=CARTESIAN_POINT ( 'NONE',  ( -11.50000000000000000, -11.50000000000100009, 15.00000000000084910 ) ) ;
#414=VERTEX_POINT ( 'NONE', #10075 ) ;
#416=PLANE ( 'NONE',  #61814 ) ;
#425=PLANE ( 'NONE',  #31811 ) ;
#434=EDGE_CURVE ( 'NONE', #62987, #48159, #64181, .T. ) ;
#438=PLANE ( 'NONE',  #6363 ) ;
#446=DIRECTION ( 'NONE',  ( 0.000000000000000000, -0.7046037717859445770, 0.7096009616573392131 ) ) ;
#458=ORIENTED_EDGE ( 'NONE', *, *, #13082, .T. ) ;
#464=AXIS2_PLACEMENT_3D ( 'NONE', #42051, #41699, #8826 ) ;
#473=LINE ( 'NONE', #6118, #22739 ) ;
#476=VECTOR ( 'NONE', #4566, 1000.000000000000000 ) ;
#478=ORIENTED_EDGE ( 'NONE', *, *, #7168, .T. ) ;
#480=ORIENTED_EDGE ( 'NONE', *, *, #45337, .T. ) ;
#487=ORIENTED_EDGE ( 'NONE', *, *, #5618, .F. ) ;
#498=LINE ( 'NONE', #1194, #5981 ) ;
#505=EDGE_CURVE ( 'NONE', #35470, #13557, #53561, .T. ) ;
#507=ADVANCED_FACE ( 'NONE', ( #26684, #69821 ), #37996, .T. ) ;
#512=CIRCLE ( 'NONE', #39986, 0.3999999999993817390 ) ;
#517=CARTESIAN_POINT ( 'NONE',  ( 11.50000000000000000, -11.50000000000100009, 19.50000000000103739 ) ) ;
#524=CARTESIAN_POINT ( 'NONE',  ( -18.85410196625000268, -17.50000000000000000, -21.50000000000000000 ) ) ;
#534=ORIENTED_EDGE ( 'NONE', *, *, #35078, .T. ) ;
#544=CIRCLE ( 'NONE', #20825, 0.5000000000001357803 ) ;
#557=ORIENTED_EDGE ( 'NONE', *, *, #21564, .T. ) ;
#563=CARTESIAN_POINT ( 'NONE',  ( 11.00000000000000000, -11.70000000000000284, 12.50000000000000000 ) ) ;
#565=DIRECTION ( 'NONE',  ( 0.000000000000000000, 0.000000000000000000, 1.000000000000000000 ) ) ;
#571=CARTESIAN_POINT ( 'NONE',  ( 13.00000000000000178, -17.50000000000000000, -20.05051025721700242 ) ) ;
#576=ORIENTED_EDGE ( 'NONE', *, *, #13666, .T. ) ;
#580=EDGE_CURVE ( 'NONE', #24182, #41169, #23453, .T. ) ;
#584=EDGE_CURVE ( 'NONE', #17555, #46156, #6828, .T. ) ;
#594=DIRECTION ( 'NONE',  ( 0.000000000000000000, 1.000000000000000000, 0.000000000000000000 ) ) ;
#595=VECTOR ( 'NONE', #44304, 1000.000000000000000 ) ;
#599=ORIENTED_EDGE ( 'NONE', *, *, #39611, .F. ) ;
#601=CARTESIAN_POINT ( 'NONE',  ( 16.75000000000000000, -2.500000000000000000, -23.22168783648699986 ) ) ;
#604=FACE_OUTER_BOUND ( 'NONE', #11488, .T. ) ;
#607=VECTOR ( 'NONE', #2459, 1000.000000000000000 ) ;
#611=VERTEX_POINT ( 'NONE', #40036 ) ;
#613=LINE ( 'NONE', #38777, #60397 ) ;
#620=AXIS2_PLACEMENT_3D ( 'NONE', #69047, #10357, #8942 ) ;
#625=VECTOR ( 'NONE', #3696, 1000.000000000000000 ) ;
#645=FACE_OUTER_BOUND ( 'NONE', #22768, .T. ) ;
#652=DIRECTION ( 'NONE',  ( 0.000000000000000000, 1.000000000000000000, 0.000000000000000000 ) ) ;
#655=AXIS2_PLACEMENT_3D ( 'NONE', #12198, #65284, #6575 ) ;
#657=DIRECTION ( 'NONE',  ( -1.000000000000000000, 0.000000000000000000, 0.000000000000000000 ) ) ;
#667=ORIENTED_EDGE ( 'NONE', *, *, #3824, .T. ) ;
#676=DIRECTION ( 'NONE',  ( 0.000000000000000000, -0.1249999999999996531, -0.9921567416492215186 ) ) ;
#678=ORIENTED_EDGE ( 'NONE', *, *, #57075, .T. ) ;
#683=ORIENTED_EDGE ( 'NONE', *, *, #53543, .T. ) ;
#687=CARTESIAN_POINT ( 'NONE',  ( -16.75000000000000000, -0.2038245569916330158, 21.77831216351300014 ) ) ;
#692=ORIENTED_EDGE ( 'NONE', *, *, #38279, .T. ) ;
#701=VERTEX_POINT ( 'NONE', #45700 ) ;
#702=DIRECTION ( 'NONE',  ( 0.000000000000000000, 1.000000000000000000, 0.000000000000000000 ) ) ;
#703=DIRECTION ( 'NONE',  ( 0.000000000000000000, 1.000000000000000000, 0.000000000000000000 ) ) ;
#709=VECTOR ( 'NONE', #25731, 1000.000000000000000 ) ;
#715=VECTOR ( 'NONE', #34605, 1000.000000000000000 ) ;
#717=EDGE_LOOP ( 'NONE', ( #1969, #50627, #51311, #41125, #30322, #8766, #47543, #54269 ) ) ;
#728=AXIS2_PLACEMENT_3D ( 'NONE', #36991, #31684, #58558 ) ;
#732=LINE ( 'NONE', #43847, #65115 ) ;
#735=ORIENTED_EDGE ( 'NONE', *, *, #49732, .T. ) ;
#736=CYLINDRICAL_SURFACE ( 'NONE', #763, 4.000000000000000000 ) ;
#748=DIRECTION ( 'NONE',  ( 0.000000000000000000, 0.000000000000000000, -1.000000000000000000 ) ) ;
#750=CARTESIAN_POINT ( 'NONE',  ( 24.00000000000000000, -15.50000000000000000, -14.50000000000000000 ) ) ;
#759=EDGE_CURVE ( 'NONE', #64942, #41138, #44198, .T. ) ;
#763=AXIS2_PLACEMENT_3D ( 'NONE', #55845, #33245, #1748 ) ;
#768=AXIS2_PLACEMENT_3D ( 'NONE', #55446, #39511, #6988 ) ;
#770=LINE ( 'NONE', #25982, #22956 ) ;
#774=ORIENTED_EDGE ( 'NONE', *, *, #17721, .F. ) ;
#775=ADVANCED_FACE ( 'NONE', ( #62666 ), #31566, .T. ) ;
#782=VECTOR ( 'NONE', #26904, 1000.000000000000000 ) ;
#792=VECTOR ( 'NONE', #20280, 1000.000000000000000 ) ;
#794=DIRECTION ( 'NONE',  ( 0.000000000000000000, 0.000000000000000000, 1.000000000000000000 ) ) ;
#795=DIRECTION ( 'NONE',  ( 0.000000000000000000, 1.000000000000000000, 0.000000000000000000 ) ) ;
#801=ORIENTED_EDGE ( 'NONE', *, *, #31729, .T. ) ;
#818=VECTOR ( 'NONE', #43071, 1000.000000000000000 ) ;
#821=ORIENTED_EDGE ( 'NONE', *, *, #16313, .T. ) ;
#822=ADVANCED_FACE ( 'NONE', ( #57369 ), #66756, .F. ) ;
#836=CARTESIAN_POINT ( 'NONE',  ( 16.75000000000000000, -0.2038245569916320166, 23.22168783648699986 ) ) ;
#839=ADVANCED_FACE ( 'NONE', ( #26252 ), #63738, .T. ) ;
#844=VECTOR ( 'NONE', #58657, 1000.000000000000000 ) ;
#851=CARTESIAN_POINT ( 'NONE',  ( 30.00000000000000000, -16.28999999999710369, -15.00000000000794920 ) ) ;
#854=EDGE_CURVE ( 'NONE', #18488, #28131, #47123, .T. ) ;
#857=PLANE ( 'NONE',  #53952 ) ;
#861=EDGE_CURVE ( 'NONE', #40609, #24879, #59816, .T. ) ;
#862=DIRECTION ( 'NONE',  ( 0.000000000000000000, 0.000000000000000000, 1.000000000000000000 ) ) ;
#870=CARTESIAN_POINT ( 'NONE',  ( 30.00000000000000000, -9.454754784057099570, -17.53999999999999915 ) ) ;
#873=DIRECTION ( 'NONE',  ( -1.000000000000000000, 0.000000000000000000, 0.000000000000000000 ) ) ;
#874=CARTESIAN_POINT ( 'NONE',  ( 15.50000000000000000, -2.500000000000000000, -21.05662432702600029 ) ) ;
#881=AXIS2_PLACEMENT_3D ( 'NONE', #32979, #11408, #38971 ) ;
#884=DIRECTION ( 'NONE',  ( 0.000000000000000000, -1.000000000000000000, 0.000000000000000000 ) ) ;
#892=ADVANCED_FACE ( 'NONE', ( #48172 ), #42853, .T. ) ;
#894=EDGE_LOOP ( 'NONE', ( #48430, #3497, #17008, #60516 ) ) ;
#897=LINE ( 'NONE', #65568, #43887 ) ;
#899=ORIENTED_EDGE ( 'NONE', *, *, #69732, .T. ) ;
#903=VERTEX_POINT ( 'NONE', #11031 ) ;
#908=EDGE_LOOP ( 'NONE', ( #65645, #15970, #35262, #63312 ) ) ;
#910=CARTESIAN_POINT ( 'NONE',  ( 30.00000000000000000, -16.64230188589299786, -14.64519951917100116 ) ) ;
#919=ADVANCED_FACE ( 'NONE', ( #58782 ), #22348, .F. ) ;
#925=ORIENTED_EDGE ( 'NONE', *, *, #48482, .F. ) ;
#927=AXIS2_PLACEMENT_3D ( 'NONE', #15351, #36558, #36936 ) ;
#937=VECTOR ( 'NONE', #53202, 1000.000000000000114 ) ;
#943=ORIENTED_EDGE ( 'NONE', *, *, #45066, .T. ) ;
#946=PLANE ( 'NONE',  #16450 ) ;
#948=CARTESIAN_POINT ( 'NONE',  ( -23.75054448485400016, -15.50000000000000000, -25.53140320652400064 ) ) ;
#952=ORIENTED_EDGE ( 'NONE', *, *, #56490, .T. ) ;
#963=ORIENTED_EDGE ( 'NONE', *, *, #20143, .F. ) ;
#972=CARTESIAN_POINT ( 'NONE',  ( 15.50000000000000000, -1.037157890325000054, -19.00000000000000000 ) ) ;
#973=ORIENTED_EDGE ( 'NONE', *, *, #16758, .F. ) ;
#974=VERTEX_POINT ( 'NONE', #43892 ) ;
#976=DIRECTION ( 'NONE',  ( 0.000000000000000000, 0.000000000000000000, 1.000000000000000000 ) ) ;
#979=AXIS2_PLACEMENT_3D ( 'NONE', #1671, #6642, #49087 ) ;
#980=EDGE_CURVE ( 'NONE', #40956, #37986, #10339, .T. ) ;
#982=DIRECTION ( 'NONE',  ( -0.000000000000000000, 1.000000000000000000, -0.000000000000000000 ) ) ;
#986=EDGE_CURVE ( 'NONE', #22607, #46315, #61093, .T. ) ;
#991=EDGE_CURVE ( 'NONE', #24393, #37044, #28320, .T. ) ;
#995=LINE ( 'NONE', #67059, #3067 ) ;
#996=CYLINDRICAL_SURFACE ( 'NONE', #17307, 3.499999999999853895 ) ;
#1001=LINE ( 'NONE', #11920, #10971 ) ;
#1002=PLANE ( 'NONE',  #36242 ) ;
#1012=DIRECTION ( 'NONE',  ( 1.000000000000000000, -0.000000000000000000, -0.000000000000000000 ) ) ;
#1013=LINE ( 'NONE', #60730, #37520 ) ;
#1020=DIRECTION ( 'NONE',  ( 1.000000000000000000, -0.000000000000000000, -0.000000000000000000 ) ) ;
#1025=CARTESIAN_POINT ( 'NONE',  ( -30.00000000000000000, -9.487228132326899654, 12.50000000000000000 ) ) ;
#1031=VERTEX_POINT ( 'NONE', #18051 ) ;
#1032=ADVANCED_FACE ( 'NONE', ( #60837 ), #45267, .T. ) ;
#1033=LINE ( 'NONE', #33190, #57372 ) ;
#1042=ORIENTED_EDGE ( 'NONE', *, *, #49305, .F. ) ;
#1056=CARTESIAN_POINT ( 'NONE',  ( -11.00000000000000000, -11.50000000000100009, -15.00000000000084910 ) ) ;
#1063=CARTESIAN_POINT ( 'NONE',  ( 15.50000000000000000, -0.1999999999999999556, -22.50000000000000000 ) ) ;
#1065=AXIS2_PLACEMENT_3D ( 'NONE', #21415, #31694, #15767 ) ;
#1069=ADVANCED_FACE ( 'NONE', ( #44930 ), #23709, .F. ) ;
#1072=EDGE_CURVE ( 'NONE', #28664, #4772, #40327, .T. ) ;
#1076=ORIENTED_EDGE ( 'NONE', *, *, #25942, .T. ) ;
#1092=CARTESIAN_POINT ( 'NONE',  ( 29.25000000000000000, -5.200000000000001066, -11.75000000000000000 ) ) ;
#1093=CARTESIAN_POINT ( 'NONE',  ( 29.50000000000000355, -11.70000000000000284, 11.00000000000000000 ) ) ;
#1095=LINE ( 'NONE', #62, #16198 ) ;
#1102=AXIS2_PLACEMENT_3D ( 'NONE', #7957, #29532, #3368 ) ;
#1113=EDGE_CURVE ( 'NONE', #62633, #46357, #23019, .T. ) ;
#1121=VERTEX_POINT ( 'NONE', #61523 ) ;
#1124=CARTESIAN_POINT ( 'NONE',  ( 11.50000000000000000, -11.50000000000100009, -15.00000000000084910 ) ) ;
#1130=ORIENTED_EDGE ( 'NONE', *, *, #66026, .F. ) ;
#1135=ADVANCED_FACE ( 'NONE', ( #13447 ), #29017, .T. ) ;
#1143=CARTESIAN_POINT ( 'NONE',  ( -11.75000000000000000, -5.000000000000000000, 21.10805890929250239 ) ) ;
#1148=CARTESIAN_POINT ( 'NONE',  ( -11.50000000000000000, -11.50000000000100009, -19.50000000000103739 ) ) ;
#1149=AXIS2_PLACEMENT_3D ( 'NONE', #2658, #12561, #19280 ) ;
#1152=EDGE_CURVE ( 'NONE', #49918, #39966, #56583, .T. ) ;
#1158=VERTEX_POINT ( 'NONE', #31132 ) ;
#1159=ORIENTED_EDGE ( 'NONE', *, *, #22456, .T. ) ;
#1160=VECTOR ( 'NONE', #55772, 1000.000000000000000 ) ;
#1161=PLANE ( 'NONE',  #26470 ) ;
#1165=CARTESIAN_POINT ( 'NONE',  ( -11.00000000000000000, -17.35230188589299871, 15.35019951917099945 ) ) ;
#1175=ORIENTED_EDGE ( 'NONE', *, *, #22784, .F. ) ;
#1185=CARTESIAN_POINT ( 'NONE',  ( 24.00000000000000000, -16.28999999999999915, 14.50000000000000000 ) ) ;
#1191=VERTEX_POINT ( 'NONE', #4266 ) ;
#1193=CARTESIAN_POINT ( 'NONE',  ( 23.48000000000000043, -15.50000000000000000, -26.00000000000000355 ) ) ;
#1194=CARTESIAN_POINT ( 'NONE',  ( -17.00000000000000000, -16.64230188589299786, -14.64519951917100116 ) ) ;
#1201=CIRCLE ( 'NONE', #29390, 3.499999999999041655 ) ;
#1204=CIRCLE ( 'NONE', #27204, 1.449999999999999956 ) ;
#1207=CARTESIAN_POINT ( 'NONE',  ( -29.50000000000000355, -11.50000000000000000, 19.00000000000000000 ) ) ;
#1210=LINE ( 'NONE', #30507, #44645 ) ;
#1213=ORIENTED_EDGE ( 'NONE', *, *, #68292, .T. ) ;
#1218=CARTESIAN_POINT ( 'NONE',  ( 13.00000000000000178, -15.50000000000000000, -20.05051025721700242 ) ) ;
#1220=ORIENTED_EDGE ( 'NONE', *, *, #37017, .T. ) ;
#1224=VECTOR ( 'NONE', #7831, 1000.000000000000000 ) ;
#1227=ADVANCED_FACE ( 'NONE', ( #14507 ), #58357, .T. ) ;
#1234=ORIENTED_EDGE ( 'NONE', *, *, #63821, .T. ) ;
#1235=CARTESIAN_POINT ( 'NONE',  ( -11.00000000000000000, -9.454754784057099570, -17.53999999999999915 ) ) ;
#1237=AXIS2_PLACEMENT_3D ( 'NONE', #42013, #69594, #37075 ) ;
#1247=ADVANCED_FACE ( 'NONE', ( #67899 ), #19451, .F. ) ;
#1248=DIRECTION ( 'NONE',  ( 0.000000000000000000, 0.000000000000000000, -1.000000000000000000 ) ) ;
#1252=VECTOR ( 'NONE', #4585, 1000.000000000000000 ) ;
#1262=DIRECTION ( 'NONE',  ( 0.000000000000000000, 0.7071067811865496822, 0.7071067811865454633 ) ) ;
#1272=DIRECTION ( 'NONE',  ( 1.000000000000000000, 0.000000000000000000, 0.000000000000000000 ) ) ;
#1277=EDGE_CURVE ( 'NONE', #59384, #6050, #25467, .T. ) ;
#1284=EDGE_CURVE ( 'NONE', #48776, #37166, #15907, .T. ) ;
#1286=PLANE ( 'NONE',  #15354 ) ;
#1314=DIRECTION ( 'NONE',  ( -1.000000000000000000, 0.000000000000000000, 0.000000000000000000 ) ) ;
#1315=DIRECTION ( 'NONE',  ( 1.000000000000000000, -0.000000000000000000, -0.000000000000000000 ) ) ;
#1316=EDGE_LOOP ( 'NONE', ( #1706, #48717, #10061, #39619 ) ) ;
#1324=EDGE_CURVE ( 'NONE', #31007, #4729, #59948, .T. ) ;
#1328=FACE_OUTER_BOUND ( 'NONE', #32846, .T. ) ;
#1333=CARTESIAN_POINT ( 'NONE',  ( 17.24945551514599984, -17.50000000000000000, 25.53140320652400064 ) ) ;
#1345=CARTESIAN_POINT ( 'NONE',  ( 14.25000000000000000, -0.2038245569916330158, 21.77831216351300014 ) ) ;
#1348=CARTESIAN_POINT ( 'NONE',  ( -14.66242688423474227, -0.3152598339554810170, 21.54019739087905094 ) ) ;
#1350=ORIENTED_EDGE ( 'NONE', *, *, #6171, .F. ) ;
#1356=LINE ( 'NONE', #38501, #62102 ) ;
#1372=EDGE_CURVE ( 'NONE', #67636, #34438, #55125, .T. ) ;
#1373=DIRECTION ( 'NONE',  ( 0.000000000000000000, -0.7046037717806115097, 0.7096009616626348659 ) ) ;
#1375=VERTEX_POINT ( 'NONE', #50147 ) ;
#1380=LINE ( 'NONE', #33209, #39108 ) ;
#1383=ORIENTED_EDGE ( 'NONE', *, *, #19821, .T. ) ;
#1386=VECTOR ( 'NONE', #23590, 1000.000000000000000 ) ;
#1389=AXIS2_PLACEMENT_3D ( 'NONE', #27171, #64642, #64999 ) ;
#1392=ORIENTED_EDGE ( 'NONE', *, *, #32157, .F. ) ;
#1394=DIRECTION ( 'NONE',  ( 0.000000000000000000, 1.000000000000000000, 0.000000000000000000 ) ) ;
#1395=VECTOR ( 'NONE', #65892, 1000.000000000000000 ) ;
#1404=DIRECTION ( 'NONE',  ( 0.000000000000000000, 0.000000000000000000, -1.000000000000000000 ) ) ;
#1413=DIRECTION ( 'NONE',  ( 0.000000000000000000, 1.000000000000000000, 0.000000000000000000 ) ) ;
#1414=LINE ( 'NONE', #22305, #61005 ) ;
#1417=CARTESIAN_POINT ( 'NONE',  ( -14.25000000000000000, -2.500000000000000000, -23.22168783648699986 ) ) ;
#1418=DIRECTION ( 'NONE',  ( 0.000000000000000000, 0.000000000000000000, 1.000000000000000000 ) ) ;
#1423=ORIENTED_EDGE ( 'NONE', *, *, #47757, .F. ) ;
#1425=PLANE ( 'NONE',  #32851 ) ;
#1436=CARTESIAN_POINT ( 'NONE',  ( 22.14589803375000088, -15.50000000000000000, -21.50000000000000000 ) ) ;
#1438=ORIENTED_EDGE ( 'NONE', *, *, #37753, .F. ) ;
#1448=CARTESIAN_POINT ( 'NONE',  ( 30.00000000000000000, -16.64230188589299786, -14.64519951917100116 ) ) ;
#1450=DIRECTION ( 'NONE',  ( -1.000000000000000000, 0.000000000000000000, 0.000000000000000000 ) ) ;
#1465=CARTESIAN_POINT ( 'NONE',  ( -28.00000000000000000, -16.28999999999999915, -14.50000000000000000 ) ) ;
#1472=CARTESIAN_POINT ( 'NONE',  ( -11.00000000000000000, -14.33999999999999986, 14.50000000000000000 ) ) ;
#1475=VERTEX_POINT ( 'NONE', #56160 ) ;
#1478=CARTESIAN_POINT ( 'NONE',  ( -14.10805890929250062, -5.000000000000000000, 26.25000000000000000 ) ) ;
#1483=EDGE_CURVE ( 'NONE', #14490, #54337, #29462, .T. ) ;
#1486=EDGE_CURVE ( 'NONE', #22030, #7056, #55806, .T. ) ;
#1491=FACE_OUTER_BOUND ( 'NONE', #7855, .T. ) ;
#1502=DIRECTION ( 'NONE',  ( 0.000000000000000000, -1.000000000000000000, 0.000000000000000000 ) ) ;
#1506=DIRECTION ( 'NONE',  ( 0.000000000000000000, 0.000000000000000000, 1.000000000000000000 ) ) ;
#1510=AXIS2_PLACEMENT_3D ( 'NONE', #36370, #14100, #8806 ) ;
#1513=ORIENTED_EDGE ( 'NONE', *, *, #6208, .T. ) ;
#1519=ORIENTED_EDGE ( 'NONE', *, *, #31973, .T. ) ;
#1520=FACE_OUTER_BOUND ( 'NONE', #17280, .T. ) ;
#1521=DIRECTION ( 'NONE',  ( 0.000000000000000000, 0.000000000000000000, 1.000000000000000000 ) ) ;
#1530=EDGE_CURVE ( 'NONE', #24780, #41832, #39594, .T. ) ;
#1537=EDGE_CURVE ( 'NONE', #32087, #62810, #57683, .T. ) ;
#1545=EDGE_CURVE ( 'NONE', #54090, #69297, #66417, .T. ) ;
#1553=LINE ( 'NONE', #46089, #36194 ) ;
#1554=ORIENTED_EDGE ( 'NONE', *, *, #19391, .T. ) ;
#1559=ORIENTED_EDGE ( 'NONE', *, *, #13351, .F. ) ;
#1583=VECTOR ( 'NONE', #66399, 1000.000000000000114 ) ;
#1587=FACE_OUTER_BOUND ( 'NONE', #30596, .T. ) ;
#1589=CARTESIAN_POINT ( 'NONE',  ( -11.75000000000000000, -5.000000000000000000, 23.89194109070750471 ) ) ;
#1590=AXIS2_PLACEMENT_3D ( 'NONE', #35235, #23946, #51530 ) ;
#1594=FACE_OUTER_BOUND ( 'NONE', #55076, .T. ) ;
#1602=EDGE_CURVE ( 'NONE', #22867, #61212, #51553, .T. ) ;
#1608=ORIENTED_EDGE ( 'NONE', *, *, #4024, .F. ) ;
#1614=CARTESIAN_POINT ( 'NONE',  ( 11.00000000000000000, -13.54524521594299991, 17.53999999999999915 ) ) ;
#1616=CARTESIAN_POINT ( 'NONE',  ( -14.25000000000000178, -0.2714405302574905976, -22.98746066354537732 ) ) ;
#1623=CARTESIAN_POINT ( 'NONE',  ( 25.50000000000000355, -17.50000000000000000, -25.99999999999985434 ) ) ;
#1627=DIRECTION ( 'NONE',  ( -0.4999999999999832356, 0.000000000000000000, 0.8660254037844483666 ) ) ;
#1628=LINE ( 'NONE', #972, #56470 ) ;
#1630=EDGE_CURVE ( 'NONE', #15321, #39690, #52252, .T. ) ;
#1643=ORIENTED_EDGE ( 'NONE', *, *, #28455, .T. ) ;
#1656=ORIENTED_EDGE ( 'NONE', *, *, #67381, .T. ) ;
#1659=DIRECTION ( 'NONE',  ( 1.000000000000000000, 0.000000000000000000, 0.000000000000000000 ) ) ;
#1663=DIRECTION ( 'NONE',  ( 1.000000000000000000, -0.000000000000000000, -0.000000000000000000 ) ) ;
#1671=CARTESIAN_POINT ( 'NONE',  ( 25.49999999999869971, -15.50000000000000000, -22.50000000000000000 ) ) ;
#1673=AXIS2_PLACEMENT_3D ( 'NONE', #16608, #16241, #66054 ) ;
#1674=LINE ( 'NONE', #32828, #36392 ) ;
#1676=LINE ( 'NONE', #66391, #8125 ) ;
#1681=VECTOR ( 'NONE', #12130, 1000.000000000000000 ) ;
#1682=VERTEX_POINT ( 'NONE', #25740 ) ;
#1687=CARTESIAN_POINT ( 'NONE',  ( -15.50000000000000000, -2.500000000000000000, -21.05662432702600029 ) ) ;
#1690=VERTEX_POINT ( 'NONE', #16519 ) ;
#1706=ORIENTED_EDGE ( 'NONE', *, *, #12925, .T. ) ;
#1708=CARTESIAN_POINT ( 'NONE',  ( 17.00000000000000000, -17.00000000000000000, -15.70499999999969809 ) ) ;
#1716=ORIENTED_EDGE ( 'NONE', *, *, #5157, .T. ) ;
#1719=PLANE ( 'NONE',  #23120 ) ;
#1722=DIRECTION ( 'NONE',  ( 0.000000000000000000, 0.7071067811865474617, -0.7071067811865474617 ) ) ;
#1723=ORIENTED_EDGE ( 'NONE', *, *, #14236, .F. ) ;
#1724=ORIENTED_EDGE ( 'NONE', *, *, #43985, .T. ) ;
#1726=ORIENTED_EDGE ( 'NONE', *, *, #4024, .T. ) ;
#1731=LINE ( 'NONE', #29290, #24476 ) ;
#1744=CARTESIAN_POINT ( 'NONE',  ( 17.00000000000000000, -17.50000000000000000, -15.70500000000000007 ) ) ;
#1745=CARTESIAN_POINT ( 'NONE',  ( 11.00000000000000000, -14.04000000000000092, 14.80000000000000071 ) ) ;
#1748=DIRECTION ( 'NONE',  ( 0.000000000000000000, 0.000000000000000000, -1.000000000000000000 ) ) ;
#1757=B_SPLINE_CURVE_WITH_KNOTS ( 'NONE', 3,
 ( #31440, #33830, #65342, #6623, #44781, #66373 ),
 .UNSPECIFIED., .F., .F.,
 ( 4, 2, 4 ),
 ( 1.820537833122031657, 2.555393473688636341, 3.290249114255240581 ),
 .UNSPECIFIED. ) ;
#1760=VERTEX_POINT ( 'NONE', #69905 ) ;
#1767=CARTESIAN_POINT ( 'NONE',  ( 30.00000000000000000, -5.000000000000000000, 27.00000000000000000 ) ) ;
#1771=FACE_OUTER_BOUND ( 'NONE', #49422, .T. ) ;
#1772=DIRECTION ( 'NONE',  ( 0.000000000000000000, 0.000000000000000000, 1.000000000000000000 ) ) ;
#1777=DIRECTION ( 'NONE',  ( 0.000000000000000000, 0.000000000000000000, -1.000000000000000000 ) ) ;
#1783=CIRCLE ( 'NONE', #16488, 4.000000000000001776 ) ;
#1793=EDGE_CURVE ( 'NONE', #34056, #15308, #39643, .T. ) ;
#1794=ORIENTED_EDGE ( 'NONE', *, *, #6856, .F. ) ;
#1806=AXIS2_PLACEMENT_3D ( 'NONE', #11968, #43123, #33553 ) ;
#1810=DIRECTION ( 'NONE',  ( 1.000000000000000000, 0.000000000000000000, 0.000000000000000000 ) ) ;
#1819=VERTEX_POINT ( 'NONE', #21126 ) ;
#1823=LINE ( 'NONE', #12759, #9699 ) ;
#1824=ORIENTED_EDGE ( 'NONE', *, *, #1545, .T. ) ;
#1829=EDGE_CURVE ( 'NONE', #20348, #7353, #5223, .T. ) ;
#1838=CIRCLE ( 'NONE', #28942, 3.499999999999040323 ) ;
#1840=EDGE_CURVE ( 'NONE', #19166, #11369, #36282, .T. ) ;
#1844=LINE ( 'NONE', #39329, #18059 ) ;
#1857=PLANE ( 'NONE',  #30991 ) ;
#1859=ADVANCED_FACE ( 'NONE', ( #61358 ), #3533, .F. ) ;
#1861=LINE ( 'NONE', #28377, #65672 ) ;
#1862=VECTOR ( 'NONE', #59394, 1000.000000000000000 ) ;
#1867=DIRECTION ( 'NONE',  ( 0.000000000000000000, 1.000000000000000000, 0.000000000000000000 ) ) ;
#1871=CARTESIAN_POINT ( 'NONE',  ( 17.51999999999999957, -15.50000000000000000, -26.00000000000000355 ) ) ;
#1872=ORIENTED_EDGE ( 'NONE', *, *, #54165, .T. ) ;
#1875=EDGE_LOOP ( 'NONE', ( #69414, #54797, #47049, #6618 ) ) ;
#1877=DIRECTION ( 'NONE',  ( 0.000000000000000000, 1.000000000000000000, 0.000000000000000000 ) ) ;
#1890=DIRECTION ( 'NONE',  ( 0.8660254037844482555, 0.000000000000000000, 0.4999999999999831801 ) ) ;
#1899=EDGE_CURVE ( 'NONE', #27192, #49549, #59981, .T. ) ;
#1903=DIRECTION ( 'NONE',  ( 0.000000000000000000, 0.7096009616570518874, 0.7046037717862339012 ) ) ;
#1922=ORIENTED_EDGE ( 'NONE', *, *, #30216, .F. ) ;
#1929=ORIENTED_EDGE ( 'NONE', *, *, #68682, .F. ) ;
#1932=DIRECTION ( 'NONE',  ( 1.000000000000000000, 0.000000000000000000, 0.000000000000000000 ) ) ;
#1941=VERTEX_POINT ( 'NONE', #2327 ) ;
#1944=LINE ( 'NONE', #55684, #9971 ) ;
#1946=VECTOR ( 'NONE', #44801, 1000.000000000000000 ) ;
#1947=FACE_OUTER_BOUND ( 'NONE', #15735, .T. ) ;
#1951=AXIS2_PLACEMENT_3D ( 'NONE', #12127, #12468, #60222 ) ;
#1954=CARTESIAN_POINT ( 'NONE',  ( 30.00000000000000000, -16.28999999999710369, 15.00000000000794920 ) ) ;
#1958=CARTESIAN_POINT ( 'NONE',  ( -15.50000000000000000, -0.4000000000000000222, -25.99999999999999645 ) ) ;
#1962=CARTESIAN_POINT ( 'NONE',  ( -15.29686605391142606, -0.2715358723588626733, -21.17390376548178210 ) ) ;
#1966=DIRECTION ( 'NONE',  ( 1.000000000000000000, 0.000000000000000000, 0.000000000000000000 ) ) ;
#1969=ORIENTED_EDGE ( 'NONE', *, *, #48362, .F. ) ;
#1970=CIRCLE ( 'NONE', #27972, 4.000000000000000888 ) ;
#1971=CARTESIAN_POINT ( 'NONE',  ( 17.51999999999999957, -17.50000000000000000, -26.00000000000000355 ) ) ;
#1973=ORIENTED_EDGE ( 'NONE', *, *, #63608, .T. ) ;
#1984=AXIS2_PLACEMENT_3D ( 'NONE', #44989, #1867, #2552 ) ;
#1985=ORIENTED_EDGE ( 'NONE', *, *, #4293, .F. ) ;
#1993=VERTEX_POINT ( 'NONE', #12227 ) ;
#1994=VECTOR ( 'NONE', #25777, 1000.000000000000000 ) ;
#1997=DIRECTION ( 'NONE',  ( 0.000000000000000000, -0.1249999999999996531, 0.9921567416492215186 ) ) ;
#1999=ORIENTED_EDGE ( 'NONE', *, *, #40865, .T. ) ;
#2008=DIRECTION ( 'NONE',  ( 0.000000000000000000, 1.000000000000000000, 0.000000000000000000 ) ) ;
#2009=CARTESIAN_POINT ( 'NONE',  ( 11.00000000000000000, -14.33999999999999986, -14.50000000000000000 ) ) ;
#2013=AXIS2_PLACEMENT_3D ( 'NONE', #32729, #6565, #218 ) ;
#2030=DIRECTION ( 'NONE',  ( 0.000000000000000000, 0.000000000000000000, 1.000000000000000000 ) ) ;
#2031=DIRECTION ( 'NONE',  ( -0.8660254037844482555, 0.000000000000000000, 0.4999999999999831801 ) ) ;
#2032=EDGE_CURVE ( 'NONE', #14101, #50592, #23855, .T. ) ;
#2041=VERTEX_POINT ( 'NONE', #35183 ) ;
#2042=CARTESIAN_POINT ( 'NONE',  ( -30.00000000000000000, -12.00000000000000000, 11.03137303340310282 ) ) ;
#2048=CIRCLE ( 'NONE', #7689, 0.2000000000005261458 ) ;
#2055=CIRCLE ( 'NONE', #65322, 0.3500000000002719824 ) ;
#2069=ORIENTED_EDGE ( 'NONE', *, *, #10123, .F. ) ;
#2072=DIRECTION ( 'NONE',  ( 1.000000000000000000, -0.000000000000000000, -0.000000000000000000 ) ) ;
#2073=EDGE_LOOP ( 'NONE', ( #13908, #1608 ) ) ;
#2075=ORIENTED_EDGE ( 'NONE', *, *, #44533, .F. ) ;
#2076=ORIENTED_EDGE ( 'NONE', *, *, #56977, .F. ) ;
#2098=CIRCLE ( 'NONE', #54057, 4.000000000000000888 ) ;
#2115=DIRECTION ( 'NONE',  ( -1.000000000000000000, 0.000000000000000000, 0.000000000000000000 ) ) ;
#2118=CIRCLE ( 'NONE', #41639, 0.2999999999998732569 ) ;
#2119=CARTESIAN_POINT ( 'NONE',  ( 30.00000000000000000, -17.50000000000000000, -15.70500000000000007 ) ) ;
#2121=CARTESIAN_POINT ( 'NONE',  ( -15.50000000000129852, -15.50000000000000000, -22.50000000000000000 ) ) ;
#2132=VERTEX_POINT ( 'NONE', #28000 ) ;
#2139=CARTESIAN_POINT ( 'NONE',  ( 25.50000000000000355, 0.000000000000000000, -22.50000000000000000 ) ) ;
#2142=ORIENTED_EDGE ( 'NONE', *, *, #64189, .T. ) ;
#2151=EDGE_CURVE ( 'NONE', #52459, #69392, #22359, .T. ) ;
#2155=CARTESIAN_POINT ( 'NONE',  ( 28.00000000000000000, -15.50000000000000000, 20.05051025721700242 ) ) ;
#2156=VERTEX_POINT ( 'NONE', #54534 ) ;
#2157=EDGE_CURVE ( 'NONE', #40956, #50486, #12673, .T. ) ;
#2175=EDGE_CURVE ( 'NONE', #18730, #21397, #26965, .T. ) ;
#2179=CARTESIAN_POINT ( 'NONE',  ( 11.00000000000000000, -5.200000000000001066, -9.400000000000000355 ) ) ;
#2180=ORIENTED_EDGE ( 'NONE', *, *, #29330, .T. ) ;
#2184=LINE ( 'NONE', #29742, #62149 ) ;
#2186=ORIENTED_EDGE ( 'NONE', *, *, #24408, .T. ) ;
#2217=VERTEX_POINT ( 'NONE', #12067 ) ;
#2219=VECTOR ( 'NONE', #7218, 1000.000000000000000 ) ;
#2229=EDGE_LOOP ( 'NONE', ( #30375, #8867, #7920, #42250 ) ) ;
#2244=ORIENTED_EDGE ( 'NONE', *, *, #66501, .F. ) ;
#2246=ADVANCED_FACE ( 'NONE', ( #50246 ), #39627, .F. ) ;
#2259=DIRECTION ( 'NONE',  ( 0.000000000000000000, 1.000000000000000000, 0.000000000000000000 ) ) ;
#2263=AXIS2_PLACEMENT_3D ( 'NONE', #34558, #40913, #24663 ) ;
#2276=AXIS2_PLACEMENT_3D ( 'NONE', #31674, #47232, #14698 ) ;
#2287=EDGE_CURVE ( 'NONE', #34666, #20953, #4792, .T. ) ;
#2288=CYLINDRICAL_SURFACE ( 'NONE', #68602, 4.500000000000188294 ) ;
#2294=CARTESIAN_POINT ( 'NONE',  ( -11.50000000000000000, -12.00000000000000000, 10.52786404500095863 ) ) ;
#2299=EDGE_LOOP ( 'NONE', ( #3724, #49032, #30876, #8902, #49888, #43618, #33137, #12672, #4862, #55127, #14124, #28234, #69378, #2404, #30624, #11403 ) ) ;
#2302=DIRECTION ( 'NONE',  ( -1.000000000000000000, 0.000000000000000000, 0.000000000000000000 ) ) ;
#2308=LINE ( 'NONE', #23872, #13602 ) ;
#2311=DIRECTION ( 'NONE',  ( 1.000000000000000000, 0.000000000000000000, 0.000000000000000000 ) ) ;
#2316=EDGE_CURVE ( 'NONE', #59292, #38183, #38654, .T. ) ;
#2319=VERTEX_POINT ( 'NONE', #55558 ) ;
#2321=AXIS2_PLACEMENT_3D ( 'NONE', #18503, #61639, #13210 ) ;
#2324=CARTESIAN_POINT ( 'NONE',  ( -14.25000000000000000, -0.2038245569916330158, -23.22168783648699986 ) ) ;
#2325=ORIENTED_EDGE ( 'NONE', *, *, #64520, .T. ) ;
#2326=VERTEX_POINT ( 'NONE', #55901 ) ;
#2327=CARTESIAN_POINT ( 'NONE',  ( -15.50000000000000000, -17.50000000000000000, -25.99999999999985079 ) ) ;
#2331=CARTESIAN_POINT ( 'NONE',  ( 30.00000000000000000, -9.199999999999999289, 12.69999999999986073 ) ) ;
#2336=ORIENTED_EDGE ( 'NONE', *, *, #65118, .T. ) ;
#2337=DIRECTION ( 'NONE',  ( -0.4999999999989361843, 0.000000000000000000, 0.8660254037850529940 ) ) ;
#2340=ORIENTED_EDGE ( 'NONE', *, *, #50487, .T. ) ;
#2343=AXIS2_PLACEMENT_3D ( 'NONE', #3500, #24710, #19397 ) ;
#2348=AXIS2_PLACEMENT_3D ( 'NONE', #68413, #19967, #26326 ) ;
#2361=LINE ( 'NONE', #47257, #21860 ) ;
#2368=CIRCLE ( 'NONE', #48668, 4.000000000000000888 ) ;
#2370=CARTESIAN_POINT ( 'NONE',  ( -29.50000000000000355, -11.50000000000000000, 15.00000000000000000 ) ) ;
#2379=CARTESIAN_POINT ( 'NONE',  ( -30.00000000000000000, -17.14999999999999858, -27.00000000000000000 ) ) ;
#2383=FACE_OUTER_BOUND ( 'NONE', #44834, .T. ) ;
#2391=VECTOR ( 'NONE', #65517, 1000.000000000000000 ) ;
#2402=DIRECTION ( 'NONE',  ( 0.000000000000000000, -0.9921567416492215186, 0.1249999999999996531 ) ) ;
#2403=ORIENTED_EDGE ( 'NONE', *, *, #4156, .T. ) ;
#2404=ORIENTED_EDGE ( 'NONE', *, *, #34068, .F. ) ;
#2405=CARTESIAN_POINT ( 'NONE',  ( -13.00000000000000178, -16.28999999999710369, -15.00000000000794920 ) ) ;
#2406=EDGE_LOOP ( 'NONE', ( #14702, #53614, #42844, #43327 ) ) ;
#2414=ADVANCED_FACE ( 'NONE', ( #3566 ), #23993, .F. ) ;
#2419=DIRECTION ( 'NONE',  ( 0.000000000000000000, 0.000000000000000000, -1.000000000000000000 ) ) ;
#2423=ORIENTED_EDGE ( 'NONE', *, *, #68126, .F. ) ;
#2425=EDGE_CURVE ( 'NONE', #8140, #23746, #53068, .T. ) ;
#2433=ORIENTED_EDGE ( 'NONE', *, *, #27594, .F. ) ;
#2434=ORIENTED_EDGE ( 'NONE', *, *, #9596, .F. ) ;
#2436=DIRECTION ( 'NONE',  ( 0.000000000000000000, -1.000000000000000000, 0.000000000000000000 ) ) ;
#2444=LINE ( 'NONE', #57241, #10004 ) ;
#2446=ORIENTED_EDGE ( 'NONE', *, *, #23329, .F. ) ;
#2451=DIRECTION ( 'NONE',  ( -0.000000000000000000, 1.000000000000000000, -0.000000000000000000 ) ) ;
#2452=VECTOR ( 'NONE', #50922, 1000.000000000000000 ) ;
#2459=DIRECTION ( 'NONE',  ( 0.000000000000000000, -1.000000000000000000, 0.000000000000000000 ) ) ;
#2464=ADVANCED_FACE ( 'NONE', ( #30079 ), #46338, .T. ) ;
#2465=VERTEX_POINT ( 'NONE', #63313 ) ;
#2466=DIRECTION ( 'NONE',  ( 0.000000000000000000, 1.000000000000000000, 0.000000000000000000 ) ) ;
#2467=DIRECTION ( 'NONE',  ( 0.000000000000000000, -1.000000000000000000, 0.000000000000000000 ) ) ;
#2468=ORIENTED_EDGE ( 'NONE', *, *, #1113, .F. ) ;
#2473=FACE_OUTER_BOUND ( 'NONE', #43304, .T. ) ;
#2483=LINE ( 'NONE', #13443, #60346 ) ;
#2489=DIRECTION ( 'NONE',  ( 0.000000000000000000, -1.000000000000000000, 0.000000000000000000 ) ) ;
#2495=FACE_OUTER_BOUND ( 'NONE', #36217, .T. ) ;
#2508=LINE ( 'NONE', #28006, #21955 ) ;
#2513=ORIENTED_EDGE ( 'NONE', *, *, #42294, .T. ) ;
#2518=VERTEX_POINT ( 'NONE', #54448 ) ;
#2525=ORIENTED_EDGE ( 'NONE', *, *, #35701, .T. ) ;
#2526=VERTEX_POINT ( 'NONE', #22608 ) ;
#2532=CARTESIAN_POINT ( 'NONE',  ( 11.50000000000000000, -15.97213595500069871, 14.50000000000000000 ) ) ;
#2539=EDGE_CURVE ( 'NONE', #47666, #46878, #27441, .T. ) ;
#2544=DIRECTION ( 'NONE',  ( 0.000000000000000000, -0.9938079899998859545, 0.1111111111112941946 ) ) ;
#2552=DIRECTION ( 'NONE',  ( 0.000000000000000000, 0.000000000000000000, 1.000000000000000000 ) ) ;
#2569=EDGE_CURVE ( 'NONE', #58795, #24609, #48906, .T. ) ;
#2576=ORIENTED_EDGE ( 'NONE', *, *, #11857, .T. ) ;
#2578=ORIENTED_EDGE ( 'NONE', *, *, #32522, .T. ) ;
#2592=AXIS2_PLACEMENT_3D ( 'NONE', #41302, #47313, #36000 ) ;
#2594=DIRECTION ( 'NONE',  ( -1.000000000000000000, 0.000000000000000000, 0.000000000000000000 ) ) ;
#2606=DIRECTION ( 'NONE',  ( 0.000000000000000000, 0.000000000000000000, -1.000000000000000000 ) ) ;
#2611=EDGE_CURVE ( 'NONE', #34045, #42164, #26339, .T. ) ;
#2612=VECTOR ( 'NONE', #7791, 1000.000000000000000 ) ;
#2618=EDGE_LOOP ( 'NONE', ( #1513, #821, #63105, #9771 ) ) ;
#2622=CYLINDRICAL_SURFACE ( 'NONE', #48523, 0.3499999999999614531 ) ;
#2623=VECTOR ( 'NONE', #5180, 1000.000000000000000 ) ;
#2628=DIRECTION ( 'NONE',  ( 0.000000000000000000, 1.000000000000000000, 0.000000000000000000 ) ) ;
#2631=ADVANCED_FACE ( 'NONE', ( #64363 ), #27919, .F. ) ;
#2637=SURFACE_SIDE_STYLE ('',( #3344 ) ) ;
#2654=CARTESIAN_POINT ( 'NONE',  ( 16.33757311576526305, -0.3152598339554824047, -23.45980260912095616 ) ) ;
#2657=TOROIDAL_SURFACE ( 'NONE', #32013, 3.299999999999474909, 0.2000000000005234813 ) ;
#2658=CARTESIAN_POINT ( 'NONE',  ( 13.00000000000000178, -17.00000000000000000, 15.70499999999969809 ) ) ;
#2663=CARTESIAN_POINT ( 'NONE',  ( -11.00000000000000000, -17.14999999999999858, 27.00000000000000000 ) ) ;
#2680=CARTESIAN_POINT ( 'NONE',  ( -15.50000000000000000, -17.50000000000000000, 22.50000000000000000 ) ) ;
#2688=DIRECTION ( 'NONE',  ( 0.000000000000000000, 1.000000000000000000, 0.000000000000000000 ) ) ;
#2695=LINE ( 'NONE', #33825, #39402 ) ;
#2702=VERTEX_POINT ( 'NONE', #2765 ) ;
#2710=EDGE_CURVE ( 'NONE', #12955, #45920, #40244, .T. ) ;
#2717=CARTESIAN_POINT ( 'NONE',  ( 13.00000000000000178, -17.50000000000000000, 15.70499999999969809 ) ) ;
#2727=LINE ( 'NONE', #3441, #54214 ) ;
#2732=DIRECTION ( 'NONE',  ( 0.000000000000000000, -0.9921567416492215186, -0.1249999999999996531 ) ) ;
#2733=CARTESIAN_POINT ( 'NONE',  ( 30.00000000000000000, -16.28999999999710369, 15.00000000000794920 ) ) ;
#2738=CARTESIAN_POINT ( 'NONE',  ( -29.50000000000000355, -12.00000000000000000, 10.69999999999999929 ) ) ;
#2740=DIRECTION ( 'NONE',  ( 0.4999999999989361843, 0.000000000000000000, -0.8660254037850529940 ) ) ;
#2741=AXIS2_PLACEMENT_3D ( 'NONE', #64332, #43438, #44128 ) ;
#2747=DIRECTION ( 'NONE',  ( -1.000000000000000000, 0.000000000000000000, 0.000000000000000000 ) ) ;
#2753=AXIS2_PLACEMENT_3D ( 'NONE', #233, #6227, #44043 ) ;
#2761=DIRECTION ( 'NONE',  ( 0.000000000000000000, -1.000000000000000000, 3.989863994748342081E-13 ) ) ;
#2762=CIRCLE ( 'NONE', #41130, 0.3500000000009988455 ) ;
#2765=CARTESIAN_POINT ( 'NONE',  ( 11.00000000000000000, -12.00000000000000000, -10.52786404500095863 ) ) ;
#2773=DIRECTION ( 'NONE',  ( 0.000000000000000000, 0.000000000000000000, 1.000000000000000000 ) ) ;
#2785=ORIENTED_EDGE ( 'NONE', *, *, #60594, .T. ) ;
#2790=ORIENTED_EDGE ( 'NONE', *, *, #9912, .F. ) ;
#2791=CARTESIAN_POINT ( 'NONE',  ( 11.00000000000000000, -9.200000000000120082, -17.30000000000000071 ) ) ;
#2794=DIRECTION ( 'NONE',  ( 1.000000000000000000, -0.000000000000000000, -0.000000000000000000 ) ) ;
#2797=CARTESIAN_POINT ( 'NONE',  ( -11.50000000000000000, -11.50000000000100009, 15.00000000000084910 ) ) ;
#2798=CARTESIAN_POINT ( 'NONE',  ( 11.00000000000000000, -5.200000000000001066, -26.59999999999999787 ) ) ;
#2800=CARTESIAN_POINT ( 'NONE',  ( 11.00000000000000000, -12.00000000000000000, -11.03137303340310282 ) ) ;
#2805=DIRECTION ( 'NONE',  ( 0.000000000000000000, -1.000000000000000000, 0.000000000000000000 ) ) ;
#2815=VERTEX_POINT ( 'NONE', #40598 ) ;
#2820=AXIS2_PLACEMENT_3D ( 'NONE', #36517, #36164, #20955 ) ;
#2823=DIRECTION ( 'NONE',  ( 0.000000000000000000, 0.000000000000000000, -1.000000000000000000 ) ) ;
#2827=EDGE_LOOP ( 'NONE', ( #35546, #61651, #61886, #57829, #60828, #10843, #34226, #22448, #53651, #51118, #32783 ) ) ;
#2832=LINE ( 'NONE', #18043, #46014 ) ;
#2842=DIRECTION ( 'NONE',  ( 0.000000000000000000, 1.000000000000000000, 0.000000000000000000 ) ) ;
#2852=ORIENTED_EDGE ( 'NONE', *, *, #23298, .T. ) ;
#2853=EDGE_CURVE ( 'NONE', #1375, #17432, #14786, .T. ) ;
#2863=AXIS2_PLACEMENT_3D ( 'NONE', #55635, #22432, #7177 ) ;
#2868=ORIENTED_EDGE ( 'NONE', *, *, #14066, .T. ) ;
#2870=VECTOR ( 'NONE', #6616, 1000.000000000000000 ) ;
#2872=CARTESIAN_POINT ( 'NONE',  ( -15.50000000000000000, -1.037157890325000054, 22.50000000000000000 ) ) ;
#2874=AXIS2_PLACEMENT_3D ( 'NONE', #18911, #57436, #30917 ) ;
#2876=CARTESIAN_POINT ( 'NONE',  ( 24.00000000000000000, -15.50000000000000000, 19.33772233983200195 ) ) ;
#2880=ORIENTED_EDGE ( 'NONE', *, *, #68126, .T. ) ;
#2881=LINE ( 'NONE', #35754, #18572 ) ;
#2893=CARTESIAN_POINT ( 'NONE',  ( 30.00000000000000000, -17.00000000000000000, 15.70499999999969809 ) ) ;
#2894=DIRECTION ( 'NONE',  ( 0.000000000000000000, 1.000000000000000000, 0.000000000000000000 ) ) ;
#2902=VECTOR ( 'NONE', #47633, 1000.000000000000000 ) ;
#2909=EDGE_CURVE ( 'NONE', #17317, #69297, #64806, .T. ) ;
#2911=VECTOR ( 'NONE', #12543, 1000.000000000000000 ) ;
#2912=AXIS2_PLACEMENT_3D ( 'NONE', #12413, #66527, #44957 ) ;
#2931=VERTEX_POINT ( 'NONE', #17868 ) ;
#2938=DIRECTION ( 'NONE',  ( 0.000000000000000000, 0.6857142857146703019, -0.7278708115914659382 ) ) ;
#2950=ORIENTED_EDGE ( 'NONE', *, *, #30654, .F. ) ;
#2964=ORIENTED_EDGE ( 'NONE', *, *, #8071, .F. ) ;
#2965=VERTEX_POINT ( 'NONE', #45423 ) ;
#2969=VECTOR ( 'NONE', #37503, 1000.000000000000000 ) ;
#2971=CARTESIAN_POINT ( 'NONE',  ( -28.00000000000000000, -15.50000000000000000, 14.50000000000000000 ) ) ;
#2980=ADVANCED_FACE ( 'NONE', ( #1594 ), #29865, .F. ) ;
#2989=EDGE_CURVE ( 'NONE', #11608, #39751, #45779, .T. ) ;
#2991=DIRECTION ( 'NONE',  ( 0.000000000000000000, -1.000000000000000000, 0.000000000000000000 ) ) ;
#2992=DIRECTION ( 'NONE',  ( 0.000000000000000000, -0.7057491738665943037, -0.7084617869628675457 ) ) ;
#2995=CARTESIAN_POINT ( 'NONE',  ( 13.00000000000000178, -16.64230188589299786, -14.64519951917100116 ) ) ;
#2996=ADVANCED_FACE ( 'NONE', ( #3007 ), #23517, .T. ) ;
#2997=CARTESIAN_POINT ( 'NONE',  ( 29.50000000000000355, -11.50000000000100009, -15.00000000000084910 ) ) ;
#3007=FACE_OUTER_BOUND ( 'NONE', #21735, .T. ) ;
#3012=CARTESIAN_POINT ( 'NONE',  ( 11.75000000000000000, -5.200000000000001066, 26.25000000000000000 ) ) ;
#3016=DIRECTION ( 'NONE',  ( 0.000000000000000000, 0.000000000000000000, 1.000000000000000000 ) ) ;
#3020=LINE ( 'NONE', #24587, #66702 ) ;
#3021=ORIENTED_EDGE ( 'NONE', *, *, #19474, .F. ) ;
#3022=CARTESIAN_POINT ( 'NONE',  ( -24.00000000000000000, -17.50000000000000000, -19.33772233983200195 ) ) ;
#3024=AXIS2_PLACEMENT_3D ( 'NONE', #51443, #18557, #8655 ) ;
#3031=EDGE_LOOP ( 'NONE', ( #46741, #15515, #66730, #1213 ) ) ;
#3032=AXIS2_PLACEMENT_3D ( 'NONE', #25521, #62994, #57681 ) ;
#3041=ADVANCED_FACE ( 'NONE', ( #53212 ), #19260, .F. ) ;
#3042=LINE ( 'NONE', #29189, #5541 ) ;
#3044=VECTOR ( 'NONE', #18798, 1000.000000000000000 ) ;
#3054=CARTESIAN_POINT ( 'NONE',  ( 15.50000000000000000, -1.037157890325000054, -22.50000000000000000 ) ) ;
#3055=EDGE_CURVE ( 'NONE', #37912, #38019, #20313, .T. ) ;
#3060=AXIS2_PLACEMENT_3D ( 'NONE', #25438, #30392, #9174 ) ;
#3061=VERTEX_POINT ( 'NONE', #41533 ) ;
#3063=EDGE_CURVE ( 'NONE', #58960, #59292, #40827, .T. ) ;
#3066=CIRCLE ( 'NONE', #35814, 2.250000000000001776 ) ;
#3067=VECTOR ( 'NONE', #39151, 1000.000000000000000 ) ;
#3083=CARTESIAN_POINT ( 'NONE',  ( 14.25000000000000000, -2.500000000000000000, 21.77831216351300014 ) ) ;
#3086=FACE_OUTER_BOUND ( 'NONE', #51552, .T. ) ;
#3089=EDGE_CURVE ( 'NONE', #7820, #32087, #63101, .T. ) ;
#3090=DIRECTION ( 'NONE',  ( -1.000000000000000000, 0.000000000000000000, 0.000000000000000000 ) ) ;
#3092=DIRECTION ( 'NONE',  ( 1.000000000000000000, 0.000000000000000000, 0.000000000000000000 ) ) ;
#3093=ORIENTED_EDGE ( 'NONE', *, *, #1284, .T. ) ;
#3101=PLANE ( 'NONE',  #2263 ) ;
#3119=ADVANCED_FACE ( 'NONE', ( #4419 ), #9716, .T. ) ;
#3125=ORIENTED_EDGE ( 'NONE', *, *, #51177, .T. ) ;
#3127=LINE ( 'NONE', #7014, #41327 ) ;
#3131=ORIENTED_EDGE ( 'NONE', *, *, #65282, .T. ) ;
#3135=ORIENTED_EDGE ( 'NONE', *, *, #23330, .T. ) ;
#3139=EDGE_CURVE ( 'NONE', #17432, #64, #46824, .T. ) ;
#3143=VECTOR ( 'NONE', #69172, 999.9999999999998863 ) ;
#3159=ORIENTED_EDGE ( 'NONE', *, *, #63992, .F. ) ;
#3162=LINE ( 'NONE', #13407, #24979 ) ;
#3164=DIRECTION ( 'NONE',  ( 1.000000000000000000, 0.000000000000000000, 0.000000000000000000 ) ) ;
#3171=AXIS2_PLACEMENT_3D ( 'NONE', #4258, #47721, #47022 ) ;
#3172=LINE ( 'NONE', #19760, #44587 ) ;
#3179=VECTOR ( 'NONE', #34237, 1000.000000000000000 ) ;
#3183=CARTESIAN_POINT ( 'NONE',  ( -16.94999999999999929, -0.2000000000000000111, -22.50000000000000000 ) ) ;
#3186=ORIENTED_EDGE ( 'NONE', *, *, #28073, .T. ) ;
#3187=CARTESIAN_POINT ( 'NONE',  ( 11.50000000000000000, -11.50000000000000000, 11.00000000000000000 ) ) ;
#3188=FACE_OUTER_BOUND ( 'NONE', #37267, .T. ) ;
#3189=CARTESIAN_POINT ( 'NONE',  ( -15.50000000000000000, -5.000000000000000000, 22.50000000000000000 ) ) ;
#3190=AXIS2_PLACEMENT_3D ( 'NONE', #3692, #51429, #51784 ) ;
#3216=ORIENTED_EDGE ( 'NONE', *, *, #36059, .T. ) ;
#3226=LINE ( 'NONE', #20528, #7050 ) ;
#3227=DIRECTION ( 'NONE',  ( 0.000000000000000000, -1.000000000000000000, 3.989863994748342081E-13 ) ) ;
#3234=DIRECTION ( 'NONE',  ( 0.000000000000000000, 1.000000000000000000, 0.000000000000000000 ) ) ;
#3240=CARTESIAN_POINT ( 'NONE',  ( 11.00000000000000000, -13.79999999999979998, 17.64999999999988844 ) ) ;
#3245=CARTESIAN_POINT ( 'NONE',  ( -30.00000000000000000, -10.85999999999999943, 9.350000000000269651 ) ) ;
#3247=DIRECTION ( 'NONE',  ( 0.000000000000000000, -0.1111111111108840643, -0.9938079899999319178 ) ) ;
#3250=CYLINDRICAL_SURFACE ( 'NONE', #59219, 0.4999999999991850963 ) ;
#3255=FACE_OUTER_BOUND ( 'NONE', #16063, .T. ) ;
#3258=CARTESIAN_POINT ( 'NONE',  ( 30.00000000000000000, -17.00000000000000000, 15.70499999999969809 ) ) ;
#3265=DIRECTION ( 'NONE',  ( 1.000000000000000000, 0.000000000000000000, 0.000000000000000000 ) ) ;
#3267=VERTEX_POINT ( 'NONE', #58850 ) ;
#3272=VECTOR ( 'NONE', #62564, 1000.000000000000000 ) ;
#3282=CIRCLE ( 'NONE', #36036, 4.500000000000191847 ) ;
#3291=ORIENTED_EDGE ( 'NONE', *, *, #57211, .T. ) ;
#3295=DIRECTION ( 'NONE',  ( 0.000000000000000000, -1.000000000000000000, -6.036837696397607468E-13 ) ) ;
#3297=CARTESIAN_POINT ( 'NONE',  ( -15.50000000000000000, -0.2038245569916614930, 23.94337567297399971 ) ) ;
#3302=ORIENTED_EDGE ( 'NONE', *, *, #31296, .F. ) ;
#3307=LINE ( 'NONE', #15322, #23200 ) ;
#3308=EDGE_CURVE ( 'NONE', #4926, #35831, #60283, .T. ) ;
#3310=VECTOR ( 'NONE', #44330, 1000.000000000000000 ) ;
#3316=VERTEX_POINT ( 'NONE', #21713 ) ;
#3324=LINE ( 'NONE', #30545, #14302 ) ;
#3344=SURFACE_STYLE_FILL_AREA ( #18546 ) ;
#3349=DIRECTION ( 'NONE',  ( 1.000000000000000000, 0.000000000000000000, 0.000000000000000000 ) ) ;
#3351=LINE ( 'NONE', #18556, #5960 ) ;
#3353=DIRECTION ( 'NONE',  ( 0.000000000000000000, -0.1111111111108840643, -0.9938079899999319178 ) ) ;
#3355=ORIENTED_EDGE ( 'NONE', *, *, #7512, .T. ) ;
#3358=DIRECTION ( 'NONE',  ( -1.000000000000000000, 0.000000000000000000, 0.000000000000000000 ) ) ;
#3368=DIRECTION ( 'NONE',  ( 0.000000000000000000, 0.000000000000000000, 1.000000000000000000 ) ) ;
#3375=VERTEX_POINT ( 'NONE', #61520 ) ;
#3383=CIRCLE ( 'NONE', #57587, 2.000000000000001776 ) ;
#3388=ORIENTED_EDGE ( 'NONE', *, *, #14739, .T. ) ;
#3404=ORIENTED_EDGE ( 'NONE', *, *, #505, .T. ) ;
#3408=LINE ( 'NONE', #46530, #27763 ) ;
#3416=ORIENTED_EDGE ( 'NONE', *, *, #51689, .T. ) ;
#3421=DIRECTION ( 'NONE',  ( 1.000000000000000000, -0.000000000000000000, -0.000000000000000000 ) ) ;
#3427=CARTESIAN_POINT ( 'NONE',  ( 11.50000000000000000, -11.50000000000000000, 15.00000000000000000 ) ) ;
#3436=TOROIDAL_SURFACE ( 'NONE', #2321, 3.299999999999474909, 0.2000000000005234813 ) ;
#3438=ORIENTED_EDGE ( 'NONE', *, *, #49140, .T. ) ;
#3439=DIRECTION ( 'NONE',  ( -1.000000000000000000, 0.000000000000000000, 0.000000000000000000 ) ) ;
#3441=CARTESIAN_POINT ( 'NONE',  ( -25.50000000000000355, 0.000000000000000000, 24.12099999999999866 ) ) ;
#3455=EDGE_CURVE ( 'NONE', #32370, #69553, #19790, .T. ) ;
#3457=DIRECTION ( 'NONE',  ( 0.9375000000000006661, 0.000000000000000000, -0.3479852726768744020 ) ) ;
#3461=ADVANCED_FACE ( 'NONE', ( #18387 ), #67896, .T. ) ;
#3466=AXIS2_PLACEMENT_3D ( 'NONE', #13833, #35746, #30452 ) ;
#3470=LINE ( 'NONE', #41640, #39481 ) ;
#3491=DIRECTION ( 'NONE',  ( -1.000000000000000000, 0.000000000000000000, 0.000000000000000000 ) ) ;
#3495=AXIS2_PLACEMENT_3D ( 'NONE', #36380, #10213, #53700 ) ;
#3497=ORIENTED_EDGE ( 'NONE', *, *, #39576, .F. ) ;
#3500=CARTESIAN_POINT ( 'NONE',  ( -15.50000000000000000, -5.000000000000000000, -22.50000000000000000 ) ) ;
#3509=EDGE_CURVE ( 'NONE', #4816, #36688, #544, .T. ) ;
#3516=LINE ( 'NONE', #46639, #13510 ) ;
#3517=VECTOR ( 'NONE', #19741, 1000.000000000000000 ) ;
#3525=ADVANCED_FACE ( 'NONE', ( #5308 ), #28733, .F. ) ;
#3528=EDGE_CURVE ( 'NONE', #36748, #48159, #15236, .T. ) ;
#3530=ADVANCED_FACE ( 'NONE', ( #52336 ), #53048, .T. ) ;
#3533=CONICAL_SURFACE ( 'NONE', #5812, 1.621000000000000885, 0.7853981633974518317 ) ;
#3541=CIRCLE ( 'NONE', #52093, 2.000000000000001776 ) ;
#3543=CARTESIAN_POINT ( 'NONE',  ( 30.00000000000000000, -5.599999999999999645, 9.000000000000001776 ) ) ;
#3546=ORIENTED_EDGE ( 'NONE', *, *, #24130, .F. ) ;
#3556=FACE_OUTER_BOUND ( 'NONE', #15906, .T. ) ;
#3558=DIRECTION ( 'NONE',  ( 0.000000000000000000, -1.000000000000000000, 0.000000000000000000 ) ) ;
#3565=ORIENTED_EDGE ( 'NONE', *, *, #35368, .T. ) ;
#3566=FACE_OUTER_BOUND ( 'NONE', #31041, .T. ) ;
#3570=DIRECTION ( 'NONE',  ( -1.000000000000000000, 0.000000000000000000, 0.000000000000000000 ) ) ;
#3575=ORIENTED_EDGE ( 'NONE', *, *, #66520, .T. ) ;
#3579=PLANE ( 'NONE',  #5205 ) ;
#3597=CARTESIAN_POINT ( 'NONE',  ( -30.00000000000000000, -5.200000000000001066, -9.400000000000000355 ) ) ;
#3603=ORIENTED_EDGE ( 'NONE', *, *, #66111, .T. ) ;
#3604=ADVANCED_FACE ( 'NONE', ( #69659 ), #20158, .F. ) ;
#3605=DIRECTION ( 'NONE',  ( -0.8660254037844485886, 0.000000000000000000, -0.4999999999999827360 ) ) ;
#3608=DIRECTION ( 'NONE',  ( -1.000000000000000000, 0.000000000000000000, 0.000000000000000000 ) ) ;
#3610=ORIENTED_EDGE ( 'NONE', *, *, #62298, .F. ) ;
#3612=EDGE_CURVE ( 'NONE', #18662, #27404, #52484, .T. ) ;
#3616=PLANE ( 'NONE',  #58297 ) ;
#3617=DIRECTION ( 'NONE',  ( 0.000000000000000000, 0.000000000000000000, -1.000000000000000000 ) ) ;
#3619=EDGE_CURVE ( 'NONE', #36815, #35302, #5091, .T. ) ;
#3633=ORIENTED_EDGE ( 'NONE', *, *, #37832, .F. ) ;
#3635=DIRECTION ( 'NONE',  ( 1.000000000000000000, 0.000000000000000000, 0.000000000000000000 ) ) ;
#3659=EDGE_CURVE ( 'NONE', #32467, #18730, #38514, .T. ) ;
#3664=EDGE_CURVE ( 'NONE', #41185, #51551, #8435, .T. ) ;
#3677=ORIENTED_EDGE ( 'NONE', *, *, #60020, .F. ) ;
#3679=DIRECTION ( 'NONE',  ( 0.000000000000000000, -1.000000000000000000, 0.000000000000000000 ) ) ;
#3687=ORIENTED_EDGE ( 'NONE', *, *, #48386, .F. ) ;
#3688=FACE_OUTER_BOUND ( 'NONE', #61355, .T. ) ;
#3692=CARTESIAN_POINT ( 'NONE',  ( 17.51999999999999957, -15.50000000000000000, -26.00000000000000355 ) ) ;
#3693=ORIENTED_EDGE ( 'NONE', *, *, #48923, .F. ) ;
#3696=DIRECTION ( 'NONE',  ( -1.000000000000000000, 0.000000000000000000, 0.000000000000000000 ) ) ;
#3700=VERTEX_POINT ( 'NONE', #27900 ) ;
#3702=DIRECTION ( 'NONE',  ( 0.000000000000000000, 1.000000000000000000, 0.000000000000000000 ) ) ;
#3708=DIRECTION ( 'NONE',  ( 0.000000000000000000, 1.000000000000000000, 0.000000000000000000 ) ) ;
#3709=DIRECTION ( 'NONE',  ( -1.000000000000000000, 0.000000000000000000, 0.000000000000000000 ) ) ;
#3711=VECTOR ( 'NONE', #4679, 1000.000000000000000 ) ;
#3721=DIRECTION ( 'NONE',  ( 0.000000000000000000, -1.000000000000000000, 3.989863994748342081E-13 ) ) ;
#3723=DIRECTION ( 'NONE',  ( -0.000000000000000000, 1.000000000000000000, -0.000000000000000000 ) ) ;
#3724=ORIENTED_EDGE ( 'NONE', *, *, #56640, .F. ) ;
#3725=LINE ( 'NONE', #36594, #8094 ) ;
#3736=CARTESIAN_POINT ( 'NONE',  ( -11.50000000000000000, -11.70000000000000284, -11.00000000000000000 ) ) ;
#3739=ORIENTED_EDGE ( 'NONE', *, *, #24449, .T. ) ;
#3741=ORIENTED_EDGE ( 'NONE', *, *, #19407, .F. ) ;
#3744=CIRCLE ( 'NONE', #15058, 4.000000000000000888 ) ;
#3746=ORIENTED_EDGE ( 'NONE', *, *, #37832, .T. ) ;
#3751=EDGE_CURVE ( 'NONE', #28596, #9113, #60752, .T. ) ;
#3752=AXIS2_PLACEMENT_3D ( 'NONE', #58775, #5024, #54516 ) ;
#3754=EDGE_CURVE ( 'NONE', #48682, #34666, #54876, .T. ) ;
#3760=DIRECTION ( 'NONE',  ( 0.000000000000000000, -0.1111111111108840643, -0.9938079899999319178 ) ) ;
#3762=AXIS2_PLACEMENT_3D ( 'NONE', #49136, #10962, #60082 ) ;
#3775=VECTOR ( 'NONE', #68253, 1000.000000000000000 ) ;
#3778=CARTESIAN_POINT ( 'NONE',  ( -11.00000000000000000, -5.599999999999999645, 27.00000000000000000 ) ) ;
#3780=FACE_OUTER_BOUND ( 'NONE', #37420, .T. ) ;
#3792=AXIS2_PLACEMENT_3D ( 'NONE', #23738, #28343, #39976 ) ;
#3794=CYLINDRICAL_SURFACE ( 'NONE', #39545, 2.250000000000001776 ) ;
#3800=DIRECTION ( 'NONE',  ( 1.000000000000000000, 0.000000000000000000, 0.000000000000000000 ) ) ;
#3804=EDGE_CURVE ( 'NONE', #1760, #37044, #30020, .T. ) ;
#3812=CARTESIAN_POINT ( 'NONE',  ( 11.50000000000000000, -11.50000000000100009, -15.00000000000084910 ) ) ;
#3820=ORIENTED_EDGE ( 'NONE', *, *, #42974, .F. ) ;
#3824=EDGE_CURVE ( 'NONE', #47349, #28596, #26606, .T. ) ;
#3825=PRODUCT_CONTEXT ( 'NONE', #11498, 'mechanical' ) ;
#3835=ORIENTED_EDGE ( 'NONE', *, *, #8071, .T. ) ;
#3837=AXIS2_PLACEMENT_3D ( 'NONE', #11107, #65217, #33706 ) ;
#3842=PLANE ( 'NONE',  #5415 ) ;
#3844=CIRCLE ( 'NONE', #15107, 3.499999999999855227 ) ;
#3847=LINE ( 'NONE', #68195, #3517 ) ;
#3849=DIRECTION ( 'NONE',  ( 0.000000000000000000, 0.000000000000000000, 1.000000000000000000 ) ) ;
#3850=CARTESIAN_POINT ( 'NONE',  ( 24.00000000000000000, -15.50000000000000000, 19.33772233983200195 ) ) ;
#3855=ORIENTED_EDGE ( 'NONE', *, *, #51825, .F. ) ;
#3863=EDGE_CURVE ( 'NONE', #41566, #21801, #41276, .T. ) ;
#3864=DIRECTION ( 'NONE',  ( -0.8660254037850523279, 0.000000000000000000, 0.4999999999989371835 ) ) ;
#3868=DIRECTION ( 'NONE',  ( 0.000000000000000000, 0.000000000000000000, 1.000000000000000000 ) ) ;
#3874=EDGE_CURVE ( 'NONE', #64729, #37150, #26083, .T. ) ;
#3878=CARTESIAN_POINT ( 'NONE',  ( 25.50000000000000355, -15.12100000000000044, 22.50000000000000000 ) ) ;
#3880=CARTESIAN_POINT ( 'NONE',  ( 30.00000000000000000, -11.70000000000000284, 12.50000000000000000 ) ) ;
#3884=DIRECTION ( 'NONE',  ( 0.000000000000000000, -1.000000000000000000, 0.000000000000000000 ) ) ;
#3888=CARTESIAN_POINT ( 'NONE',  ( 25.50000000000000355, -15.50000000000000000, 22.50000000000000000 ) ) ;
#3890=CARTESIAN_POINT ( 'NONE',  ( -25.49999999999869971, -17.50000000000000000, 22.50000000000000000 ) ) ;
#3903=DIRECTION ( 'NONE',  ( 1.000000000000000000, -0.000000000000000000, -0.000000000000000000 ) ) ;
#3904=ORIENTED_EDGE ( 'NONE', *, *, #56288, .F. ) ;
#3908=ORIENTED_EDGE ( 'NONE', *, *, #62298, .T. ) ;
#3911=DIRECTION ( 'NONE',  ( 1.000000000000000000, -0.000000000000000000, -0.000000000000000000 ) ) ;
#3913=CIRCLE ( 'NONE', #33283, 1.620999999999997332 ) ;
#3926=AXIS2_PLACEMENT_3D ( 'NONE', #36416, #41717, #43111 ) ;
#3928=CARTESIAN_POINT ( 'NONE',  ( 16.75000000000000000, -2.500000000000000000, 23.22168783648699986 ) ) ;
#3931=AXIS2_PLACEMENT_3D ( 'NONE', #61788, #18641, #17608 ) ;
#3935=ADVANCED_FACE ( 'NONE', ( #52962 ), #4172, .F. ) ;
#3939=CIRCLE ( 'NONE', #48000, 3.499999999999849454 ) ;
#3943=EDGE_LOOP ( 'NONE', ( #64335, #2578, #18772, #55088, #63262, #8375 ) ) ;
#3944=ORIENTED_EDGE ( 'NONE', *, *, #9244, .T. ) ;
#3946=AXIS2_PLACEMENT_3D ( 'NONE', #67895, #14858, #47024 ) ;
#3951=CARTESIAN_POINT ( 'NONE',  ( -11.00000000000000000, -13.79999999999979998, 17.30000000000000071 ) ) ;
#3959=CYLINDRICAL_SURFACE ( 'NONE', #40293, 0.3499999999998886224 ) ;
#3977=CARTESIAN_POINT ( 'NONE',  ( -11.00000000000000000, -11.50000000000000000, 15.00000000000000000 ) ) ;
#3979=DIRECTION ( 'NONE',  ( 0.000000000000000000, -2.854859206170826497E-12, 1.000000000000000000 ) ) ;
#3982=FACE_OUTER_BOUND ( 'NONE', #46968, .T. ) ;
#3998=CARTESIAN_POINT ( 'NONE',  ( -29.50000000000000355, -11.50000000000000000, -19.00000000000000000 ) ) ;
#4001=ORIENTED_EDGE ( 'NONE', *, *, #15083, .F. ) ;
#4004=DIRECTION ( 'NONE',  ( 0.000000000000000000, -1.000000000000000000, 0.000000000000000000 ) ) ;
#4008=AXIS2_PLACEMENT_3D ( 'NONE', #60290, #11847, #13600 ) ;
#4013=AXIS2_PLACEMENT_3D ( 'NONE', #34975, #18720, #12703 ) ;
#4020=ADVANCED_FACE ( 'NONE', ( #27122 ), #48687, .F. ) ;
#4024=EDGE_CURVE ( 'NONE', #26009, #29819, #53717, .T. ) ;
#4031=DIRECTION ( 'NONE',  ( 0.000000000000000000, 1.000000000000000000, 0.000000000000000000 ) ) ;
#4036=CARTESIAN_POINT ( 'NONE',  ( 14.25000000000000000, -0.2038245569916330158, 21.77831216351300014 ) ) ;
#4037=AXIS2_PLACEMENT_3D ( 'NONE', #24317, #46225, #67461 ) ;
#4044=AXIS2_PLACEMENT_3D ( 'NONE', #14396, #8734, #23940 ) ;
#4048=ORIENTED_EDGE ( 'NONE', *, *, #69876, .F. ) ;
#4062=CARTESIAN_POINT ( 'NONE',  ( -30.00000000000000000, -16.28999999999999915, 14.50000000000000000 ) ) ;
#4073=DIRECTION ( 'NONE',  ( 1.000000000000000000, -0.000000000000000000, 1.224646799147353207E-16 ) ) ;
#4079=VERTEX_POINT ( 'NONE', #17192 ) ;
#4085=DIRECTION ( 'NONE',  ( -1.000000000000000000, 0.000000000000000000, 0.000000000000000000 ) ) ;
#4088=ORIENTED_EDGE ( 'NONE', *, *, #48607, .F. ) ;
#4089=VERTEX_POINT ( 'NONE', #33797 ) ;
#4097=VECTOR ( 'NONE', #53812, 1000.000000000000000 ) ;
#4104=VECTOR ( 'NONE', #39112, 1000.000000000000000 ) ;
#4107=VERTEX_POINT ( 'NONE', #251 ) ;
#4109=ORIENTED_EDGE ( 'NONE', *, *, #40177, .F. ) ;
#4119=ADVANCED_FACE ( 'NONE', ( #21465 ), #1286, .F. ) ;
#4128=VECTOR ( 'NONE', #32655, 1000.000000000000000 ) ;
#4129=CARTESIAN_POINT ( 'NONE',  ( 30.00000000000000000, -12.00000000000000000, 12.20000000000000107 ) ) ;
#4130=ORIENTED_EDGE ( 'NONE', *, *, #39443, .F. ) ;
#4133=DIRECTION ( 'NONE',  ( 0.000000000000000000, 1.000000000000000000, 0.000000000000000000 ) ) ;
#4141=DIRECTION ( 'NONE',  ( -0.000000000000000000, 1.000000000000000000, -0.000000000000000000 ) ) ;
#4145=CIRCLE ( 'NONE', #43661, 4.500000000000191847 ) ;
#4148=VECTOR ( 'NONE', #36924, 1000.000000000000000 ) ;
#4153=LINE ( 'NONE', #58591, #47431 ) ;
#4156=EDGE_CURVE ( 'NONE', #64280, #17297, #43732, .T. ) ;
#4161=ORIENTED_EDGE ( 'NONE', *, *, #6444, .F. ) ;
#4164=FACE_BOUND ( 'NONE', #5904, .T. ) ;
#4165=LINE ( 'NONE', #42322, #709 ) ;
#4171=EDGE_CURVE ( 'NONE', #30626, #5395, #64601, .T. ) ;
#4172=PLANE ( 'NONE',  #19825 ) ;
#4188=AXIS2_PLACEMENT_3D ( 'NONE', #53003, #19492, #9867 ) ;
#4194=CARTESIAN_POINT ( 'NONE',  ( 16.74999999999999289, -0.3152037684892571301, -22.74589050208021845 ) ) ;
#4196=EDGE_CURVE ( 'NONE', #35525, #57629, #55383, .T. ) ;
#4204=EDGE_CURVE ( 'NONE', #14841, #66296, #29537, .T. ) ;
#4205=ORIENTED_EDGE ( 'NONE', *, *, #46348, .T. ) ;
#4207=VECTOR ( 'NONE', #48089, 1000.000000000000114 ) ;
#4208=PLANE ( 'NONE',  #67377 ) ;
#4221=DIRECTION ( 'NONE',  ( 1.000000000000000000, 0.000000000000000000, 0.000000000000000000 ) ) ;
#4225=CARTESIAN_POINT ( 'NONE',  ( 30.00000000000000000, -17.14999999999999858, -27.00000000000000000 ) ) ;
#4230=CYLINDRICAL_SURFACE ( 'NONE', #12377, 0.3500000000002719824 ) ;
#4234=CARTESIAN_POINT ( 'NONE',  ( 11.00000000000000000, -5.599999999999999645, 9.400000000000000355 ) ) ;
#4245=DIRECTION ( 'NONE',  ( -1.000000000000000000, 0.000000000000000000, 0.000000000000000000 ) ) ;
#4246=AXIS2_PLACEMENT_3D ( 'NONE', #27082, #10132, #16127 ) ;
#4254=ORIENTED_EDGE ( 'NONE', *, *, #3619, .F. ) ;
#4255=CARTESIAN_POINT ( 'NONE',  ( 13.00000000000000178, -15.50000000000000000, 14.50000000000000000 ) ) ;
#4256=ORIENTED_EDGE ( 'NONE', *, *, #18153, .F. ) ;
#4258=CARTESIAN_POINT ( 'NONE',  ( 15.50000000000000000, -5.000000000000000000, 22.50000000000000000 ) ) ;
#4265=ORIENTED_EDGE ( 'NONE', *, *, #2032, .T. ) ;
#4266=CARTESIAN_POINT ( 'NONE',  ( -30.00000000000000000, -13.79999999999979998, 17.64999999999988844 ) ) ;
#4275=EDGE_CURVE ( 'NONE', #59373, #24243, #49106, .T. ) ;
#4290=ORIENTED_EDGE ( 'NONE', *, *, #19172, .T. ) ;
#4292=VERTEX_POINT ( 'NONE', #37228 ) ;
#4293=EDGE_CURVE ( 'NONE', #8038, #11924, #16003, .T. ) ;
#4304=CIRCLE ( 'NONE', #60701, 0.5000000000001392220 ) ;
#4307=CIRCLE ( 'NONE', #13304, 1.620999999999997332 ) ;
#4320=ORIENTED_EDGE ( 'NONE', *, *, #14739, .F. ) ;
#4321=CARTESIAN_POINT ( 'NONE',  ( -11.75000000000000000, -5.200000000000001066, 26.25000000000000000 ) ) ;
#4322=DIRECTION ( 'NONE',  ( 0.000000000000000000, 1.000000000000000000, 0.000000000000000000 ) ) ;
#4324=VECTOR ( 'NONE', #64231, 1000.000000000000000 ) ;
#4339=DIRECTION ( 'NONE',  ( 0.000000000000000000, 0.000000000000000000, -1.000000000000000000 ) ) ;
#4343=ORIENTED_EDGE ( 'NONE', *, *, #24183, .F. ) ;
#4349=ADVANCED_FACE ( 'NONE', ( #69388 ), #31233, .T. ) ;
#4353=CARTESIAN_POINT ( 'NONE',  ( 25.50000000000000355, -15.50000000000000000, -22.50000000000000000 ) ) ;
#4355=ORIENTED_EDGE ( 'NONE', *, *, #6868, .T. ) ;
#4356=LINE ( 'NONE', #10343, #58599 ) ;
#4357=CYLINDRICAL_SURFACE ( 'NONE', #30951, 4.500000000000188294 ) ;
#4361=VECTOR ( 'NONE', #19726, 1000.000000000000000 ) ;
#4362=CARTESIAN_POINT ( 'NONE',  ( 11.00000000000000000, -10.85999999999999943, -9.000000000000001776 ) ) ;
#4365=EDGE_LOOP ( 'NONE', ( #25783, #56255 ) ) ;
#4367=VERTEX_POINT ( 'NONE', #26609 ) ;
#4370=LINE ( 'NONE', #30514, #54770 ) ;
#4378=ORIENTED_EDGE ( 'NONE', *, *, #22449, .T. ) ;
#4382=CARTESIAN_POINT ( 'NONE',  ( -11.50000000000000000, -12.00000000000000000, -10.69999999999999929 ) ) ;
#4387=DIRECTION ( 'NONE',  ( 0.000000000000000000, 0.000000000000000000, 1.000000000000000000 ) ) ;
#4390=ADVANCED_FACE ( 'NONE', ( #4696 ), #438, .F. ) ;
#4396=CARTESIAN_POINT ( 'NONE',  ( 15.50000000000000000, -0.2038245569916610489, 21.05662432702600029 ) ) ;
#4407=FACE_OUTER_BOUND ( 'NONE', #30855, .T. ) ;
#4419=FACE_OUTER_BOUND ( 'NONE', #51295, .T. ) ;
#4423=AXIS2_PLACEMENT_3D ( 'NONE', #18803, #61934, #24468 ) ;
#4436=DIRECTION ( 'NONE',  ( 0.000000000000000000, 0.000000000000000000, -1.000000000000000000 ) ) ;
#4438=LINE ( 'NONE', #64184, #62088 ) ;
#4441=VERTEX_POINT ( 'NONE', #33972 ) ;
#4462=ORIENTED_EDGE ( 'NONE', *, *, #3874, .T. ) ;
#4466=CARTESIAN_POINT ( 'NONE',  ( 15.50000000000000000, 0.000000000000000000, -22.50000000000000000 ) ) ;
#4467=CARTESIAN_POINT ( 'NONE',  ( -17.51999999999999957, -15.50000000000000000, -26.00000000000000355 ) ) ;
#4468=ORIENTED_EDGE ( 'NONE', *, *, #43195, .F. ) ;
#4478=ORIENTED_EDGE ( 'NONE', *, *, #24906, .T. ) ;
#4484=VERTEX_POINT ( 'NONE', #2155 ) ;
#4494=CARTESIAN_POINT ( 'NONE',  ( -11.00000000000000000, -11.70000000000000284, -12.50000000000000000 ) ) ;
#4497=CARTESIAN_POINT ( 'NONE',  ( -13.00000000000000178, -17.35230188589299516, -15.35019951917100478 ) ) ;
#4508=VERTEX_POINT ( 'NONE', #22357 ) ;
#4509=VECTOR ( 'NONE', #25546, 1000.000000000000000 ) ;
#4513=CARTESIAN_POINT ( 'NONE',  ( -14.25000000000000000, -0.2038245569916330158, 23.22168783648699986 ) ) ;
#4515=CARTESIAN_POINT ( 'NONE',  ( -15.50000000000000000, -1.037157890325000054, -22.50000000000000000 ) ) ;
#4530=DIRECTION ( 'NONE',  ( 0.000000000000000000, -1.000000000000000000, 0.000000000000000000 ) ) ;
#4549=EDGE_CURVE ( 'NONE', #32931, #16848, #6435, .T. ) ;
#4554=CARTESIAN_POINT ( 'NONE',  ( -15.50000000000000000, -0.2038245569916614930, -23.94337567297399971 ) ) ;
#4556=LINE ( 'NONE', #47328, #6878 ) ;
#4557=AXIS2_PLACEMENT_3D ( 'NONE', #49999, #39046, #65582 ) ;
#4559=CIRCLE ( 'NONE', #19068, 4.000000000000000888 ) ;
#4566=DIRECTION ( 'NONE',  ( -1.000000000000000000, 0.000000000000000000, 0.000000000000000000 ) ) ;
#4570=DIRECTION ( 'NONE',  ( 0.000000000000000000, 0.000000000000000000, 1.000000000000000000 ) ) ;
#4576=DIRECTION ( 'NONE',  ( -1.000000000000000000, 0.000000000000000000, 0.000000000000000000 ) ) ;
#4577=ORIENTED_EDGE ( 'NONE', *, *, #57799, .T. ) ;
#4579=CIRCLE ( 'NONE', #33914, 0.5000000000079367624 ) ;
#4583=ORIENTED_EDGE ( 'NONE', *, *, #60205, .T. ) ;
#4585=DIRECTION ( 'NONE',  ( 0.000000000000000000, -1.000000000000000000, 0.000000000000000000 ) ) ;
#4588=DIRECTION ( 'NONE',  ( 0.000000000000000000, 1.000000000000000000, 0.000000000000000000 ) ) ;
#4595=VERTEX_POINT ( 'NONE', #56938 ) ;
#4596=EDGE_CURVE ( 'NONE', #20240, #701, #25552, .T. ) ;
#4599=VERTEX_POINT ( 'NONE', #57299 ) ;
#4612=EDGE_CURVE ( 'NONE', #24514, #64746, #44589, .T. ) ;
#4626=VERTEX_POINT ( 'NONE', #67568 ) ;
#4645=AXIS2_PLACEMENT_3D ( 'NONE', #40648, #2467, #41346 ) ;
#4648=DIRECTION ( 'NONE',  ( 0.000000000000000000, 1.000000000000000000, 0.000000000000000000 ) ) ;
#4650=LINE ( 'NONE', #9603, #60613 ) ;
#4666=DIRECTION ( 'NONE',  ( -1.000000000000000000, 0.000000000000000000, 0.000000000000000000 ) ) ;
#4667=FACE_OUTER_BOUND ( 'NONE', #68562, .T. ) ;
#4675=FACE_OUTER_BOUND ( 'NONE', #2618, .T. ) ;
#4676=ORIENTED_EDGE ( 'NONE', *, *, #56521, .F. ) ;
#4679=DIRECTION ( 'NONE',  ( 0.000000000000000000, 1.000000000000000000, 0.000000000000000000 ) ) ;
#4680=CARTESIAN_POINT ( 'NONE',  ( -11.00000000000000000, -17.14999999999900027, -26.64999999999900027 ) ) ;
#4681=CARTESIAN_POINT ( 'NONE',  ( 15.50000000000000000, -17.50000000000000000, 22.50000000000000000 ) ) ;
#4684=ORIENTED_EDGE ( 'NONE', *, *, #39373, .T. ) ;
#4693=CARTESIAN_POINT ( 'NONE',  ( -11.00000000000000000, -15.46862696659690073, 14.50000000000000000 ) ) ;
#4696=FACE_OUTER_BOUND ( 'NONE', #4721, .T. ) ;
#4701=EDGE_LOOP ( 'NONE', ( #11092, #8591, #13126, #47125 ) ) ;
#4702=AXIS2_PLACEMENT_3D ( 'NONE', #4859, #15811, #10157 ) ;
#4705=FACE_OUTER_BOUND ( 'NONE', #53811, .T. ) ;
#4714=DIRECTION ( 'NONE',  ( 0.000000000000000000, 0.000000000000000000, -1.000000000000000000 ) ) ;
#4718=PLANE ( 'NONE',  #11355 ) ;
#4721=EDGE_LOOP ( 'NONE', ( #19732, #61744, #10164, #19730, #66416, #53845, #61548, #62593, #51560, #18821, #37537, #1042 ) ) ;
#4729=VERTEX_POINT ( 'NONE', #48096 ) ;
#4742=CARTESIAN_POINT ( 'NONE',  ( 16.74999999999999289, -0.3152037684892571301, 22.25410949791978155 ) ) ;
#4747=LINE ( 'NONE', #31626, #937 ) ;
#4754=CARTESIAN_POINT ( 'NONE',  ( 11.00000000000000000, -15.97213595500069871, -14.50000000000000000 ) ) ;
#4772=VERTEX_POINT ( 'NONE', #10959 ) ;
#4792=CIRCLE ( 'NONE', #42031, 0.3499999999998879008 ) ;
#4794=ORIENTED_EDGE ( 'NONE', *, *, #23519, .T. ) ;
#4801=LINE ( 'NONE', #30276, #7386 ) ;
#4802=ORIENTED_EDGE ( 'NONE', *, *, #41907, .T. ) ;
#4807=DIRECTION ( 'NONE',  ( 0.000000000000000000, 0.7096009616570518874, 0.7046037717862339012 ) ) ;
#4808=ORIENTED_EDGE ( 'NONE', *, *, #66111, .F. ) ;
#4811=VECTOR ( 'NONE', #41250, 1000.000000000000114 ) ;
#4815=DIRECTION ( 'NONE',  ( 0.000000000000000000, 1.000000000000000000, 0.000000000000000000 ) ) ;
#4816=VERTEX_POINT ( 'NONE', #64698 ) ;
#4848=ORIENTED_EDGE ( 'NONE', *, *, #60594, .F. ) ;
#4851=ORIENTED_EDGE ( 'NONE', *, *, #23641, .T. ) ;
#4856=DIRECTION ( 'NONE',  ( 0.000000000000000000, -5.800915303574361727E-12, -1.000000000000000000 ) ) ;
#4859=CARTESIAN_POINT ( 'NONE',  ( -15.50000000000000000, -0.2000000000000000111, -22.50000000000000000 ) ) ;
#4862=ORIENTED_EDGE ( 'NONE', *, *, #50829, .F. ) ;
#4881=FACE_OUTER_BOUND ( 'NONE', #68791, .T. ) ;
#4886=CARTESIAN_POINT ( 'NONE',  ( 30.00000000000000000, -9.487228132326899654, 12.50000000000000000 ) ) ;
#4896=LINE ( 'NONE', #27156, #46927 ) ;
#4909=CARTESIAN_POINT ( 'NONE',  ( 30.00000000000000000, -10.85999999999999943, 9.000000000000001776 ) ) ;
#4912=CARTESIAN_POINT ( 'NONE',  ( -25.50000000000000355, -5.578999999999999737, -22.50000000000000000 ) ) ;
#4922=DIRECTION ( 'NONE',  ( -1.000000000000000000, 0.000000000000000000, 0.000000000000000000 ) ) ;
#4926=VERTEX_POINT ( 'NONE', #59743 ) ;
#4927=CARTESIAN_POINT ( 'NONE',  ( -30.00000000000000000, -14.04000000000000092, -17.04524521594300523 ) ) ;
#4932=PLANE ( 'NONE',  #18642 ) ;
#4934=PLANE ( 'NONE',  #51985 ) ;
#4943=CARTESIAN_POINT ( 'NONE',  ( 15.50000000000000000, -0.2000000000000000111, -22.50000000000000000 ) ) ;
#4949=ORIENTED_EDGE ( 'NONE', *, *, #35078, .F. ) ;
#4953=CARTESIAN_POINT ( 'NONE',  ( 15.50000000000000000, -0.2038245569916610489, -23.94337567297399971 ) ) ;
#4967=ORIENTED_EDGE ( 'NONE', *, *, #64706, .F. ) ;
#4970=CARTESIAN_POINT ( 'NONE',  ( -25.49999999999869971, -15.50000000000000000, -22.50000000000000000 ) ) ;
#4974=LINE ( 'NONE', #16974, #2969 ) ;
#4977=DIRECTION ( 'NONE',  ( 0.000000000000000000, -0.7071067811865496822, 0.7071067811865454633 ) ) ;
#4978=CARTESIAN_POINT ( 'NONE',  ( 15.50000000000000000, -17.50000000000000000, -25.99999999999985079 ) ) ;
#4984=DIRECTION ( 'NONE',  ( -1.000000000000000000, 0.000000000000000000, 0.000000000000000000 ) ) ;
#4987=ORIENTED_EDGE ( 'NONE', *, *, #60049, .T. ) ;
#4995=DIRECTION ( 'NONE',  ( 0.000000000000000000, 0.000000000000000000, -1.000000000000000000 ) ) ;
#5002=CARTESIAN_POINT ( 'NONE',  ( 15.50000000000000000, -1.037157890325000054, 22.50000000000000000 ) ) ;
#5014=AXIS2_PLACEMENT_3D ( 'NONE', #5320, #69669, #11621 ) ;
#5024=DIRECTION ( 'NONE',  ( 0.000000000000000000, 0.000000000000000000, 1.000000000000000000 ) ) ;
#5038=ADVANCED_FACE ( 'NONE', ( #51915 ), #40939, .F. ) ;
#5042=ORIENTED_EDGE ( 'NONE', *, *, #23162, .F. ) ;
#5047=CARTESIAN_POINT ( 'NONE',  ( 29.50000000000000355, -11.50000000000000000, -15.00000000000000000 ) ) ;
#5050=AXIS2_PLACEMENT_3D ( 'NONE', #56742, #57096, #62747 ) ;
#5051=LINE ( 'NONE', #10699, #38761 ) ;
#5061=ORIENTED_EDGE ( 'NONE', *, *, #39679, .F. ) ;
#5063=DIRECTION ( 'NONE',  ( 0.000000000000000000, 0.000000000000000000, 1.000000000000000000 ) ) ;
#5065=CARTESIAN_POINT ( 'NONE',  ( -15.91242688423474050, -0.3152598339554945062, -23.70526090034005051 ) ) ;
#5087=EDGE_CURVE ( 'NONE', #59852, #40687, #46248, .T. ) ;
#5088=ORIENTED_EDGE ( 'NONE', *, *, #58233, .T. ) ;
#5089=CARTESIAN_POINT ( 'NONE',  ( 30.00000000000000000, -13.54524521594299991, -17.53999999999999915 ) ) ;
#5091=CIRCLE ( 'NONE', #1673, 3.499999999999849454 ) ;
#5092=CARTESIAN_POINT ( 'NONE',  ( 11.50000000000000000, -11.50000000000000000, -15.00000000000000000 ) ) ;
#5107=LINE ( 'NONE', #27024, #57914 ) ;
#5113=EDGE_CURVE ( 'NONE', #9139, #45628, #11890, .T. ) ;
#5116=CARTESIAN_POINT ( 'NONE',  ( -15.50000000000000000, -0.2000000000000000111, -25.79999999999947136 ) ) ;
#5118=CARTESIAN_POINT ( 'NONE',  ( -23.48000000000000043, -15.50000000000000000, 26.00000000000000355 ) ) ;
#5120=EDGE_CURVE ( 'NONE', #50235, #32493, #66050, .T. ) ;
#5122=DIRECTION ( 'NONE',  ( 1.000000000000000000, 0.000000000000000000, 0.000000000000000000 ) ) ;
#5128=ORIENTED_EDGE ( 'NONE', *, *, #20766, .T. ) ;
#5129=ORIENTED_EDGE ( 'NONE', *, *, #30495, .F. ) ;
#5138=CARTESIAN_POINT ( 'NONE',  ( 30.00000000000000000, -17.00000000000000000, -15.70499999999969809 ) ) ;
#5148=DIRECTION ( 'NONE',  ( 0.000000000000000000, 0.000000000000000000, 1.000000000000000000 ) ) ;
#5153=AXIS2_PLACEMENT_3D ( 'NONE', #16452, #38034, #54288 ) ;
#5157=EDGE_CURVE ( 'NONE', #38076, #1682, #37749, .T. ) ;
#5159=VERTEX_POINT ( 'NONE', #53328 ) ;
#5166=FACE_OUTER_BOUND ( 'NONE', #12152, .T. ) ;
#5177=DIRECTION ( 'NONE',  ( 0.000000000000000000, 0.000000000000000000, 1.000000000000000000 ) ) ;
#5180=DIRECTION ( 'NONE',  ( 0.000000000000000000, -0.7096009616570518874, 0.7046037717862339012 ) ) ;
#5184=DIRECTION ( 'NONE',  ( 0.000000000000000000, 0.000000000000000000, 1.000000000000000000 ) ) ;
#5186=DIRECTION ( 'NONE',  ( -1.000000000000000000, 0.000000000000000000, 0.000000000000000000 ) ) ;
#5187=VECTOR ( 'NONE', #56032, 1000.000000000000000 ) ;
#5190=CARTESIAN_POINT ( 'NONE',  ( -29.25000000000000000, -5.200000000000001066, 26.25000000000000000 ) ) ;
#5191=ORIENTED_EDGE ( 'NONE', *, *, #42420, .F. ) ;
#5192=FACE_OUTER_BOUND ( 'NONE', #46422, .T. ) ;
#5194=VECTOR ( 'NONE', #58164, 1000.000000000000000 ) ;
#5196=ADVANCED_FACE ( 'NONE', ( #21139 ), #14784, .F. ) ;
#5205=AXIS2_PLACEMENT_3D ( 'NONE', #13827, #35380, #67925 ) ;
#5211=PLANE ( 'NONE',  #11142 ) ;
#5223=LINE ( 'NONE', #601, #26106 ) ;
#5224=EDGE_LOOP ( 'NONE', ( #53534, #51564, #4320, #6005 ) ) ;
#5225=FACE_OUTER_BOUND ( 'NONE', #66472, .T. ) ;
#5250=CARTESIAN_POINT ( 'NONE',  ( 11.50000000000000000, -11.50000000000000000, 15.00000000000000000 ) ) ;
#5252=AXIS2_PLACEMENT_3D ( 'NONE', #53220, #26328, #47886 ) ;
#5255=VERTEX_POINT ( 'NONE', #59663 ) ;
#5257=VECTOR ( 'NONE', #18796, 1000.000000000000000 ) ;
#5268=CARTESIAN_POINT ( 'NONE',  ( 30.00000000000000000, -14.33999999999999986, -14.50000000000000000 ) ) ;
#5276=DIRECTION ( 'NONE',  ( 0.000000000000000000, -1.000000000000000000, 0.000000000000000000 ) ) ;
#5281=CYLINDRICAL_SURFACE ( 'NONE', #45007, 0.3499999999999614531 ) ;
#5285=LINE ( 'NONE', #28216, #21902 ) ;
#5291=DIRECTION ( 'NONE',  ( -1.000000000000000000, 0.000000000000000000, 0.000000000000000000 ) ) ;
#5292=EDGE_CURVE ( 'NONE', #25620, #1191, #17549, .T. ) ;
#5304=EDGE_CURVE ( 'NONE', #34775, #33396, #28796, .T. ) ;
#5308=FACE_OUTER_BOUND ( 'NONE', #8413, .T. ) ;
#5320=CARTESIAN_POINT ( 'NONE',  ( 15.50000000000000000, -0.2000000000000000111, -22.50000000000000000 ) ) ;
#5321=EDGE_CURVE ( 'NONE', #59441, #56315, #613, .T. ) ;
#5324=CARTESIAN_POINT ( 'NONE',  ( 29.50000000000000355, -11.70000000000000284, -11.00000000000000000 ) ) ;
#5326=VECTOR ( 'NONE', #2337, 999.9999999999998863 ) ;
#5332=VERTEX_POINT ( 'NONE', #5916 ) ;
#5340=DIRECTION ( 'NONE',  ( 0.000000000000000000, 1.000000000000000000, 0.000000000000000000 ) ) ;
#5348=DIRECTION ( 'NONE',  ( -1.000000000000000000, 0.000000000000000000, 0.000000000000000000 ) ) ;
#5366=DIRECTION ( 'NONE',  ( 0.000000000000000000, 0.000000000000000000, -1.000000000000000000 ) ) ;
#5374=EDGE_LOOP ( 'NONE', ( #22596, #46775, #38858, #21998 ) ) ;
#5380=CARTESIAN_POINT ( 'NONE',  ( 13.00000000000000178, -17.35230188589299871, 15.35019951917099945 ) ) ;
#5382=LINE ( 'NONE', #26233, #63954 ) ;
#5388=B_SPLINE_CURVE_WITH_KNOTS ( 'NONE', 3,
 ( #30707, #15145, #52271, #4194, #68177, #25768 ),
 .UNSPECIFIED., .F., .F.,
 ( 4, 2, 4 ),
 ( 1.820537833122030991, 2.555393473688635453, 3.290249114255240137 ),
 .UNSPECIFIED. ) ;
#5390=ORIENTED_EDGE ( 'NONE', *, *, #66520, .F. ) ;
#5392=CARTESIAN_POINT ( 'NONE',  ( -28.00000000000000000, -17.50000000000000000, -20.05051025721700242 ) ) ;
#5394=FACE_OUTER_BOUND ( 'NONE', #17067, .T. ) ;
#5395=VERTEX_POINT ( 'NONE', #16874 ) ;
#5397=EDGE_LOOP ( 'NONE', ( #15840, #40139, #67385, #117, #801, #5510, #69473, #21839, #53673, #6333, #51791, #11188, #1559, #37850, #39398, #7037 ) ) ;
#5398=EDGE_CURVE ( 'NONE', #28218, #51205, #50078, .T. ) ;
#5404=EDGE_CURVE ( 'NONE', #41930, #27322, #1628, .T. ) ;
#5415=AXIS2_PLACEMENT_3D ( 'NONE', #63947, #58290, #41666 ) ;
#5418=PLANE ( 'NONE',  #60342 ) ;
#5420=AXIS2_PLACEMENT_3D ( 'NONE', #13441, #67185, #61170 ) ;
#5426=DIRECTION ( 'NONE',  ( -1.000000000000000000, 0.000000000000000000, 0.000000000000000000 ) ) ;
#5427=CIRCLE ( 'NONE', #14440, 4.500000000000191847 ) ;
#5430=CARTESIAN_POINT ( 'NONE',  ( -11.75000000000000000, -5.000000000000000000, -11.75000000000000000 ) ) ;
#5431=VERTEX_POINT ( 'NONE', #22529 ) ;
#5448=ADVANCED_FACE ( 'NONE', ( #66686 ), #35191, .F. ) ;
#5454=CARTESIAN_POINT ( 'NONE',  ( -30.00000000000000000, -12.00000000000000000, 10.52786404500095863 ) ) ;
#5462=VECTOR ( 'NONE', #61426, 1000.000000000000000 ) ;
#5472=CARTESIAN_POINT ( 'NONE',  ( -15.50000000000000000, -0.4000000000005236034, -19.20000000000052509 ) ) ;
#5473=DIRECTION ( 'NONE',  ( 0.8660254037844482555, 0.000000000000000000, -0.4999999999999831801 ) ) ;
#5481=FACE_OUTER_BOUND ( 'NONE', #52020, .T. ) ;
#5487=ORIENTED_EDGE ( 'NONE', *, *, #18733, .T. ) ;
#5496=ORIENTED_EDGE ( 'NONE', *, *, #60049, .F. ) ;
#5497=ORIENTED_EDGE ( 'NONE', *, *, #21383, .F. ) ;
#5500=ORIENTED_EDGE ( 'NONE', *, *, #38404, .F. ) ;
#5503=DIRECTION ( 'NONE',  ( 0.000000000000000000, 0.000000000000000000, -1.000000000000000000 ) ) ;
#5510=ORIENTED_EDGE ( 'NONE', *, *, #41287, .F. ) ;
#5512=CARTESIAN_POINT ( 'NONE',  ( -14.25000000000000000, -0.2038245569916330158, 23.22168783648699986 ) ) ;
#5513=DIRECTION ( 'NONE',  ( 0.000000000000000000, 1.000000000000000000, 0.000000000000000000 ) ) ;
#5521=ADVANCED_FACE ( 'NONE', ( #18589 ), #40153, .F. ) ;
#5523=PLANE ( 'NONE',  #14452 ) ;
#5530=ORIENTED_EDGE ( 'NONE', *, *, #22139, .F. ) ;
#5532=ADVANCED_FACE ( 'NONE', ( #35545 ), #57128, .T. ) ;
#5535=CARTESIAN_POINT ( 'NONE',  ( 11.00000000000000000, -14.33999999999999986, 14.50000000000000000 ) ) ;
#5541=VECTOR ( 'NONE', #66340, 1000.000000000000000 ) ;
#5544=LINE ( 'NONE', #10838, #61036 ) ;
#5548=DIRECTION ( 'NONE',  ( 0.000000000000000000, -0.9938079899998859545, 0.1111111111112941946 ) ) ;
#5551=VERTEX_POINT ( 'NONE', #52178 ) ;
#5557=CARTESIAN_POINT ( 'NONE',  ( -29.25000000000000000, -5.200000000000001066, -11.75000000000000000 ) ) ;
#5561=EDGE_CURVE ( 'NONE', #5255, #45628, #15403, .T. ) ;
#5562=ORIENTED_EDGE ( 'NONE', *, *, #53602, .T. ) ;
#5566=DIRECTION ( 'NONE',  ( 0.000000000000000000, 0.000000000000000000, -1.000000000000000000 ) ) ;
#5573=CARTESIAN_POINT ( 'NONE',  ( 25.50000000000000355, -5.578999999999999737, 20.87899999999999778 ) ) ;
#5582=LINE ( 'NONE', #21836, #50316 ) ;
#5590=DIRECTION ( 'NONE',  ( -1.000000000000000000, 0.000000000000000000, 0.000000000000000000 ) ) ;
#5591=ORIENTED_EDGE ( 'NONE', *, *, #63078, .T. ) ;
#5596=LINE ( 'NONE', #20805, #9845 ) ;
#5598=ORIENTED_EDGE ( 'NONE', *, *, #44976, .F. ) ;
#5599=VERTEX_POINT ( 'NONE', #19638 ) ;
#5608=EDGE_CURVE ( 'NONE', #8160, #26381, #57596, .T. ) ;
#5618=EDGE_CURVE ( 'NONE', #61956, #8473, #63840, .T. ) ;
#5623=ORIENTED_EDGE ( 'NONE', *, *, #8037, .T. ) ;
#5624=CARTESIAN_POINT ( 'NONE',  ( 11.75000000000000000, -5.000000000000000000, 11.75000000000000000 ) ) ;
#5627=CARTESIAN_POINT ( 'NONE',  ( -30.00000000000000000, -13.79999999999979998, 17.30000000000000071 ) ) ;
#5628=ADVANCED_FACE ( 'NONE', ( #25677 ), #32017, .F. ) ;
#5633=EDGE_CURVE ( 'NONE', #68720, #41169, #41799, .T. ) ;
#5636=VERTEX_POINT ( 'NONE', #41915 ) ;
#5642=CARTESIAN_POINT ( 'NONE',  ( -25.50000000000000355, 0.000000000000000000, 20.24999999999999645 ) ) ;
#5649=EDGE_CURVE ( 'NONE', #46357, #50590, #15050, .T. ) ;
#5656=LINE ( 'NONE', #47733, #4207 ) ;
#5660=CIRCLE ( 'NONE', #50796, 4.000000000000000888 ) ;
#5662=DIRECTION ( 'NONE',  ( 0.000000000000000000, -0.1111111111108840643, -0.9938079899999319178 ) ) ;
#5665=VERTEX_POINT ( 'NONE', #54982 ) ;
#5667=VERTEX_POINT ( 'NONE', #22097 ) ;
#5676=AXIS2_PLACEMENT_3D ( 'NONE', #5138, #25309, #69486 ) ;
#5679=EDGE_LOOP ( 'NONE', ( #56881, #54792, #37840, #26266 ) ) ;
#5680=ORIENTED_EDGE ( 'NONE', *, *, #38569, .F. ) ;
#5682=CARTESIAN_POINT ( 'NONE',  ( 30.00000000000000000, -9.200000000000120082, 17.64999999999993108 ) ) ;
#5706=AXIS2_PLACEMENT_3D ( 'NONE', #8519, #20535, #47408 ) ;
#5709=CYLINDRICAL_SURFACE ( 'NONE', #36695, 0.3499999999999302558 ) ;
#5712=CARTESIAN_POINT ( 'NONE',  ( 14.24999999999999822, -0.3152037684892591285, -22.25410949791979220 ) ) ;
#5713=AXIS2_PLACEMENT_3D ( 'NONE', #37702, #28128, #565 ) ;
#5716=DIRECTION ( 'NONE',  ( 0.000000000000000000, -1.000000000000000000, 0.000000000000000000 ) ) ;
#5717=ORIENTED_EDGE ( 'NONE', *, *, #18235, .T. ) ;
#5740=FACE_OUTER_BOUND ( 'NONE', #35982, .T. ) ;
#5749=ORIENTED_EDGE ( 'NONE', *, *, #33259, .T. ) ;
#5752=LINE ( 'NONE', #17045, #9661 ) ;
#5756=VECTOR ( 'NONE', #43495, 1000.000000000000000 ) ;
#5775=ORIENTED_EDGE ( 'NONE', *, *, #62161, .T. ) ;
#5778=LINE ( 'NONE', #58491, #59765 ) ;
#5780=DIRECTION ( 'NONE',  ( -1.000000000000000000, 0.000000000000000000, 0.000000000000000000 ) ) ;
#5787=VERTEX_POINT ( 'NONE', #43308 ) ;
#5789=ORIENTED_EDGE ( 'NONE', *, *, #42442, .T. ) ;
#5792=EDGE_CURVE ( 'NONE', #54079, #5667, #7961, .T. ) ;
#5793=CIRCLE ( 'NONE', #49778, 3.499999999999855227 ) ;
#5796=LINE ( 'NONE', #54582, #65286 ) ;
#5798=DIRECTION ( 'NONE',  ( 0.000000000000000000, 0.000000000000000000, -1.000000000000000000 ) ) ;
#5799=AXIS2_PLACEMENT_3D ( 'NONE', #24098, #66876, #18432 ) ;
#5802=ORIENTED_EDGE ( 'NONE', *, *, #60971, .F. ) ;
#5803=LINE ( 'NONE', #59880, #47347 ) ;
#5805=ORIENTED_EDGE ( 'NONE', *, *, #60886, .T. ) ;
#5808=EDGE_LOOP ( 'NONE', ( #30080, #576, #66937, #23035 ) ) ;
#5810=CARTESIAN_POINT ( 'NONE',  ( 30.00000000000000000, -9.454754784057099570, 17.53999999999999915 ) ) ;
#5811=AXIS2_PLACEMENT_3D ( 'NONE', #59204, #37994, #11109 ) ;
#5812=AXIS2_PLACEMENT_3D ( 'NONE', #29186, #39453, #17889 ) ;
#5815=ORIENTED_EDGE ( 'NONE', *, *, #8037, .F. ) ;
#5818=VECTOR ( 'NONE', #30151, 1000.000000000000000 ) ;
#5823=EDGE_CURVE ( 'NONE', #6488, #6937, #29820, .T. ) ;
#5825=VECTOR ( 'NONE', #13859, 1000.000000000000000 ) ;
#5828=ORIENTED_EDGE ( 'NONE', *, *, #17065, .T. ) ;
#5835=EDGE_LOOP ( 'NONE', ( #39234, #16059, #15395, #63726 ) ) ;
#5838=DIRECTION ( 'NONE',  ( 0.000000000000000000, -0.1111111111108836896, -0.9938079899999319178 ) ) ;
#5840=ORIENTED_EDGE ( 'NONE', *, *, #35281, .F. ) ;
#5843=DIRECTION ( 'NONE',  ( 0.000000000000000000, 1.000000000000000000, 0.000000000000000000 ) ) ;
#5851=ORIENTED_EDGE ( 'NONE', *, *, #32727, .T. ) ;
#5856=AXIS2_PLACEMENT_3D ( 'NONE', #18753, #24055, #38934 ) ;
#5864=ORIENTED_EDGE ( 'NONE', *, *, #13830, .T. ) ;
#5868=EDGE_CURVE ( 'NONE', #2526, #27219, #56696, .T. ) ;
#5872=EDGE_CURVE ( 'NONE', #30626, #58695, #41850, .T. ) ;
#5880=DIRECTION ( 'NONE',  ( 0.000000000000000000, -0.9921567416492215186, 0.1249999999999996531 ) ) ;
#5891=AXIS2_PLACEMENT_3D ( 'NONE', #49436, #44110, #60361 ) ;
#5901=EDGE_CURVE ( 'NONE', #38222, #11065, #49992, .T. ) ;
#5902=DIRECTION ( 'NONE',  ( 0.000000000000000000, -1.000000000000000000, 0.000000000000000000 ) ) ;
#5904=EDGE_LOOP ( 'NONE', ( #32785, #59046 ) ) ;
#5911=VECTOR ( 'NONE', #41265, 1000.000000000000000 ) ;
#5916=CARTESIAN_POINT ( 'NONE',  ( -15.50000000000000000, -0.1999999999999999556, -23.94999999999999929 ) ) ;
#5917=EDGE_CURVE ( 'NONE', #66963, #41832, #66947, .T. ) ;
#5921=EDGE_CURVE ( 'NONE', #69139, #7820, #1553, .T. ) ;
#5923=PLANE ( 'NONE',  #48946 ) ;
#5934=VECTOR ( 'NONE', #52569, 1000.000000000000000 ) ;
#5937=EDGE_CURVE ( 'NONE', #60780, #36470, #7557, .T. ) ;
#5944=EDGE_CURVE ( 'NONE', #56315, #51110, #26066, .T. ) ;
#5953=ADVANCED_FACE ( 'NONE', ( #45031 ), #3436, .T. ) ;
#5960=VECTOR ( 'NONE', #18918, 1000.000000000000000 ) ;
#5964=DIRECTION ( 'NONE',  ( -1.000000000000000000, 0.000000000000000000, 0.000000000000000000 ) ) ;
#5968=DIRECTION ( 'NONE',  ( 0.000000000000000000, 0.000000000000000000, -1.000000000000000000 ) ) ;
#5980=DIRECTION ( 'NONE',  ( 0.000000000000000000, -1.000000000000000000, 0.000000000000000000 ) ) ;
#5981=VECTOR ( 'NONE', #28064, 1000.000000000000000 ) ;
#5983=DIRECTION ( 'NONE',  ( -0.3479852726768748461, 0.000000000000000000, 0.9375000000000006661 ) ) ;
#5984=DIRECTION ( 'NONE',  ( 0.000000000000000000, 1.000000000000000000, 0.000000000000000000 ) ) ;
#6004=VERTEX_POINT ( 'NONE', #47831 ) ;
#6005=ORIENTED_EDGE ( 'NONE', *, *, #24357, .T. ) ;
#6007=CYLINDRICAL_SURFACE ( 'NONE', #27659, 3.499999999999055866 ) ;
#6012=ORIENTED_EDGE ( 'NONE', *, *, #31714, .T. ) ;
#6013=EDGE_CURVE ( 'NONE', #32779, #47223, #52822, .T. ) ;
#6014=AXIS2_PLACEMENT_3D ( 'NONE', #31636, #25270, #31295 ) ;
#6027=ADVANCED_FACE ( 'NONE', ( #47488 ), #46435, .T. ) ;
#6030=CARTESIAN_POINT ( 'NONE',  ( -11.00000000000000000, -5.599999999999999645, 27.00000000000000000 ) ) ;
#6038=FACE_OUTER_BOUND ( 'NONE', #50518, .T. ) ;
#6039=DIRECTION ( 'NONE',  ( 0.000000000000000000, 0.000000000000000000, 1.000000000000000000 ) ) ;
#6042=VECTOR ( 'NONE', #312, 1000.000000000000000 ) ;
#6050=VERTEX_POINT ( 'NONE', #63055 ) ;
#6053=CARTESIAN_POINT ( 'NONE',  ( 14.24999999999999822, -0.2715193793361447838, -22.98718409945083252 ) ) ;
#6058=ORIENTED_EDGE ( 'NONE', *, *, #6722, .T. ) ;
#6065=DIRECTION ( 'NONE',  ( -1.000000000000000000, 0.000000000000000000, 0.000000000000000000 ) ) ;
#6067=ORIENTED_EDGE ( 'NONE', *, *, #5872, .F. ) ;
#6068=AXIS2_PLACEMENT_3D ( 'NONE', #44473, #6994, #676 ) ;
#6072=DIRECTION ( 'NONE',  ( -1.000000000000000000, 0.000000000000000000, 0.000000000000000000 ) ) ;
#6082=CARTESIAN_POINT ( 'NONE',  ( -31.00000000000000000, -2.500000000000000000, 45.00000000000000000 ) ) ;
#6083=LINE ( 'NONE', #15998, #8258 ) ;
#6087=EDGE_LOOP ( 'NONE', ( #23796, #25144, #41401, #47122 ) ) ;
#6088=ADVANCED_FACE ( 'NONE', ( #34241 ), #52014, .F. ) ;
#6098=ORIENTED_EDGE ( 'NONE', *, *, #16137, .T. ) ;
#6100=DIRECTION ( 'NONE',  ( 0.000000000000000000, 0.000000000000000000, 1.000000000000000000 ) ) ;
#6106=CARTESIAN_POINT ( 'NONE',  ( -16.54633693294649888, -0.2717122460102565085, -23.33927276307431598 ) ) ;
#6114=LINE ( 'NONE', #55244, #52514 ) ;
#6118=CARTESIAN_POINT ( 'NONE',  ( -11.00000000000000000, -17.50000000000000000, 15.70500000000000007 ) ) ;
#6119=DIRECTION ( 'NONE',  ( 0.000000000000000000, 1.000000000000000000, 0.000000000000000000 ) ) ;
#6128=CARTESIAN_POINT ( 'NONE',  ( 11.00000000000000000, -11.85423089348099879, 9.852125413066602277 ) ) ;
#6143=CARTESIAN_POINT ( 'NONE',  ( 11.50000000000000000, -11.50000000000000000, 15.00000000000000000 ) ) ;
#6151=ORIENTED_EDGE ( 'NONE', *, *, #22855, .F. ) ;
#6153=ORIENTED_EDGE ( 'NONE', *, *, #24112, .F. ) ;
#6164=VECTOR ( 'NONE', #53196, 1000.000000000000000 ) ;
#6171=EDGE_CURVE ( 'NONE', #59441, #2526, #4579, .T. ) ;
#6176=ADVANCED_FACE ( 'NONE', ( #48894 ), #32278, .F. ) ;
#6180=AXIS2_PLACEMENT_3D ( 'NONE', #69306, #52005, #63310 ) ;
#6186=CARTESIAN_POINT ( 'NONE',  ( 13.00000000000000178, -16.64230188589299786, -14.64519951917100116 ) ) ;
#6199=EDGE_CURVE ( 'NONE', #24879, #43126, #57660, .T. ) ;
#6206=EDGE_CURVE ( 'NONE', #55340, #31859, #16358, .T. ) ;
#6208=EDGE_CURVE ( 'NONE', #4107, #37811, #44074, .T. ) ;
#6214=CARTESIAN_POINT ( 'NONE',  ( 12.00000000000000000, -5.000000000000000000, 22.50000000000000000 ) ) ;
#6215=CARTESIAN_POINT ( 'NONE',  ( 22.14589803375000088, -15.50000000000000000, -21.50000000000000000 ) ) ;
#6216=FACE_OUTER_BOUND ( 'NONE', #52637, .T. ) ;
#6227=DIRECTION ( 'NONE',  ( -1.000000000000000000, 0.000000000000000000, 0.000000000000000000 ) ) ;
#6228=DIRECTION ( 'NONE',  ( -1.000000000000000000, 0.000000000000000000, 0.000000000000000000 ) ) ;
#6236=CARTESIAN_POINT ( 'NONE',  ( 30.00000000000000000, -15.97213595500069871, -14.50000000000000000 ) ) ;
#6237=ORIENTED_EDGE ( 'NONE', *, *, #44925, .F. ) ;
#6242=DIRECTION ( 'NONE',  ( 0.000000000000000000, 1.000000000000000000, 0.000000000000000000 ) ) ;
#6244=EDGE_LOOP ( 'NONE', ( #28760, #276, #24416, #9245 ) ) ;
#6247=ORIENTED_EDGE ( 'NONE', *, *, #29845, .F. ) ;
#6248=CARTESIAN_POINT ( 'NONE',  ( 30.00000000000000000, -9.200000000000120082, 17.30000000000000071 ) ) ;
#6250=CARTESIAN_POINT ( 'NONE',  ( -11.50000000000000000, -12.00000000000000000, 10.52786404500095863 ) ) ;
#6251=AXIS2_PLACEMENT_3D ( 'NONE', #41577, #14364, #68458 ) ;
#6252=AXIS2_PLACEMENT_3D ( 'NONE', #16914, #652, #7317 ) ;
#6261=ORIENTED_EDGE ( 'NONE', *, *, #15712, .F. ) ;
#6275=ORIENTED_EDGE ( 'NONE', *, *, #4196, .F. ) ;
#6280=DIRECTION ( 'NONE',  ( 0.000000000000000000, 0.000000000000000000, -1.000000000000000000 ) ) ;
#6290=CARTESIAN_POINT ( 'NONE',  ( -16.54633693294650953, -0.2717122460102549542, 21.66072723692568402 ) ) ;
#6295=DIRECTION ( 'NONE',  ( 0.000000000000000000, -0.7071067811865455743, 0.7071067811865495711 ) ) ;
#6300=AXIS2_PLACEMENT_3D ( 'NONE', #37704, #15090, #5184 ) ;
#6310=CARTESIAN_POINT ( 'NONE',  ( 24.00000000000000000, -15.50000000000000000, 19.33772233983200195 ) ) ;
#6311=LINE ( 'NONE', #17254, #56443 ) ;
#6332=DIRECTION ( 'NONE',  ( 0.000000000000000000, -1.000000000000000000, 0.000000000000000000 ) ) ;
#6333=ORIENTED_EDGE ( 'NONE', *, *, #46640, .T. ) ;
#6334=ORIENTED_EDGE ( 'NONE', *, *, #18482, .T. ) ;
#6338=CARTESIAN_POINT ( 'NONE',  ( 29.25000000000000000, -5.000000000000000000, 26.25000000000000000 ) ) ;
#6341=VECTOR ( 'NONE', #13315, 1000.000000000000114 ) ;
#6354=DIRECTION ( 'NONE',  ( 0.000000000000000000, -0.1111111111108836896, 0.9938079899999319178 ) ) ;
#6356=VECTOR ( 'NONE', #131, 1000.000000000000114 ) ;
#6362=CIRCLE ( 'NONE', #52717, 4.000000000000001776 ) ;
#6363=AXIS2_PLACEMENT_3D ( 'NONE', #65146, #16703, #54531 ) ;
#6367=EDGE_LOOP ( 'NONE', ( #56548, #6962, #7208, #31046 ) ) ;
#6368=DIRECTION ( 'NONE',  ( 0.000000000000000000, -1.000000000000000000, 0.000000000000000000 ) ) ;
#6369=DIRECTION ( 'NONE',  ( 0.000000000000000000, 0.000000000000000000, -1.000000000000000000 ) ) ;
#6377=ORIENTED_EDGE ( 'NONE', *, *, #32816, .T. ) ;
#6382=CARTESIAN_POINT ( 'NONE',  ( -16.75000000000000000, -0.2038245569916330158, -21.77831216351300014 ) ) ;
#6384=DIRECTION ( 'NONE',  ( 0.000000000000000000, 0.000000000000000000, 1.000000000000000000 ) ) ;
#6386=ORIENTED_EDGE ( 'NONE', *, *, #28368, .F. ) ;
#6388=PLANE ( 'NONE',  #68362 ) ;
#6393=VECTOR ( 'NONE', #23069, 1000.000000000000000 ) ;
#6394=DIRECTION ( 'NONE',  ( 0.000000000000000000, 0.6857142857142869419, -0.7278708115918273158 ) ) ;
#6396=ORIENTED_EDGE ( 'NONE', *, *, #60764, .T. ) ;
#6399=ORIENTED_EDGE ( 'NONE', *, *, #3863, .T. ) ;
#6402=VECTOR ( 'NONE', #24020, 1000.000000000000000 ) ;
#6411=CARTESIAN_POINT ( 'NONE',  ( 30.00000000000000000, -5.599999999999999645, 9.400000000000000355 ) ) ;
#6415=DIRECTION ( 'NONE',  ( 0.000000000000000000, -0.9921567416492215186, 0.1249999999999996531 ) ) ;
#6416=CARTESIAN_POINT ( 'NONE',  ( 30.00000000000000000, -14.04000000000000092, -14.80000000000000071 ) ) ;
#6420=VECTOR ( 'NONE', #27248, 1000.000000000000000 ) ;
#6421=CYLINDRICAL_SURFACE ( 'NONE', #18559, 0.2999999999998732569 ) ;
#6431=EDGE_CURVE ( 'NONE', #54584, #2465, #53198, .T. ) ;
#6432=FACE_OUTER_BOUND ( 'NONE', #36332, .T. ) ;
#6434=CARTESIAN_POINT ( 'NONE',  ( 11.00000000000000000, -11.50000000000100009, -15.00000000000084910 ) ) ;
#6435=LINE ( 'NONE', #44241, #68449 ) ;
#6436=ORIENTED_EDGE ( 'NONE', *, *, #39576, .T. ) ;
#6444=EDGE_CURVE ( 'NONE', #35366, #2217, #47316, .T. ) ;
#6455=CIRCLE ( 'NONE', #45962, 0.3500000000002719824 ) ;
#6456=VECTOR ( 'NONE', #62530, 1000.000000000000000 ) ;
#6460=CIRCLE ( 'NONE', #39199, 4.000000000000000888 ) ;
#6463=CARTESIAN_POINT ( 'NONE',  ( 29.25000000000000000, -5.200000000000001066, -11.75000000000000000 ) ) ;
#6466=ORIENTED_EDGE ( 'NONE', *, *, #34229, .F. ) ;
#6477=EDGE_CURVE ( 'NONE', #29553, #67310, #21154, .T. ) ;
#6481=CARTESIAN_POINT ( 'NONE',  ( -15.50000000000000000, -1.037157890325000054, 18.50000000000000000 ) ) ;
#6482=LINE ( 'NONE', #5454, #4128 ) ;
#6488=VERTEX_POINT ( 'NONE', #57924 ) ;
#6490=FACE_OUTER_BOUND ( 'NONE', #5808, .T. ) ;
#6503=CARTESIAN_POINT ( 'NONE',  ( -25.50000000000000355, -15.50000000000000000, -22.50000000000000000 ) ) ;
#6504=CARTESIAN_POINT ( 'NONE',  ( 30.00000000000000000, -17.50000000000000000, 15.70500000000000007 ) ) ;
#6506=EDGE_CURVE ( 'NONE', #50486, #14586, #5793, .T. ) ;
#6512=DIRECTION ( 'NONE',  ( 0.000000000000000000, 1.000000000000000000, 0.000000000000000000 ) ) ;
#6515=CIRCLE ( 'NONE', #5420, 0.4000000000000600298 ) ;
#6533=CIRCLE ( 'NONE', #46035, 0.3499999999998879008 ) ;
#6541=ORIENTED_EDGE ( 'NONE', *, *, #59084, .T. ) ;
#6556=EDGE_CURVE ( 'NONE', #23985, #6050, #46394, .T. ) ;
#6557=DIRECTION ( 'NONE',  ( 0.000000000000000000, -1.000000000000000000, 0.000000000000000000 ) ) ;
#6558=CARTESIAN_POINT ( 'NONE',  ( 28.00000000000000000, -15.50000000000000000, 20.05051025721700242 ) ) ;
#6561=EDGE_CURVE ( 'NONE', #34396, #2518, #24951, .T. ) ;
#6565=DIRECTION ( 'NONE',  ( -1.000000000000000000, 0.000000000000000000, 0.000000000000000000 ) ) ;
#6571=CARTESIAN_POINT ( 'NONE',  ( 15.50000000000000000, -0.2000000000000000111, -25.80000000297970075 ) ) ;
#6573=PLANE ( 'NONE',  #60989 ) ;
#6575=DIRECTION ( 'NONE',  ( 0.000000000000000000, 0.000000000000000000, 1.000000000000000000 ) ) ;
#6578=CARTESIAN_POINT ( 'NONE',  ( 11.00000000000000000, -9.200000000000120082, 17.64999999999993108 ) ) ;
#6579=CARTESIAN_POINT ( 'NONE',  ( 17.00000000000000000, -15.50000000000000000, 19.33772233983200195 ) ) ;
#6580=DIRECTION ( 'NONE',  ( -1.000000000000000000, 0.000000000000000000, 0.000000000000000000 ) ) ;
#6588=ORIENTED_EDGE ( 'NONE', *, *, #69097, .T. ) ;
#6594=DIRECTION ( 'NONE',  ( 0.000000000000000000, 0.000000000000000000, -1.000000000000000000 ) ) ;
#6595=ORIENTED_EDGE ( 'NONE', *, *, #54510, .T. ) ;
#6600=AXIS2_PLACEMENT_3D ( 'NONE', #41273, #62852, #4856 ) ;
#6604=ORIENTED_EDGE ( 'NONE', *, *, #57462, .T. ) ;
#6609=VERTEX_POINT ( 'NONE', #65335 ) ;
#6611=ORIENTED_EDGE ( 'NONE', *, *, #62221, .T. ) ;
#6616=DIRECTION ( 'NONE',  ( -1.000000000000000000, 0.000000000000000000, 0.000000000000000000 ) ) ;
#6618=ORIENTED_EDGE ( 'NONE', *, *, #43178, .T. ) ;
#6622=EDGE_CURVE ( 'NONE', #44394, #68236, #55747, .T. ) ;
#6623=CARTESIAN_POINT ( 'NONE',  ( 14.24999999999999822, -0.3152037684892576297, 22.74589050208021845 ) ) ;
#6630=CARTESIAN_POINT ( 'NONE',  ( 11.00000000000000000, -11.50000000000000000, 11.00000000000000000 ) ) ;
#6633=DIRECTION ( 'NONE',  ( 0.000000000000000000, 0.000000000000000000, 1.000000000000000000 ) ) ;
#6642=DIRECTION ( 'NONE',  ( -0.000000000000000000, 1.000000000000000000, -0.000000000000000000 ) ) ;
#6674=ADVANCED_FACE ( 'NONE', ( #33135 ), #40871, .T. ) ;
#6678=LINE ( 'NONE', #61444, #42307 ) ;
#6694=CARTESIAN_POINT ( 'NONE',  ( 29.50000000000000355, -15.97213595500069871, -14.50000000000000000 ) ) ;
#6696=VECTOR ( 'NONE', #51854, 1000.000000000000000 ) ;
#6706=ORIENTED_EDGE ( 'NONE', *, *, #7197, .F. ) ;
#6709=LINE ( 'NONE', #60800, #40851 ) ;
#6712=CARTESIAN_POINT ( 'NONE',  ( -13.00000000000000178, -15.50000000000000000, 20.05051025721700242 ) ) ;
#6714=ORIENTED_EDGE ( 'NONE', *, *, #56971, .T. ) ;
#6722=EDGE_CURVE ( 'NONE', #27877, #39887, #45831, .T. ) ;
#6723=FACE_OUTER_BOUND ( 'NONE', #28964, .T. ) ;
#6744=PLANE ( 'NONE',  #10134 ) ;
#6746=DIRECTION ( 'NONE',  ( 1.000000000000000000, -0.000000000000000000, -0.000000000000000000 ) ) ;
#6751=ORIENTED_EDGE ( 'NONE', *, *, #19308, .T. ) ;
#6765=VERTEX_POINT ( 'NONE', #51491 ) ;
#6774=CARTESIAN_POINT ( 'NONE',  ( 15.91242688423647600, -0.3152598339557935447, -21.29473909966096556 ) ) ;
#6775=VERTEX_POINT ( 'NONE', #40169 ) ;
#6790=FACE_OUTER_BOUND ( 'NONE', #20477, .T. ) ;
#6794=AXIS2_PLACEMENT_3D ( 'NONE', #2733, #25014, #45874 ) ;
#6798=CIRCLE ( 'NONE', #40516, 4.000000000000000000 ) ;
#6811=DIRECTION ( 'NONE',  ( 0.000000000000000000, -0.7096009616570518874, 0.7046037717862339012 ) ) ;
#6828=LINE ( 'NONE', #18476, #27222 ) ;
#6844=CARTESIAN_POINT ( 'NONE',  ( -28.00000000000000000, -16.28999999999710369, 14.50000000000000000 ) ) ;
#6847=LINE ( 'NONE', #66941, #3310 ) ;
#6855=ORIENTED_EDGE ( 'NONE', *, *, #30649, .F. ) ;
#6856=EDGE_CURVE ( 'NONE', #54090, #66376, #15977, .T. ) ;
#6857=ORIENTED_EDGE ( 'NONE', *, *, #20458, .T. ) ;
#6866=VECTOR ( 'NONE', #58282, 1000.000000000000000 ) ;
#6868=EDGE_CURVE ( 'NONE', #38183, #59292, #6916, .T. ) ;
#6869=DIRECTION ( 'NONE',  ( -0.000000000000000000, 1.000000000000000000, -0.000000000000000000 ) ) ;
#6876=CARTESIAN_POINT ( 'NONE',  ( 11.00000000000000000, -11.50000000000000000, -19.00000000000000000 ) ) ;
#6878=VECTOR ( 'NONE', #58644, 1000.000000000000000 ) ;
#6899=EDGE_CURVE ( 'NONE', #20240, #46397, #48290, .T. ) ;
#6902=CARTESIAN_POINT ( 'NONE',  ( -29.25000000000000000, -5.000000000000000000, -11.75000000000000000 ) ) ;
#6903=LINE ( 'NONE', #16489, #311 ) ;
#6906=DIRECTION ( 'NONE',  ( 0.000000000000000000, 1.000000000000000000, 0.000000000000000000 ) ) ;
#6913=ORIENTED_EDGE ( 'NONE', *, *, #19735, .F. ) ;
#6914=EDGE_LOOP ( 'NONE', ( #61146, #42562, #29777, #67228 ) ) ;
#6916=CIRCLE ( 'NONE', #46448, 2.250000000000001776 ) ;
#6918=EDGE_LOOP ( 'NONE', ( #60617, #6588, #22039, #42468 ) ) ;
#6923=ORIENTED_EDGE ( 'NONE', *, *, #48349, .F. ) ;
#6925=AXIS2_PLACEMENT_3D ( 'NONE', #62714, #31613, #53188 ) ;
#6927=EDGE_CURVE ( 'NONE', #50486, #25888, #58901, .T. ) ;
#6932=EDGE_CURVE ( 'NONE', #24609, #58795, #63422, .T. ) ;
#6937=VERTEX_POINT ( 'NONE', #32030 ) ;
#6946=ORIENTED_EDGE ( 'NONE', *, *, #7740, .F. ) ;
#6948=FACE_OUTER_BOUND ( 'NONE', #23254, .T. ) ;
#6960=VECTOR ( 'NONE', #30543, 1000.000000000000000 ) ;
#6962=ORIENTED_EDGE ( 'NONE', *, *, #56752, .T. ) ;
#6968=DIRECTION ( 'NONE',  ( 0.000000000000000000, -0.1249999999999996531, -0.9921567416492215186 ) ) ;
#6984=ORIENTED_EDGE ( 'NONE', *, *, #67464, .T. ) ;
#6985=DIRECTION ( 'NONE',  ( 0.000000000000000000, 1.000000000000000000, 0.000000000000000000 ) ) ;
#6988=DIRECTION ( 'NONE',  ( -0.4999999999989371835, 0.000000000000000000, -0.8660254037850523279 ) ) ;
#6994=DIRECTION ( 'NONE',  ( 1.000000000000000000, -0.000000000000000000, -0.000000000000000000 ) ) ;
#7004=DIRECTION ( 'NONE',  ( -1.000000000000000000, 0.000000000000000000, 0.000000000000000000 ) ) ;
#7006=VERTEX_POINT ( 'NONE', #33059 ) ;
#7014=CARTESIAN_POINT ( 'NONE',  ( 18.85410196625000268, -15.50000000000000000, -21.50000000000000000 ) ) ;
#7020=EDGE_CURVE ( 'NONE', #21729, #40956, #43321, .T. ) ;
#7032=ORIENTED_EDGE ( 'NONE', *, *, #12680, .T. ) ;
#7037=ORIENTED_EDGE ( 'NONE', *, *, #52038, .F. ) ;
#7040=CARTESIAN_POINT ( 'NONE',  ( 11.50000000000000000, -11.50000000000000000, -11.00000000000000000 ) ) ;
#7043=CARTESIAN_POINT ( 'NONE',  ( 11.50000000000000000, -12.00000000000000000, 10.69999999999999929 ) ) ;
#7048=VECTOR ( 'NONE', #42660, 1000.000000000000000 ) ;
#7050=VECTOR ( 'NONE', #35741, 1000.000000000000114 ) ;
#7055=DIRECTION ( 'NONE',  ( 0.000000000000000000, 1.000000000000000000, 0.000000000000000000 ) ) ;
#7056=VERTEX_POINT ( 'NONE', #60625 ) ;
#7059=PLANE ( 'NONE',  #4013 ) ;
#7075=LINE ( 'NONE', #40652, #17840 ) ;
#7076=AXIS2_PLACEMENT_3D ( 'NONE', #37694, #32044, #5177 ) ;
#7077=CARTESIAN_POINT ( 'NONE',  ( 23.75054448485400016, -17.50000000000000000, -25.53140320652400064 ) ) ;
#7081=ORIENTED_EDGE ( 'NONE', *, *, #37969, .T. ) ;
#7086=FACE_OUTER_BOUND ( 'NONE', #50925, .T. ) ;
#7087=CARTESIAN_POINT ( 'NONE',  ( 25.50000000000000355, 0.000000000000000000, -24.75000000000000000 ) ) ;
#7090=DIRECTION ( 'NONE',  ( 0.000000000000000000, 0.000000000000000000, -1.000000000000000000 ) ) ;
#7103=VERTEX_POINT ( 'NONE', #23131 ) ;
#7107=CARTESIAN_POINT ( 'NONE',  ( -14.25000000000000000, -0.2038245569916330158, -21.77831216351300014 ) ) ;
#7116=CARTESIAN_POINT ( 'NONE',  ( 15.50000000000000000, -0.2038245569916604938, -21.05662432702600029 ) ) ;
#7128=ORIENTED_EDGE ( 'NONE', *, *, #50695, .T. ) ;
#7132=DIRECTION ( 'NONE',  ( 0.000000000000000000, 1.000000000000000000, 0.000000000000000000 ) ) ;
#7139=VERTEX_POINT ( 'NONE', #34079 ) ;
#7140=DIRECTION ( 'NONE',  ( 0.000000000000000000, 0.000000000000000000, 1.000000000000000000 ) ) ;
#7147=AXIS2_PLACEMENT_3D ( 'NONE', #5472, #68415, #15022 ) ;
#7148=DIRECTION ( 'NONE',  ( 0.9375000000000004441, 0.000000000000000000, -0.3479852726768752902 ) ) ;
#7159=CARTESIAN_POINT ( 'NONE',  ( 11.75000000000000000, -5.000000000000000000, -26.25000000000000000 ) ) ;
#7161=ORIENTED_EDGE ( 'NONE', *, *, #55642, .T. ) ;
#7164=EDGE_CURVE ( 'NONE', #5551, #37065, #40076, .T. ) ;
#7165=EDGE_LOOP ( 'NONE', ( #9178, #68433, #39645, #38401 ) ) ;
#7168=EDGE_CURVE ( 'NONE', #11406, #23447, #61658, .T. ) ;
#7171=DIRECTION ( 'NONE',  ( 0.000000000000000000, 0.000000000000000000, -1.000000000000000000 ) ) ;
#7175=CARTESIAN_POINT ( 'NONE',  ( -30.00000000000000000, -5.599999999999999645, -27.00000000000000000 ) ) ;
#7177=DIRECTION ( 'NONE',  ( 0.9375000000000004441, 0.000000000000000000, 0.3479852726768752902 ) ) ;
#7197=EDGE_CURVE ( 'NONE', #30907, #29553, #23834, .T. ) ;
#7200=ORIENTED_EDGE ( 'NONE', *, *, #43405, .T. ) ;
#7208=ORIENTED_EDGE ( 'NONE', *, *, #66270, .T. ) ;
#7218=DIRECTION ( 'NONE',  ( -1.000000000000000000, 0.000000000000000000, 0.000000000000000000 ) ) ;
#7222=CARTESIAN_POINT ( 'NONE',  ( -29.25000000000000000, -5.000000000000000000, -11.75000000000000000 ) ) ;
#7226=DIRECTION ( 'NONE',  ( -1.000000000000000000, 0.000000000000000000, 0.000000000000000000 ) ) ;
#7247=DIRECTION ( 'NONE',  ( -0.4999999999989410693, 0.000000000000000000, -0.8660254037850499964 ) ) ;
#7249=CARTESIAN_POINT ( 'NONE',  ( -24.00000000000000000, -16.28999999999999915, 14.50000000000000000 ) ) ;
#7250=DIRECTION ( 'NONE',  ( 0.000000000000000000, 0.000000000000000000, -1.000000000000000000 ) ) ;
#7251=EDGE_CURVE ( 'NONE', #414, #35831, #19231, .T. ) ;
#7254=ORIENTED_EDGE ( 'NONE', *, *, #61101, .T. ) ;
#7264=ADVANCED_FACE ( 'NONE', ( #57760 ), #52109, .F. ) ;
#7267=ORIENTED_EDGE ( 'NONE', *, *, #30649, .T. ) ;
#7283=ORIENTED_EDGE ( 'NONE', *, *, #16189, .F. ) ;
#7285=EDGE_CURVE ( 'NONE', #62767, #22867, #44217, .T. ) ;
#7291=DIRECTION ( 'NONE',  ( 0.000000000000000000, 0.000000000000000000, 1.000000000000000000 ) ) ;
#7299=DIRECTION ( 'NONE',  ( -1.000000000000000000, 0.000000000000000000, 0.000000000000000000 ) ) ;
#7303=CARTESIAN_POINT ( 'NONE',  ( -17.51999999999999957, -15.50000000000000000, 26.00000000000000355 ) ) ;
#7305=ORIENTED_EDGE ( 'NONE', *, *, #8843, .T. ) ;
#7306=VECTOR ( 'NONE', #7494, 1000.000000000000000 ) ;
#7307=FACE_OUTER_BOUND ( 'NONE', #28004, .T. ) ;
#7311=CARTESIAN_POINT ( 'NONE',  ( 11.50000000000000000, -11.50000000000000000, 15.00000000000000000 ) ) ;
#7312=ORIENTED_EDGE ( 'NONE', *, *, #22615, .T. ) ;
#7315=DIRECTION ( 'NONE',  ( 0.000000000000000000, 1.000000000000000000, 0.000000000000000000 ) ) ;
#7317=DIRECTION ( 'NONE',  ( 0.000000000000000000, 0.000000000000000000, 1.000000000000000000 ) ) ;
#7324=EDGE_CURVE ( 'NONE', #63611, #54102, #20621, .T. ) ;
#7325=CARTESIAN_POINT ( 'NONE',  ( 25.50000000000000355, 0.000000000000000000, -20.24999999999999645 ) ) ;
#7342=CARTESIAN_POINT ( 'NONE',  ( 23.48000000000000043, -15.50000000000000000, 26.00000000000000355 ) ) ;
#7352=CARTESIAN_POINT ( 'NONE',  ( 30.00000000000000000, -9.487228132326899654, 12.50000000000000000 ) ) ;
#7353=VERTEX_POINT ( 'NONE', #45999 ) ;
#7359=ORIENTED_EDGE ( 'NONE', *, *, #10273, .T. ) ;
#7360=VECTOR ( 'NONE', #39923, 1000.000000000000000 ) ;
#7364=ORIENTED_EDGE ( 'NONE', *, *, #56136, .T. ) ;
#7369=CARTESIAN_POINT ( 'NONE',  ( -11.00000000000000000, -14.04000000000000092, -14.80000000000000071 ) ) ;
#7373=CARTESIAN_POINT ( 'NONE',  ( -30.00000000000000000, -5.000000000000000000, -27.00000000000000000 ) ) ;
#7378=CARTESIAN_POINT ( 'NONE',  ( -11.00000000000000000, -14.33999999999999986, -14.50000000000000000 ) ) ;
#7380=ORIENTED_EDGE ( 'NONE', *, *, #66432, .T. ) ;
#7384=CARTESIAN_POINT ( 'NONE',  ( -15.50000000000129852, -17.50000000000000000, 22.50000000000000000 ) ) ;
#7386=VECTOR ( 'NONE', #58555, 1000.000000000000000 ) ;
#7396=CIRCLE ( 'NONE', #22281, 4.000000000000000888 ) ;
#7397=AXIS2_PLACEMENT_3D ( 'NONE', #16516, #6242, #11531 ) ;
#7406=CYLINDRICAL_SURFACE ( 'NONE', #43995, 0.3499999999999302558 ) ;
#7409=CARTESIAN_POINT ( 'NONE',  ( 25.50000000000000355, -5.200000000000001066, 22.50000000000000000 ) ) ;
#7414=PLANE ( 'NONE',  #56679 ) ;
#7417=DIRECTION ( 'NONE',  ( 0.000000000000000000, 0.000000000000000000, 1.000000000000000000 ) ) ;
#7419=CARTESIAN_POINT ( 'NONE',  ( 28.00000000000000000, -17.50000000000000000, 15.70499999999969809 ) ) ;
#7427=LINE ( 'NONE', #66480, #62058 ) ;
#7437=CIRCLE ( 'NONE', #17642, 0.3500000000009988455 ) ;
#7450=CARTESIAN_POINT ( 'NONE',  ( -15.50000000000000000, -5.000000000000000000, -18.50000000000000000 ) ) ;
#7454=FACE_OUTER_BOUND ( 'NONE', #57145, .T. ) ;
#7456=ORIENTED_EDGE ( 'NONE', *, *, #20360, .F. ) ;
#7458=ORIENTED_EDGE ( 'NONE', *, *, #64520, .F. ) ;
#7461=VECTOR ( 'NONE', #67324, 1000.000000000000000 ) ;
#7464=CIRCLE ( 'NONE', #36879, 0.3499999999998879008 ) ;
#7466=EDGE_LOOP ( 'NONE', ( #7380, #36277, #64703, #33388, #49833, #45777, #32691, #23631, #64782, #18489, #22258, #62954, #25773, #59063, #32589, #12575, #16345, #21027 ) ) ;
#7485=DIRECTION ( 'NONE',  ( -1.000000000000000000, 0.000000000000000000, 0.000000000000000000 ) ) ;
#7489=CIRCLE ( 'NONE', #35761, 0.3499999999998875677 ) ;
#7494=DIRECTION ( 'NONE',  ( 0.000000000000000000, 1.000000000000000000, 0.000000000000000000 ) ) ;
#7495=VERTEX_POINT ( 'NONE', #50950 ) ;
#7498=EDGE_CURVE ( 'NONE', #67429, #29771, #40592, .T. ) ;
#7500=DIRECTION ( 'NONE',  ( 1.000000000000000000, 0.000000000000000000, 0.000000000000000000 ) ) ;
#7504=AXIS2_PLACEMENT_3D ( 'NONE', #30205, #24895, #68030 ) ;
#7505=VECTOR ( 'NONE', #64275, 1000.000000000000000 ) ;
#7512=EDGE_CURVE ( 'NONE', #51926, #16848, #19820, .T. ) ;
#7514=VECTOR ( 'NONE', #51691, 1000.000000000000000 ) ;
#7515=DIRECTION ( 'NONE',  ( -0.4999999999989417354, 0.000000000000000000, 0.8660254037850495523 ) ) ;
#7517=ORIENTED_EDGE ( 'NONE', *, *, #54593, .T. ) ;
#7518=CARTESIAN_POINT ( 'NONE',  ( 12.00000000000000000, -5.000000000000000000, -22.50000000000000000 ) ) ;
#7522=FACE_BOUND ( 'NONE', #55162, .T. ) ;
#7524=LINE ( 'NONE', #33367, #595 ) ;
#7530=ORIENTED_EDGE ( 'NONE', *, *, #8843, .F. ) ;
#7537=DIRECTION ( 'NONE',  ( 0.000000000000000000, 1.000000000000000000, 0.000000000000000000 ) ) ;
#7540=ORIENTED_EDGE ( 'NONE', *, *, #26580, .F. ) ;
#7545=LINE ( 'NONE', #23814, #55871 ) ;
#7556=ADVANCED_FACE ( 'NONE', ( #31504 ), #14524, .T. ) ;
#7557=LINE ( 'NONE', #62338, #56524 ) ;
#7573=DIRECTION ( 'NONE',  ( 1.000000000000000000, -0.000000000000000000, -0.000000000000000000 ) ) ;
#7580=CARTESIAN_POINT ( 'NONE',  ( 24.00000000000000000, -17.50000000000000000, -15.70500000000000007 ) ) ;
#7583=MECHANICAL_DESIGN_GEOMETRIC_PRESENTATION_REPRESENTATION('',(#44825),#16648);
#7585=DIRECTION ( 'NONE',  ( 0.000000000000000000, 0.000000000000000000, -1.000000000000000000 ) ) ;
#7591=SURFACE_STYLE_USAGE ( .BOTH. , #2637 ) ;
#7592=CARTESIAN_POINT ( 'NONE',  ( -16.75000000000000000, -2.500000000000000000, -21.77831216351300014 ) ) ;
#7602=CARTESIAN_POINT ( 'NONE',  ( 30.00000000000000000, -12.00000000000000000, -12.20000000000000107 ) ) ;
#7607=LINE ( 'NONE', #13261, #9542 ) ;
#7610=CARTESIAN_POINT ( 'NONE',  ( 11.50000000000000000, -12.00000000000000000, 11.03137303340310282 ) ) ;
#7619=CYLINDRICAL_SURFACE ( 'NONE', #1102, 0.3999999999993835154 ) ;
#7630=DIRECTION ( 'NONE',  ( 0.000000000000000000, 0.000000000000000000, 1.000000000000000000 ) ) ;
#7632=ORIENTED_EDGE ( 'NONE', *, *, #56553, .F. ) ;
#7635=DIRECTION ( 'NONE',  ( 0.000000000000000000, 1.000000000000000000, 0.000000000000000000 ) ) ;
#7636=ORIENTED_EDGE ( 'NONE', *, *, #25077, .T. ) ;
#7646=VECTOR ( 'NONE', #68990, 1000.000000000000000 ) ;
#7647=ORIENTED_EDGE ( 'NONE', *, *, #3063, .T. ) ;
#7661=ORIENTED_EDGE ( 'NONE', *, *, #29226, .F. ) ;
#7666=CARTESIAN_POINT ( 'NONE',  ( -15.50000000000000000, -1.037157890325000054, -22.50000000000000000 ) ) ;
#7667=ORIENTED_EDGE ( 'NONE', *, *, #14521, .T. ) ;
#7674=LINE ( 'NONE', #35230, #31519 ) ;
#7682=CARTESIAN_POINT ( 'NONE',  ( 29.50000000000000355, -11.70000000000000284, -11.00000000000000000 ) ) ;
#7687=ORIENTED_EDGE ( 'NONE', *, *, #9247, .F. ) ;
#7689=AXIS2_PLACEMENT_3D ( 'NONE', #29255, #23609, #56153 ) ;
#7702=ORIENTED_EDGE ( 'NONE', *, *, #67099, .F. ) ;
#7708=DIRECTION ( 'NONE',  ( -0.000000000000000000, 1.000000000000000000, -0.000000000000000000 ) ) ;
#7715=ORIENTED_EDGE ( 'NONE', *, *, #15311, .F. ) ;
#7720=ORIENTED_EDGE ( 'NONE', *, *, #68785, .F. ) ;
#7728=EDGE_CURVE ( 'NONE', #37811, #65011, #47411, .T. ) ;
#7732=DIRECTION ( 'NONE',  ( 0.000000000000000000, -0.9938079899998859545, 0.1111111111112941946 ) ) ;
#7735=DIRECTION ( 'NONE',  ( -0.000000000000000000, 1.000000000000000000, -0.000000000000000000 ) ) ;
#7740=EDGE_CURVE ( 'NONE', #50075, #9129, #45464, .T. ) ;
#7746=CARTESIAN_POINT ( 'NONE',  ( 25.50000000000000355, -15.50000000000000000, -22.50000000000000000 ) ) ;
#7755=DIRECTION ( 'NONE',  ( 0.000000000000000000, 1.000000000000000000, 0.000000000000000000 ) ) ;
#7759=VECTOR ( 'NONE', #5186, 1000.000000000000000 ) ;
#7760=AXIS2_PLACEMENT_3D ( 'NONE', #10381, #53879, #42199 ) ;
#7767=PLANE ( 'NONE',  #4645 ) ;
#7772=DIRECTION ( 'NONE',  ( 0.000000000000000000, -1.000000000000000000, 0.000000000000000000 ) ) ;
#7776=DIRECTION ( 'NONE',  ( -1.000000000000000000, 0.000000000000000000, 0.000000000000000000 ) ) ;
#7779=CARTESIAN_POINT ( 'NONE',  ( -11.00000000000000000, -12.00000000000000000, -11.03137303340310282 ) ) ;
#7780=AXIS2_PLACEMENT_3D ( 'NONE', #2331, #63485, #35540 ) ;
#7783=DIRECTION ( 'NONE',  ( 0.000000000000000000, 0.000000000000000000, 1.000000000000000000 ) ) ;
#7787=ORIENTED_EDGE ( 'NONE', *, *, #18520, .F. ) ;
#7791=DIRECTION ( 'NONE',  ( 1.000000000000000000, 0.000000000000000000, 0.000000000000000000 ) ) ;
#7795=DIRECTION ( 'NONE',  ( 0.000000000000000000, -1.000000000000000000, 0.000000000000000000 ) ) ;
#7800=VERTEX_POINT ( 'NONE', #35551 ) ;
#7804=AXIS2_PLACEMENT_3D ( 'NONE', #33359, #22412, #48239 ) ;
#7810=EDGE_CURVE ( 'NONE', #1819, #66376, #57831, .T. ) ;
#7813=EDGE_CURVE ( 'NONE', #23746, #9687, #46866, .T. ) ;
#7820=VERTEX_POINT ( 'NONE', #62420 ) ;
#7831=DIRECTION ( 'NONE',  ( -1.000000000000000000, 0.000000000000000000, 0.000000000000000000 ) ) ;
#7842=CARTESIAN_POINT ( 'NONE',  ( -30.00000000000000000, -15.97213595500069871, -14.50000000000000000 ) ) ;
#7844=DIRECTION ( 'NONE',  ( 0.000000000000000000, 1.000000000000000000, 0.000000000000000000 ) ) ;
#7855=EDGE_LOOP ( 'NONE', ( #61994, #9078, #29327, #28319 ) ) ;
#7857=ORIENTED_EDGE ( 'NONE', *, *, #45372, .T. ) ;
#7859=ORIENTED_EDGE ( 'NONE', *, *, #50551, .T. ) ;
#7860=LINE ( 'NONE', #29783, #50560 ) ;
#7864=CARTESIAN_POINT ( 'NONE',  ( 23.48000000000000043, -15.50000000000000000, -26.00000000000000355 ) ) ;
#7871=ORIENTED_EDGE ( 'NONE', *, *, #10042, .F. ) ;
#7878=CARTESIAN_POINT ( 'NONE',  ( -11.00000000000000000, -14.04000000000000092, -17.04524521594300523 ) ) ;
#7879=ORIENTED_EDGE ( 'NONE', *, *, #28824, .F. ) ;
#7882=ORIENTED_EDGE ( 'NONE', *, *, #7324, .T. ) ;
#7900=ORIENTED_EDGE ( 'NONE', *, *, #33146, .F. ) ;
#7902=ADVANCED_FACE ( 'NONE', ( #56778 ), #62789, .F. ) ;
#7905=VERTEX_POINT ( 'NONE', #36268 ) ;
#7913=EDGE_LOOP ( 'NONE', ( #68696, #62911, #16531, #33759 ) ) ;
#7914=EDGE_LOOP ( 'NONE', ( #51406, #36601, #58545, #62082 ) ) ;
#7917=CARTESIAN_POINT ( 'NONE',  ( 11.00000000000000000, -5.200000000000001066, 26.59999999999999787 ) ) ;
#7920=ORIENTED_EDGE ( 'NONE', *, *, #47268, .F. ) ;
#7923=DIRECTION ( 'NONE',  ( 0.000000000000000000, 0.000000000000000000, 1.000000000000000000 ) ) ;
#7929=ORIENTED_EDGE ( 'NONE', *, *, #6622, .T. ) ;
#7931=LINE ( 'NONE', #2294, #32445 ) ;
#7933=DIRECTION ( 'NONE',  ( 0.000000000000000000, 0.000000000000000000, 1.000000000000000000 ) ) ;
#7942=AXIS2_PLACEMENT_3D ( 'NONE', #3258, #46385, #67965 ) ;
#7945=CARTESIAN_POINT ( 'NONE',  ( 30.00000000000000000, -17.35230188589299871, 15.35019951917099945 ) ) ;
#7957=CARTESIAN_POINT ( 'NONE',  ( 30.00000000000000000, -5.599999999999379696, -26.60000000000059828 ) ) ;
#7961=CIRCLE ( 'NONE', #50864, 4.500000000000190958 ) ;
#7970=CARTESIAN_POINT ( 'NONE',  ( 24.00000000000000000, -15.50000000000000000, -19.33772233983200195 ) ) ;
#7971=AXIS2_PLACEMENT_3D ( 'NONE', #56434, #46178, #23562 ) ;
#7972=ORIENTED_EDGE ( 'NONE', *, *, #19333, .T. ) ;
#7974=LINE ( 'NONE', #12234, #5326 ) ;
#7975=DIRECTION ( 'NONE',  ( 0.000000000000000000, 0.000000000000000000, -1.000000000000000000 ) ) ;
#7988=ADVANCED_FACE ( 'NONE', ( #20702 ), #16451, .T. ) ;
#8000=CARTESIAN_POINT ( 'NONE',  ( -15.50000000000000000, -1.037157890325000054, -18.50000000000000000 ) ) ;
#8005=DIRECTION ( 'NONE',  ( 0.000000000000000000, 0.000000000000000000, 1.000000000000000000 ) ) ;
#8006=AXIS2_PLACEMENT_3D ( 'NONE', #62373, #29852, #51782 ) ;
#8012=LINE ( 'NONE', #19671, #39489 ) ;
#8013=CARTESIAN_POINT ( 'NONE',  ( -15.50000000000000000, -2.500000000000000000, -23.94337567297399971 ) ) ;
#8014=CARTESIAN_POINT ( 'NONE',  ( 13.00000000000000178, -16.64230188589299786, 14.64519951917100116 ) ) ;
#8025=ADVANCED_FACE ( 'NONE', ( #16101 ), #69844, .F. ) ;
#8027=CARTESIAN_POINT ( 'NONE',  ( -15.50000000000000000, -2.500000000000000000, 21.05662432702600029 ) ) ;
#8033=ORIENTED_EDGE ( 'NONE', *, *, #1483, .T. ) ;
#8037=EDGE_CURVE ( 'NONE', #52042, #64218, #47927, .T. ) ;
#8038=VERTEX_POINT ( 'NONE', #48286 ) ;
#8043=DIRECTION ( 'NONE',  ( 1.000000000000000000, 0.000000000000000000, 0.000000000000000000 ) ) ;
#8044=ORIENTED_EDGE ( 'NONE', *, *, #45661, .F. ) ;
#8056=CARTESIAN_POINT ( 'NONE',  ( -30.00000000000000000, -5.000000000000000000, -27.00000000000000000 ) ) ;
#8061=ORIENTED_EDGE ( 'NONE', *, *, #13623, .T. ) ;
#8065=ORIENTED_EDGE ( 'NONE', *, *, #43626, .F. ) ;
#8067=DIRECTION ( 'NONE',  ( 0.000000000000000000, -0.1249999999999996531, 0.9921567416492215186 ) ) ;
#8071=EDGE_CURVE ( 'NONE', #49745, #47971, #50778, .T. ) ;
#8072=VERTEX_POINT ( 'NONE', #27059 ) ;
#8073=DIRECTION ( 'NONE',  ( 0.000000000000000000, -0.9921567416492215186, 0.1249999999999996531 ) ) ;
#8076=ORIENTED_EDGE ( 'NONE', *, *, #45284, .F. ) ;
#8077=CARTESIAN_POINT ( 'NONE',  ( 30.00000000000000000, -5.000000000000000000, 27.00000000000000000 ) ) ;
#8079=EDGE_CURVE ( 'NONE', #22759, #37065, #38385, .T. ) ;
#8083=EDGE_CURVE ( 'NONE', #66296, #69443, #18050, .T. ) ;
#8087=ORIENTED_EDGE ( 'NONE', *, *, #22093, .T. ) ;
#8093=CARTESIAN_POINT ( 'NONE',  ( 29.50000000000000355, -11.50000000000100009, -19.50000000000103739 ) ) ;
#8094=VECTOR ( 'NONE', #37307, 1000.000000000000000 ) ;
#8099=CARTESIAN_POINT ( 'NONE',  ( 30.00000000000000000, -11.50000000000100009, -19.50000000000103739 ) ) ;
#8100=DIRECTION ( 'NONE',  ( -0.4999999999989417354, 0.000000000000000000, -0.8660254037850495523 ) ) ;
#8109=ORIENTED_EDGE ( 'NONE', *, *, #54793, .T. ) ;
#8118=CARTESIAN_POINT ( 'NONE',  ( -29.25000000000000000, -5.000000000000000000, 26.25000000000000000 ) ) ;
#8123=ORIENTED_EDGE ( 'NONE', *, *, #44976, .T. ) ;
#8124=LINE ( 'NONE', #29697, #39301 ) ;
#8125=VECTOR ( 'NONE', #16581, 1000.000000000000114 ) ;
#8130=ORIENTED_EDGE ( 'NONE', *, *, #35054, .T. ) ;
#8132=CARTESIAN_POINT ( 'NONE',  ( 17.00000000000000000, -17.50000000000000000, 15.70499999999969809 ) ) ;
#8140=VERTEX_POINT ( 'NONE', #33406 ) ;
#8141=AXIS2_PLACEMENT_3D ( 'NONE', #12402, #67570, #40340 ) ;
#8142=EDGE_CURVE ( 'NONE', #69139, #31900, #66613, .T. ) ;
#8143=CARTESIAN_POINT ( 'NONE',  ( 11.50000000000000000, -11.50000000000100009, -15.00000000000084910 ) ) ;
#8153=EDGE_CURVE ( 'NONE', #54936, #18065, #60262, .T. ) ;
#8160=VERTEX_POINT ( 'NONE', #66612 ) ;
#8161=ORIENTED_EDGE ( 'NONE', *, *, #46646, .T. ) ;
#8169=ADVANCED_FACE ( 'NONE', ( #23828 ), #22454, .F. ) ;
#8170=DIRECTION ( 'NONE',  ( 0.000000000000000000, 1.000000000000000000, 0.000000000000000000 ) ) ;
#8184=CARTESIAN_POINT ( 'NONE',  ( 11.00000000000000000, -11.50000000000100009, 19.50000000000103739 ) ) ;
#8189=DIRECTION ( 'NONE',  ( 0.7142857142857395036, 0.000000000000000000, 0.6998542122237394469 ) ) ;
#8203=DIRECTION ( 'NONE',  ( 0.000000000000000000, -1.000000000000000000, 0.000000000000000000 ) ) ;
#8216=EDGE_CURVE ( 'NONE', #60418, #20791, #40071, .T. ) ;
#8225=VERTEX_POINT ( 'NONE', #30887 ) ;
#8231=DIRECTION ( 'NONE',  ( 1.000000000000000000, 0.000000000000000000, 0.000000000000000000 ) ) ;
#8232=AXIS2_PLACEMENT_3D ( 'NONE', #68764, #47881, #8656 ) ;
#8233=VERTEX_POINT ( 'NONE', #24539 ) ;
#8243=ORIENTED_EDGE ( 'NONE', *, *, #5868, .F. ) ;
#8248=PLANE ( 'NONE',  #48050 ) ;
#8258=VECTOR ( 'NONE', #795, 1000.000000000000000 ) ;
#8259=CARTESIAN_POINT ( 'NONE',  ( 11.75000000000000000, -5.000000000000000000, -21.10805890929250950 ) ) ;
#8261=CARTESIAN_POINT ( 'NONE',  ( -25.50000000000000355, -15.50000000000000000, -25.99999999999985079 ) ) ;
#8262=ORIENTED_EDGE ( 'NONE', *, *, #25942, .F. ) ;
#8271=VECTOR ( 'NONE', #20037, 1000.000000000000000 ) ;
#8272=EDGE_LOOP ( 'NONE', ( #27221, #63272, #26068, #2513, #38933, #38240, #69156 ) ) ;
#8277=DIRECTION ( 'NONE',  ( 1.000000000000000000, 0.000000000000000000, 0.000000000000000000 ) ) ;
#8278=CARTESIAN_POINT ( 'NONE',  ( -15.50000000000000000, -1.037157890325000054, 22.50000000000000000 ) ) ;
#8284=ADVANCED_FACE ( 'NONE', ( #56353 ), #24880, .T. ) ;
#8291=DIRECTION ( 'NONE',  ( 0.000000000000000000, -0.7046037717859445770, 0.7096009616573392131 ) ) ;
#8305=EDGE_LOOP ( 'NONE', ( #68304, #69736, #33350, #64408, #26166, #68244, #29730, #36286, #65341, #48698, #62535 ) ) ;
#8312=VECTOR ( 'NONE', #22833, 1000.000000000000000 ) ;
#8313=CARTESIAN_POINT ( 'NONE',  ( -30.00000000000000000, -11.50000000000000000, 15.00000000000000000 ) ) ;
#8316=VECTOR ( 'NONE', #53696, 1000.000000000000000 ) ;
#8320=ORIENTED_EDGE ( 'NONE', *, *, #33430, .F. ) ;
#8329=ORIENTED_EDGE ( 'NONE', *, *, #6206, .F. ) ;
#8339=ADVANCED_FACE ( 'NONE', ( #42185 ), #16365, .F. ) ;
#8348=AXIS2_PLACEMENT_3D ( 'NONE', #46079, #62687, #3295 ) ;
#8354=CARTESIAN_POINT ( 'NONE',  ( 15.50000000000000000, 998.9628421096749662, 22.50000000000000000 ) ) ;
#8357=AXIS2_PLACEMENT_3D ( 'NONE', #68389, #2991, #57773 ) ;
#8359=VECTOR ( 'NONE', #48438, 1000.000000000000000 ) ;
#8365=CARTESIAN_POINT ( 'NONE',  ( 14.05000000000000249, -0.2000000000000000111, 22.50000000000000000 ) ) ;
#8368=LINE ( 'NONE', #8736, #23603 ) ;
#8369=CARTESIAN_POINT ( 'NONE',  ( -11.00000000000000000, -14.33999999999999986, 14.50000000000000000 ) ) ;
#8375=ORIENTED_EDGE ( 'NONE', *, *, #59380, .T. ) ;
#8378=LINE ( 'NONE', #53639, #59246 ) ;
#8380=CYLINDRICAL_SURFACE ( 'NONE', #6794, 0.5000000000079367624 ) ;
#8384=VERTEX_POINT ( 'NONE', #63417 ) ;
#8386=DIRECTION ( 'NONE',  ( -1.000000000000000000, 0.000000000000000000, 0.000000000000000000 ) ) ;
#8387=DIRECTION ( 'NONE',  ( 0.000000000000000000, 0.000000000000000000, 1.000000000000000000 ) ) ;
#8391=ORIENTED_EDGE ( 'NONE', *, *, #34416, .F. ) ;
#8393=ORIENTED_EDGE ( 'NONE', *, *, #41393, .F. ) ;
#8394=ORIENTED_EDGE ( 'NONE', *, *, #27796, .F. ) ;
#8413=EDGE_LOOP ( 'NONE', ( #10305, #63925, #60058, #39641 ) ) ;
#8417=CARTESIAN_POINT ( 'NONE',  ( -15.50000000000000000, 998.9628421096749662, -22.50000000000000000 ) ) ;
#8418=ORIENTED_EDGE ( 'NONE', *, *, #3824, .F. ) ;
#8419=DIRECTION ( 'NONE',  ( 1.000000000000000000, -0.000000000000000000, -0.000000000000000000 ) ) ;
#8431=LINE ( 'NONE', #46615, #65594 ) ;
#8435=CIRCLE ( 'NONE', #51350, 2.250000000000001776 ) ;
#8436=LINE ( 'NONE', #68200, #24074 ) ;
#8449=CARTESIAN_POINT ( 'NONE',  ( 17.24945551514599984, -15.50000000000000000, 25.53140320652400064 ) ) ;
#8451=FACE_OUTER_BOUND ( 'NONE', #33215, .T. ) ;
#8454=CARTESIAN_POINT ( 'NONE',  ( -16.75000000000000000, -0.2038245569916330158, -23.22168783648699986 ) ) ;
#8465=DIRECTION ( 'NONE',  ( 0.000000000000000000, 0.000000000000000000, 1.000000000000000000 ) ) ;
#8470=ORIENTED_EDGE ( 'NONE', *, *, #65563, .T. ) ;
#8471=ADVANCED_FACE ( 'NONE', ( #21328 ), #4718, .T. ) ;
#8473=VERTEX_POINT ( 'NONE', #26280 ) ;
#8492=CARTESIAN_POINT ( 'NONE',  ( -15.91434062215688350, -0.3156604612129211285, -21.29584399676446793 ) ) ;
#8495=LINE ( 'NONE', #30072, #17599 ) ;
#8496=CARTESIAN_POINT ( 'NONE',  ( 15.50000000000000000, -0.4000000000000000222, 25.99999999999999645 ) ) ;
#8500=ORIENTED_EDGE ( 'NONE', *, *, #18068, .T. ) ;
#8501=CIRCLE ( 'NONE', #24353, 0.3500000000009988455 ) ;
#8507=AXIS2_PLACEMENT_3D ( 'NONE', #58277, #9847, #47660 ) ;
#8512=AXIS2_PLACEMENT_3D ( 'NONE', #14256, #35808, #9651 ) ;
#8514=DIRECTION ( 'NONE',  ( 1.000000000000000000, -0.000000000000000000, -0.000000000000000000 ) ) ;
#8519=CARTESIAN_POINT ( 'NONE',  ( 30.00000000000000000, -9.454754784057099570, -17.53999999999999915 ) ) ;
#8526=ORIENTED_EDGE ( 'NONE', *, *, #51003, .F. ) ;
#8546=CIRCLE ( 'NONE', #48100, 0.5000000000079362072 ) ;
#8548=DIRECTION ( 'NONE',  ( -0.7142857142857395036, 0.000000000000000000, -0.6998542122237394469 ) ) ;
#8563=LINE ( 'NONE', #50656, #26810 ) ;
#8569=CARTESIAN_POINT ( 'NONE',  ( 25.50000000000000355, -15.50000000000000000, -20.49999999999999645 ) ) ;
#8573=VERTEX_POINT ( 'NONE', #27669 ) ;
#8576=EDGE_CURVE ( 'NONE', #67636, #62094, #30537, .T. ) ;
#8581=DIRECTION ( 'NONE',  ( 0.000000000000000000, 1.000000000000000000, 0.000000000000000000 ) ) ;
#8582=CARTESIAN_POINT ( 'NONE',  ( 30.00000000000000000, -8.959999999999999076, 17.04524521594300523 ) ) ;
#8591=ORIENTED_EDGE ( 'NONE', *, *, #46172, .T. ) ;
#8594=CARTESIAN_POINT ( 'NONE',  ( -15.91434062215689060, -0.3156604612129251808, 23.70415600323552852 ) ) ;
#8611=EDGE_LOOP ( 'NONE', ( #40784, #57202, #37961, #42521 ) ) ;
#8615=AXIS2_PLACEMENT_3D ( 'NONE', #54842, #28640, #61157 ) ;
#8617=CARTESIAN_POINT ( 'NONE',  ( -25.50000000000000355, 0.000000000000000000, -24.75000000000000000 ) ) ;
#8627=CARTESIAN_POINT ( 'NONE',  ( -11.00000000000000000, -15.97213595500069871, -14.50000000000000000 ) ) ;
#8628=PLANE ( 'NONE',  #7504 ) ;
#8632=ORIENTED_EDGE ( 'NONE', *, *, #13805, .F. ) ;
#8652=DIRECTION ( 'NONE',  ( -1.000000000000000000, 0.000000000000000000, 0.000000000000000000 ) ) ;
#8654=LINE ( 'NONE', #24576, #56772 ) ;
#8655=DIRECTION ( 'NONE',  ( 0.000000000000000000, 0.000000000000000000, -1.000000000000000000 ) ) ;
#8656=DIRECTION ( 'NONE',  ( 0.000000000000000000, 0.000000000000000000, 1.000000000000000000 ) ) ;
#8661=LINE ( 'NONE', #45788, #34530 ) ;
#8662=AXIS2_PLACEMENT_3D ( 'NONE', #56549, #7755, #61487 ) ;
#8670=EDGE_CURVE ( 'NONE', #12490, #21729, #68280, .T. ) ;
#8674=LINE ( 'NONE', #26336, #62766 ) ;
#8685=LINE ( 'NONE', #14689, #62509 ) ;
#8688=CIRCLE ( 'NONE', #22228, 4.500000000000191847 ) ;
#8691=DIRECTION ( 'NONE',  ( -1.000000000000000000, 0.000000000000000000, 0.000000000000000000 ) ) ;
#8695=ORIENTED_EDGE ( 'NONE', *, *, #25340, .T. ) ;
#8704=EDGE_LOOP ( 'NONE', ( #35944, #35427, #7364, #49048, #60616, #64898, #11915, #60921, #50079, #37427, #48515, #36675, #16470, #46376, #23361, #50711 ) ) ;
#8706=ORIENTED_EDGE ( 'NONE', *, *, #54384, .T. ) ;
#8707=ADVANCED_FACE ( 'NONE', ( #51309, #24087 ), #25146, .F. ) ;
#8708=ADVANCED_FACE ( 'NONE', ( #19831 ), #57667, .T. ) ;
#8718=DIRECTION ( 'NONE',  ( 0.4285714285711678118, 0.000000000000000000, 0.9035079029053749711 ) ) ;
#8726=AXIS2_PLACEMENT_3D ( 'NONE', #41725, #62237, #36426 ) ;
#8728=DIRECTION ( 'NONE',  ( 0.000000000000000000, 0.7278708115913771204, 0.6857142857147648929 ) ) ;
#8733=CARTESIAN_POINT ( 'NONE',  ( -30.00000000000000000, -17.50000000000000000, 26.64999999999999858 ) ) ;
#8734=DIRECTION ( 'NONE',  ( 0.000000000000000000, 1.000000000000000000, 0.000000000000000000 ) ) ;
#8736=CARTESIAN_POINT ( 'NONE',  ( -28.00000000000000000, -16.64230188589299786, 14.64519951917100116 ) ) ;
#8739=ORIENTED_EDGE ( 'NONE', *, *, #37552, .T. ) ;
#8741=LINE ( 'NONE', #13689, #27089 ) ;
#8742=EDGE_LOOP ( 'NONE', ( #26271, #7456, #15910, #38300, #43490, #29809, #18499 ) ) ;
#8743=DIRECTION ( 'NONE',  ( 0.000000000000000000, 0.000000000000000000, 1.000000000000000000 ) ) ;
#8748=ORIENTED_EDGE ( 'NONE', *, *, #69075, .T. ) ;
#8750=EDGE_CURVE ( 'NONE', #23746, #67816, #62264, .T. ) ;
#8753=FACE_OUTER_BOUND ( 'NONE', #68269, .T. ) ;
#8754=AXIS2_PLACEMENT_3D ( 'NONE', #65867, #44631, #27012 ) ;
#8763=VERTEX_POINT ( 'NONE', #47066 ) ;
#8766=ORIENTED_EDGE ( 'NONE', *, *, #39432, .T. ) ;
#8769=FACE_OUTER_BOUND ( 'NONE', #59374, .T. ) ;
#8770=DIRECTION ( 'NONE',  ( 1.000000000000000000, 0.000000000000000000, 0.000000000000000000 ) ) ;
#8777=DIRECTION ( 'NONE',  ( 0.000000000000000000, 0.000000000000000000, -1.000000000000000000 ) ) ;
#8791=ORIENTED_EDGE ( 'NONE', *, *, #2316, .T. ) ;
#8795=EDGE_CURVE ( 'NONE', #61811, #22725, #48115, .T. ) ;
#8796=EDGE_LOOP ( 'NONE', ( #7128, #12540, #18429, #32700, #15017 ) ) ;
#8802=VERTEX_POINT ( 'NONE', #9584 ) ;
#8804=LINE ( 'NONE', #62899, #6456 ) ;
#8806=DIRECTION ( 'NONE',  ( 0.000000000000000000, 0.000000000000000000, 1.000000000000000000 ) ) ;
#8813=CARTESIAN_POINT ( 'NONE',  ( -25.50000000000000355, -17.50000000000000000, -25.99999999999985079 ) ) ;
#8815=ORIENTED_EDGE ( 'NONE', *, *, #19497, .F. ) ;
#8816=DIRECTION ( 'NONE',  ( 0.000000000000000000, 0.000000000000000000, 1.000000000000000000 ) ) ;
#8820=DIRECTION ( 'NONE',  ( 0.000000000000000000, 0.000000000000000000, -1.000000000000000000 ) ) ;
#8826=DIRECTION ( 'NONE',  ( 0.000000000000000000, 0.000000000000000000, 1.000000000000000000 ) ) ;
#8839=ADVANCED_FACE ( 'NONE', ( #53776 ), #41749, .T. ) ;
#8840=EDGE_CURVE ( 'NONE', #59731, #27989, #36817, .T. ) ;
#8843=EDGE_CURVE ( 'NONE', #29771, #22437, #14893, .T. ) ;
#8848=DIRECTION ( 'NONE',  ( 0.000000000000000000, 0.000000000000000000, 1.000000000000000000 ) ) ;
#8849=ORIENTED_EDGE ( 'NONE', *, *, #56069, .T. ) ;
#8863=ORIENTED_EDGE ( 'NONE', *, *, #65964, .F. ) ;
#8867=ORIENTED_EDGE ( 'NONE', *, *, #10403, .F. ) ;
#8881=CARTESIAN_POINT ( 'NONE',  ( 30.00000000000000000, -13.54524521594299991, -17.53999999999999915 ) ) ;
#8890=CARTESIAN_POINT ( 'NONE',  ( -22.14589803375000088, -17.50000000000000000, -21.50000000000000000 ) ) ;
#8893=LINE ( 'NONE', #36113, #24739 ) ;
#8896=EDGE_CURVE ( 'NONE', #45446, #55340, #46645, .T. ) ;
#8902=ORIENTED_EDGE ( 'NONE', *, *, #68714, .F. ) ;
#8905=ORIENTED_EDGE ( 'NONE', *, *, #56076, .F. ) ;
#8917=LINE ( 'NONE', #67280, #60381 ) ;
#8929=DIRECTION ( 'NONE',  ( -0.8660254037844482555, 0.000000000000000000, 0.4999999999999831801 ) ) ;
#8930=CARTESIAN_POINT ( 'NONE',  ( 11.50000000000000000, -12.00000000000000000, -10.52786404500095863 ) ) ;
#8942=DIRECTION ( 'NONE',  ( 0.000000000000000000, 0.000000000000000000, -1.000000000000000000 ) ) ;
#8948=VERTEX_POINT ( 'NONE', #21930 ) ;
#8949=CARTESIAN_POINT ( 'NONE',  ( -29.50000000000000355, -11.50000000000000000, -15.00000000000000000 ) ) ;
#8952=CARTESIAN_POINT ( 'NONE',  ( 14.25000000000000000, -2.500000000000000000, -21.77831216351300014 ) ) ;
#8954=ORIENTED_EDGE ( 'NONE', *, *, #32529, .F. ) ;
#8956=ORIENTED_EDGE ( 'NONE', *, *, #17971, .T. ) ;
#8959=ORIENTED_EDGE ( 'NONE', *, *, #9596, .T. ) ;
#8970=VECTOR ( 'NONE', #5366, 1000.000000000000000 ) ;
#8972=CARTESIAN_POINT ( 'NONE',  ( 16.89194109070750116, -5.000000000000000000, 26.25000000000000000 ) ) ;
#8991=CARTESIAN_POINT ( 'NONE',  ( 11.00000000000000000, -11.85423089348099879, -9.852125413066602277 ) ) ;
#8995=DIRECTION ( 'NONE',  ( -0.4999999999999832356, 0.000000000000000000, -0.8660254037844483666 ) ) ;
#9004=DIRECTION ( 'NONE',  ( 0.000000000000000000, 0.6857142857142869419, -0.7278708115918273158 ) ) ;
#9007=VECTOR ( 'NONE', #8581, 1000.000000000000000 ) ;
#9008=LINE ( 'NONE', #31311, #63354 ) ;
#9009=ORIENTED_EDGE ( 'NONE', *, *, #45983, .F. ) ;
#9017=EDGE_CURVE ( 'NONE', #27679, #29817, #49838, .T. ) ;
#9019=CARTESIAN_POINT ( 'NONE',  ( 15.50000000000000000, -5.000000000000000000, -26.00000000000000000 ) ) ;
#9023=AXIS2_PLACEMENT_3D ( 'NONE', #20142, #64670, #31815 ) ;
#9037=VECTOR ( 'NONE', #23061, 1000.000000000000000 ) ;
#9043=ADVANCED_FACE ( 'NONE', ( #16976 ), #44356, .F. ) ;
#9044=EDGE_CURVE ( 'NONE', #67807, #50438, #49499, .T. ) ;
#9048=UNCERTAINTY_MEASURE_WITH_UNIT (LENGTH_MEASURE( 1.000000000000000082E-05 ), #29858, 'distance_accuracy_value', 'NONE');
#9050=EDGE_LOOP ( 'NONE', ( #53591, #11337, #62448, #29903, #26503, #26775, #15815, #26952, #39979, #3603, #27634, #18877, #39339, #8956, #59144, #15584, #19016, #52333 ) ) ;
#9051=ADVANCED_FACE ( 'NONE', ( #34607 ), #24355, .T. ) ;
#9069=DIRECTION ( 'NONE',  ( 0.000000000000000000, 1.000000000000000000, 0.000000000000000000 ) ) ;
#9070=VERTEX_POINT ( 'NONE', #35650 ) ;
#9074=DIRECTION ( 'NONE',  ( 0.000000000000000000, -1.000000000000000000, 0.000000000000000000 ) ) ;
#9078=ORIENTED_EDGE ( 'NONE', *, *, #29541, .T. ) ;
#9097=CARTESIAN_POINT ( 'NONE',  ( 30.00000000000000000, -17.14999999999900027, 26.64999999999900027 ) ) ;
#9104=DIRECTION ( 'NONE',  ( -1.000000000000000000, 0.000000000000000000, 0.000000000000000000 ) ) ;
#9105=ORIENTED_EDGE ( 'NONE', *, *, #35608, .T. ) ;
#9106=EDGE_CURVE ( 'NONE', #27584, #26198, #60645, .T. ) ;
#9109=ADVANCED_FACE ( 'NONE', ( #18695 ), #66781, .F. ) ;
#9113=VERTEX_POINT ( 'NONE', #68190 ) ;
#9115=EDGE_LOOP ( 'NONE', ( #44719, #67166, #18119, #13546 ) ) ;
#9119=ORIENTED_EDGE ( 'NONE', *, *, #34568, .F. ) ;
#9125=VECTOR ( 'NONE', #64083, 1000.000000000000114 ) ;
#9129=VERTEX_POINT ( 'NONE', #13394 ) ;
#9133=AXIS2_PLACEMENT_3D ( 'NONE', #57101, #2311, #24231 ) ;
#9139=VERTEX_POINT ( 'NONE', #67844 ) ;
#9140=VECTOR ( 'NONE', #49630, 999.9999999999998863 ) ;
#9150=CARTESIAN_POINT ( 'NONE',  ( -11.50000000000000000, -12.00000000000000000, -10.52786404500095863 ) ) ;
#9157=DIRECTION ( 'NONE',  ( -0.4999999999989410693, 0.000000000000000000, 0.8660254037850499964 ) ) ;
#9168=DIRECTION ( 'NONE',  ( 0.000000000000000000, -1.000000000000000000, 0.000000000000000000 ) ) ;
#9170=AXIS2_PLACEMENT_3D ( 'NONE', #55246, #28364, #55935 ) ;
#9174=DIRECTION ( 'NONE',  ( 0.000000000000000000, 0.7071067811865495711, -0.7071067811865455743 ) ) ;
#9178=ORIENTED_EDGE ( 'NONE', *, *, #51736, .F. ) ;
#9187=DIRECTION ( 'NONE',  ( 0.000000000000000000, -0.7096009616570518874, 0.7046037717862339012 ) ) ;
#9200=EDGE_CURVE ( 'NONE', #9204, #16876, #52281, .T. ) ;
#9201=ADVANCED_FACE ( 'NONE', ( #10539 ), #58983, .T. ) ;
#9204=VERTEX_POINT ( 'NONE', #26120 ) ;
#9209=ORIENTED_EDGE ( 'NONE', *, *, #17923, .F. ) ;
#9212=CARTESIAN_POINT ( 'NONE',  ( 15.50000000000000000, -5.000000000000000000, 26.00000000000000000 ) ) ;
#9213=DIRECTION ( 'NONE',  ( 0.000000000000000000, 0.000000000000000000, -1.000000000000000000 ) ) ;
#9215=CARTESIAN_POINT ( 'NONE',  ( 11.00000000000000000, -12.00000000000000000, 12.20000000000000107 ) ) ;
#9216=ORIENTED_EDGE ( 'NONE', *, *, #64726, .T. ) ;
#9219=DIRECTION ( 'NONE',  ( 0.000000000000000000, -1.000000000000000000, 0.000000000000000000 ) ) ;
#9229=EDGE_LOOP ( 'NONE', ( #47069, #2468, #53993, #28332 ) ) ;
#9230=CARTESIAN_POINT ( 'NONE',  ( -24.00000000000000000, -17.50000000000000000, -19.33772233983200195 ) ) ;
#9237=CARTESIAN_POINT ( 'NONE',  ( 11.50000000000000000, -11.50000000000100009, -19.50000000000103739 ) ) ;
#9238=ORIENTED_EDGE ( 'NONE', *, *, #32802, .T. ) ;
#9241=CYLINDRICAL_SURFACE ( 'NONE', #19922, 2.250000000000001776 ) ;
#9244=EDGE_CURVE ( 'NONE', #16044, #45304, #26821, .T. ) ;
#9245=ORIENTED_EDGE ( 'NONE', *, *, #17921, .F. ) ;
#9247=EDGE_CURVE ( 'NONE', #24243, #8233, #20113, .T. ) ;
#9248=AXIS2_PLACEMENT_3D ( 'NONE', #28635, #17004, #66125 ) ;
#9257=EDGE_LOOP ( 'NONE', ( #23106, #68263, #33112, #65740 ) ) ;
#9261=DIRECTION ( 'NONE',  ( 0.000000000000000000, 0.000000000000000000, 1.000000000000000000 ) ) ;
#9276=ORIENTED_EDGE ( 'NONE', *, *, #68677, .T. ) ;
#9278=LINE ( 'NONE', #31559, #3711 ) ;
#9279=CARTESIAN_POINT ( 'NONE',  ( -11.00000000000000000, -17.14999999999900027, 26.64999999999900027 ) ) ;
#9281=DIRECTION ( 'NONE',  ( 1.000000000000000000, -0.000000000000000000, -0.000000000000000000 ) ) ;
#9285=EDGE_CURVE ( 'NONE', #54102, #51111, #32504, .T. ) ;
#9286=CARTESIAN_POINT ( 'NONE',  ( -11.50000000000000000, -11.50000000000100009, 15.00000000000084910 ) ) ;
#9291=VECTOR ( 'NONE', #28562, 1000.000000000000114 ) ;
#9293=ADVANCED_FACE ( 'NONE', ( #36723 ), #3842, .F. ) ;
#9297=DIRECTION ( 'NONE',  ( 0.000000000000000000, 1.000000000000000000, 0.000000000000000000 ) ) ;
#9299=CARTESIAN_POINT ( 'NONE',  ( -14.25000000000000000, -0.2038245569916330158, -21.77831216351300014 ) ) ;
#9306=ADVANCED_FACE ( 'NONE', ( #63240 ), #69243, .T. ) ;
#9308=EDGE_CURVE ( 'NONE', #3375, #2041, #15849, .T. ) ;
#9311=ORIENTED_EDGE ( 'NONE', *, *, #9446, .T. ) ;
#9332=DIRECTION ( 'NONE',  ( 0.000000000000000000, 0.000000000000000000, 1.000000000000000000 ) ) ;
#9336=B_SPLINE_CURVE_WITH_KNOTS ( 'NONE', 3,
 ( #60183, #32285, #5065, #16030, #6106, #48206 ),
 .UNSPECIFIED., .F., .F.,
 ( 4, 2, 4 ),
 ( 0.0002380763768129734448, 0.7291065797294589146, 1.457975083082104995 ),
 .UNSPECIFIED. ) ;
#9351=CIRCLE ( 'NONE', #11600, 3.499999999999849454 ) ;
#9356=DIRECTION ( 'NONE',  ( 0.000000000000000000, 0.000000000000000000, 1.000000000000000000 ) ) ;
#9357=LINE ( 'NONE', #21009, #27461 ) ;
#9358=CARTESIAN_POINT ( 'NONE',  ( -14.24999999999999822, -0.3152037684892594616, 22.25410949791978510 ) ) ;
#9364=CARTESIAN_POINT ( 'NONE',  ( -29.50000000000000355, -11.50000000000000000, -19.00000000000000000 ) ) ;
#9370=ADVANCED_FACE ( 'NONE', ( #55415 ), #59679, .T. ) ;
#9371=CARTESIAN_POINT ( 'NONE',  ( 24.00000000000000000, -17.50000000000000000, 15.70499999999969809 ) ) ;
#9386=DIRECTION ( 'NONE',  ( 0.000000000000000000, -0.7096009616570518874, 0.7046037717862339012 ) ) ;
#9391=VERTEX_POINT ( 'NONE', #44098 ) ;
#9392=ORIENTED_EDGE ( 'NONE', *, *, #46118, .T. ) ;
#9393=FACE_OUTER_BOUND ( 'NONE', #64101, .T. ) ;
#9394=CIRCLE ( 'NONE', #54579, 3.499999999999999556 ) ;
#9399=ORIENTED_EDGE ( 'NONE', *, *, #63992, .T. ) ;
#9407=EDGE_CURVE ( 'NONE', #14976, #4599, #16549, .T. ) ;
#9418=DIRECTION ( 'NONE',  ( 0.000000000000000000, 0.000000000000000000, -1.000000000000000000 ) ) ;
#9421=CARTESIAN_POINT ( 'NONE',  ( 18.85410196625000268, -17.50000000000000000, -21.50000000000000000 ) ) ;
#9424=LINE ( 'NONE', #30992, #66372 ) ;
#9425=EDGE_CURVE ( 'NONE', #20373, #50555, #22544, .T. ) ;
#9427=ORIENTED_EDGE ( 'NONE', *, *, #12560, .F. ) ;
#9446=EDGE_CURVE ( 'NONE', #51551, #41185, #69909, .T. ) ;
#9447=EDGE_CURVE ( 'NONE', #30907, #33465, #54126, .T. ) ;
#9460=LINE ( 'NONE', #37045, #47284 ) ;
#9463=ORIENTED_EDGE ( 'NONE', *, *, #54492, .F. ) ;
#9466=ORIENTED_EDGE ( 'NONE', *, *, #56098, .F. ) ;
#9478=CARTESIAN_POINT ( 'NONE',  ( 30.00000000000000000, -17.35230188589299871, 15.35019951917099945 ) ) ;
#9488=CIRCLE ( 'NONE', #38849, 2.000000000000001776 ) ;
#9490=VERTEX_POINT ( 'NONE', #34164 ) ;
#9496=CARTESIAN_POINT ( 'NONE',  ( 15.50000000000000000, 0.000000000000000000, 22.50000000000000000 ) ) ;
#9503=DIRECTION ( 'NONE',  ( 0.000000000000000000, 0.6857142857146703019, -0.7278708115914659382 ) ) ;
#9505=CARTESIAN_POINT ( 'NONE',  ( 17.51999999999999957, -17.50000000000000000, -26.00000000000000355 ) ) ;
#9509=EDGE_CURVE ( 'NONE', #22867, #54447, #3282, .T. ) ;
#9513=EDGE_CURVE ( 'NONE', #56934, #59373, #45836, .T. ) ;
#9514=LINE ( 'NONE', #30730, #55042 ) ;
#9518=ORIENTED_EDGE ( 'NONE', *, *, #32161, .T. ) ;
#9519=CARTESIAN_POINT ( 'NONE',  ( -11.50000000000000000, -12.00000000000000000, 10.69999999999999929 ) ) ;
#9533=VECTOR ( 'NONE', #45161, 1000.000000000000000 ) ;
#9538=DIRECTION ( 'NONE',  ( 1.000000000000000000, -0.000000000000000000, -0.000000000000000000 ) ) ;
#9542=VECTOR ( 'NONE', #39429, 1000.000000000000000 ) ;
#9554=DIRECTION ( 'NONE',  ( 1.000000000000000000, -0.000000000000000000, -0.000000000000000000 ) ) ;
#9560=VERTEX_POINT ( 'NONE', #32644 ) ;
#9569=CARTESIAN_POINT ( 'NONE',  ( 29.50000000000000355, -12.00000000000000000, 11.00000000000000000 ) ) ;
#9581=VECTOR ( 'NONE', #43718, 1000.000000000000000 ) ;
#9583=ORIENTED_EDGE ( 'NONE', *, *, #20014, .F. ) ;
#9584=CARTESIAN_POINT ( 'NONE',  ( -11.00000000000000000, -17.14999999999999858, -27.00000000000000000 ) ) ;
#9587=EDGE_CURVE ( 'NONE', #11595, #27939, #5778, .T. ) ;
#9591=CARTESIAN_POINT ( 'NONE',  ( -15.50000000000000000, -0.1999999999999999556, -22.50000000000000000 ) ) ;
#9596=EDGE_CURVE ( 'NONE', #6050, #23985, #38324, .T. ) ;
#9599=CARTESIAN_POINT ( 'NONE',  ( -29.50000000000000355, -11.50000000000000000, -15.00000000000000000 ) ) ;
#9603=CARTESIAN_POINT ( 'NONE',  ( 11.50000000000000000, -12.00000000000000000, -10.52786404500095863 ) ) ;
#9614=VECTOR ( 'NONE', #69180, 1000.000000000000000 ) ;
#9619=LINE ( 'NONE', #62642, #22813 ) ;
#9621=CARTESIAN_POINT ( 'NONE',  ( -16.75000000000000000, -0.2038245569916330158, 21.77831216351300014 ) ) ;
#9627=ORIENTED_EDGE ( 'NONE', *, *, #21200, .T. ) ;
#9636=VECTOR ( 'NONE', #18289, 1000.000000000000114 ) ;
#9646=AXIS2_PLACEMENT_3D ( 'NONE', #17559, #24535, #40440 ) ;
#9651=DIRECTION ( 'NONE',  ( 0.000000000000000000, 0.000000000000000000, 1.000000000000000000 ) ) ;
#9661=VECTOR ( 'NONE', #53848, 1000.000000000000000 ) ;
#9663=DIRECTION ( 'NONE',  ( 0.000000000000000000, 0.000000000000000000, 1.000000000000000000 ) ) ;
#9667=ORIENTED_EDGE ( 'NONE', *, *, #13891, .F. ) ;
#9672=ORIENTED_EDGE ( 'NONE', *, *, #10320, .F. ) ;
#9673=ORIENTED_EDGE ( 'NONE', *, *, #42802, .T. ) ;
#9675=ORIENTED_EDGE ( 'NONE', *, *, #38577, .T. ) ;
#9680=ORIENTED_EDGE ( 'NONE', *, *, #15672, .F. ) ;
#9687=VERTEX_POINT ( 'NONE', #69429 ) ;
#9696=ORIENTED_EDGE ( 'NONE', *, *, #22019, .T. ) ;
#9699=VECTOR ( 'NONE', #49916, 1000.000000000000000 ) ;
#9701=DIRECTION ( 'NONE',  ( 0.8660254037844482555, 0.000000000000000000, 0.4999999999999831801 ) ) ;
#9705=AXIS2_PLACEMENT_3D ( 'NONE', #66627, #62715, #1932 ) ;
#9716=CYLINDRICAL_SURFACE ( 'NONE', #39975, 4.000000000000000000 ) ;
#9718=DIRECTION ( 'NONE',  ( 1.000000000000000000, -0.000000000000000000, -0.000000000000000000 ) ) ;
#9723=CARTESIAN_POINT ( 'NONE',  ( 30.00000000000000000, -10.85999999999999943, 9.350000000000269651 ) ) ;
#9727=DIRECTION ( 'NONE',  ( 0.000000000000000000, -1.000000000000000000, 0.000000000000000000 ) ) ;
#9730=LINE ( 'NONE', #30944, #65107 ) ;
#9732=EDGE_LOOP ( 'NONE', ( #18251, #64042, #60061, #21885, #19597, #61004, #14508 ) ) ;
#9736=EDGE_CURVE ( 'NONE', #55561, #52369, #6114, .T. ) ;
#9744=VERTEX_POINT ( 'NONE', #55933 ) ;
#9765=ORIENTED_EDGE ( 'NONE', *, *, #60633, .T. ) ;
#9770=ORIENTED_EDGE ( 'NONE', *, *, #8670, .T. ) ;
#9771=ORIENTED_EDGE ( 'NONE', *, *, #16869, .F. ) ;
#9777=EDGE_CURVE ( 'NONE', #22677, #373, #58165, .T. ) ;
#9783=CARTESIAN_POINT ( 'NONE',  ( -11.75000000000000000, -5.000000000000000000, -21.10805890929250239 ) ) ;
#9787=DIRECTION ( 'NONE',  ( -1.000000000000000000, 0.000000000000000000, 0.000000000000000000 ) ) ;
#9805=CARTESIAN_POINT ( 'NONE',  ( 30.00000000000000000, -17.35230188589299871, 15.35019951917099945 ) ) ;
#9807=CARTESIAN_POINT ( 'NONE',  ( 11.00000000000000000, -11.50000000000100009, 15.00000000000084910 ) ) ;
#9817=AXIS2_PLACEMENT_3D ( 'NONE', #52838, #63425, #14988 ) ;
#9828=DIRECTION ( 'NONE',  ( 1.000000000000000000, 0.000000000000000000, 0.000000000000000000 ) ) ;
#9834=EDGE_LOOP ( 'NONE', ( #25035, #41635, #67390, #26862 ) ) ;
#9845=VECTOR ( 'NONE', #27855, 1000.000000000000000 ) ;
#9847=DIRECTION ( 'NONE',  ( 0.000000000000000000, -1.000000000000000000, 0.000000000000000000 ) ) ;
#9852=CARTESIAN_POINT ( 'NONE',  ( 25.50000000000000355, -15.50000000000000000, -22.50000000000000000 ) ) ;
#9857=VECTOR ( 'NONE', #41017, 1000.000000000000000 ) ;
#9859=ADVANCED_FACE ( 'NONE', ( #49589 ), #1161, .T. ) ;
#9861=CARTESIAN_POINT ( 'NONE',  ( 28.00000000000000000, -15.50000000000000000, 20.05051025721700242 ) ) ;
#9862=AXIS2_PLACEMENT_3D ( 'NONE', #57147, #13659, #56439 ) ;
#9864=DIRECTION ( 'NONE',  ( 0.000000000000000000, 1.000000000000000000, 0.000000000000000000 ) ) ;
#9867=DIRECTION ( 'NONE',  ( 0.000000000000000000, 0.000000000000000000, 1.000000000000000000 ) ) ;
#9881=FACE_OUTER_BOUND ( 'NONE', #23083, .T. ) ;
#9894=EDGE_CURVE ( 'NONE', #974, #20953, #30809, .T. ) ;
#9896=CARTESIAN_POINT ( 'NONE',  ( -28.00000000000000000, -16.28999999999999915, 14.50000000000000000 ) ) ;
#9899=CARTESIAN_POINT ( 'NONE',  ( -11.00000000000000000, -11.10796162543699950, -9.102987789146602893 ) ) ;
#9900=DIRECTION ( 'NONE',  ( 0.000000000000000000, 0.000000000000000000, 1.000000000000000000 ) ) ;
#9911=CONICAL_SURFACE ( 'NONE', #29061, 2.000000000000001776, 0.7853981633974503884 ) ;
#9912=EDGE_CURVE ( 'NONE', #18037, #51018, #2881, .T. ) ;
#9914=DIRECTION ( 'NONE',  ( -1.000000000000000000, 0.000000000000000000, 0.000000000000000000 ) ) ;
#9927=DIRECTION ( 'NONE',  ( 8.659560562354951347E-17, -0.7071067811865460184, 0.7071067811865489050 ) ) ;
#9931=DIRECTION ( 'NONE',  ( 0.000000000000000000, 1.000000000000000000, 0.000000000000000000 ) ) ;
#9932=EDGE_LOOP ( 'NONE', ( #16187, #27195, #4355, #61907 ) ) ;
#9941=CARTESIAN_POINT ( 'NONE',  ( -11.00000000000000000, -11.50000000000000000, -15.00000000000000000 ) ) ;
#9952=CYLINDRICAL_SURFACE ( 'NONE', #23295, 4.500000000000189182 ) ;
#9953=FACE_OUTER_BOUND ( 'NONE', #35550, .T. ) ;
#9955=VERTEX_POINT ( 'NONE', #67239 ) ;
#9959=CIRCLE ( 'NONE', #69771, 2.000000000000001776 ) ;
#9962=FACE_OUTER_BOUND ( 'NONE', #33688, .T. ) ;
#9966=ORIENTED_EDGE ( 'NONE', *, *, #47243, .F. ) ;
#9971=VECTOR ( 'NONE', #45412, 1000.000000000000000 ) ;
#9979=EDGE_LOOP ( 'NONE', ( #65781, #47563, #2325, #36064 ) ) ;
#9986=AXIS2_PLACEMENT_3D ( 'NONE', #12030, #55186, #38247 ) ;
#9990=CARTESIAN_POINT ( 'NONE',  ( 13.00000000000000178, -17.35230188589299871, -15.35019951917099945 ) ) ;
#9992=CARTESIAN_POINT ( 'NONE',  ( 25.50000000000000355, -5.200000000000001066, 20.49999999999999645 ) ) ;
#10000=DIRECTION ( 'NONE',  ( 1.000000000000000000, -0.000000000000000000, -0.000000000000000000 ) ) ;
#10004=VECTOR ( 'NONE', #24005, 1000.000000000000000 ) ;
#10009=ORIENTED_EDGE ( 'NONE', *, *, #27499, .T. ) ;
#10023=DIRECTION ( 'NONE',  ( 0.000000000000000000, -1.000000000000000000, 0.000000000000000000 ) ) ;
#10026=ORIENTED_EDGE ( 'NONE', *, *, #2287, .T. ) ;
#10027=CARTESIAN_POINT ( 'NONE',  ( 30.00000000000000000, -9.200000000000120082, -17.30000000000000071 ) ) ;
#10038=FACE_OUTER_BOUND ( 'NONE', #47476, .T. ) ;
#10042=EDGE_CURVE ( 'NONE', #34031, #37597, #42112, .T. ) ;
#10046=EDGE_CURVE ( 'NONE', #57233, #1031, #67808, .T. ) ;
#10051=CARTESIAN_POINT ( 'NONE',  ( -25.50000000000000355, -5.200000000000001066, -22.50000000000000000 ) ) ;
#10056=VECTOR ( 'NONE', #7299, 1000.000000000000000 ) ;
#10060=DIRECTION ( 'NONE',  ( -1.000000000000000000, 0.000000000000000000, 0.000000000000000000 ) ) ;
#10061=ORIENTED_EDGE ( 'NONE', *, *, #26015, .F. ) ;
#10070=LINE ( 'NONE', #48245, #10737 ) ;
#10075=CARTESIAN_POINT ( 'NONE',  ( -11.00000000000000000, -5.200000000000001066, -9.400000000000000355 ) ) ;
#10096=ADVANCED_FACE ( 'NONE', ( #48131 ), #10991, .T. ) ;
#10100=CARTESIAN_POINT ( 'NONE',  ( -28.00000000000000000, -15.50000000000000000, 14.49999999999999645 ) ) ;
#10101=ORIENTED_EDGE ( 'NONE', *, *, #286, .F. ) ;
#10104=AXIS2_PLACEMENT_3D ( 'NONE', #47942, #5513, #44612 ) ;
#10105=ORIENTED_EDGE ( 'NONE', *, *, #28645, .F. ) ;
#10106=DIRECTION ( 'NONE',  ( 0.000000000000000000, 1.000000000000000000, 0.000000000000000000 ) ) ;
#10122=ORIENTED_EDGE ( 'NONE', *, *, #17321, .T. ) ;
#10123=EDGE_CURVE ( 'NONE', #3316, #47101, #47416, .T. ) ;
#10128=CARTESIAN_POINT ( 'NONE',  ( -30.00000000000000000, -13.79999999999979998, 17.30000000000000071 ) ) ;
#10132=DIRECTION ( 'NONE',  ( 0.000000000000000000, 1.000000000000000000, 0.000000000000000000 ) ) ;
#10134=AXIS2_PLACEMENT_3D ( 'NONE', #51544, #19353, #35249 ) ;
#10138=LINE ( 'NONE', #15094, #41689 ) ;
#10157=DIRECTION ( 'NONE',  ( 0.000000000000000000, 0.000000000000000000, 1.000000000000000000 ) ) ;
#10164=ORIENTED_EDGE ( 'NONE', *, *, #10320, .T. ) ;
#10183=VECTOR ( 'NONE', #12144, 1000.000000000000000 ) ;
#10191=ORIENTED_EDGE ( 'NONE', *, *, #5120, .F. ) ;
#10192=VECTOR ( 'NONE', #68573, 1000.000000000000000 ) ;
#10205=VERTEX_POINT ( 'NONE', #16988 ) ;
#10213=DIRECTION ( 'NONE',  ( 0.000000000000000000, 1.000000000000000000, 0.000000000000000000 ) ) ;
#10229=DIRECTION ( 'NONE',  ( -0.4999999999989410693, 0.000000000000000000, 0.8660254037850499964 ) ) ;
#10233=LINE ( 'NONE', #21535, #15447 ) ;
#10237=CARTESIAN_POINT ( 'NONE',  ( -11.00000000000000000, -17.50000000000000000, 26.64999999999999858 ) ) ;
#10238=VECTOR ( 'NONE', #36450, 1000.000000000000000 ) ;
#10239=CARTESIAN_POINT ( 'NONE',  ( 29.50000000000000355, -11.50000000000100009, -15.00000000000084910 ) ) ;
#10240=VECTOR ( 'NONE', #53783, 1000.000000000000000 ) ;
#10241=VERTEX_POINT ( 'NONE', #60798 ) ;
#10251=ORIENTED_EDGE ( 'NONE', *, *, #29226, .T. ) ;
#10257=EDGE_CURVE ( 'NONE', #52237, #41185, #60110, .T. ) ;
#10258=DIRECTION ( 'NONE',  ( 1.000000000000000000, 0.000000000000000000, 0.000000000000000000 ) ) ;
#10269=CARTESIAN_POINT ( 'NONE',  ( -30.00000000000000000, -11.50000000000000000, 15.00000000000000000 ) ) ;
#10270=EDGE_CURVE ( 'NONE', #38222, #32779, #4307, .T. ) ;
#10271=ORIENTED_EDGE ( 'NONE', *, *, #68670, .T. ) ;
#10272=ORIENTED_EDGE ( 'NONE', *, *, #28106, .T. ) ;
#10273=EDGE_CURVE ( 'NONE', #65734, #48070, #18008, .T. ) ;
#10278=CARTESIAN_POINT ( 'NONE',  ( -30.00000000000000000, -11.70000000000000284, 12.50000000000000000 ) ) ;
#10280=VERTEX_POINT ( 'NONE', #43500 ) ;
#10290=CARTESIAN_POINT ( 'NONE',  ( -29.50000000000000355, -11.50000000000100009, -15.00000000000084910 ) ) ;
#10291=CARTESIAN_POINT ( 'NONE',  ( -11.00000000000000000, -9.200000000000120082, -17.30000000000000071 ) ) ;
#10292=VERTEX_POINT ( 'NONE', #40973 ) ;
#10293=DIRECTION ( 'NONE',  ( 0.000000000000000000, 1.000000000000000000, 0.000000000000000000 ) ) ;
#10300=AXIS2_PLACEMENT_3D ( 'NONE', #67283, #45003, #12815 ) ;
#10305=ORIENTED_EDGE ( 'NONE', *, *, #67999, .F. ) ;
#10310=DIRECTION ( 'NONE',  ( 0.000000000000000000, 0.000000000000000000, 1.000000000000000000 ) ) ;
#10315=CARTESIAN_POINT ( 'NONE',  ( -16.75000000000000000, -0.3156864504677194816, 22.25638000318209109 ) ) ;
#10320=EDGE_CURVE ( 'NONE', #68853, #13557, #51600, .T. ) ;
#10324=DIRECTION ( 'NONE',  ( 0.000000000000000000, -0.1249999999999996531, -0.9921567416492215186 ) ) ;
#10325=ORIENTED_EDGE ( 'NONE', *, *, #20360, .T. ) ;
#10328=EDGE_CURVE ( 'NONE', #41566, #64346, #171, .T. ) ;
#10332=EDGE_CURVE ( 'NONE', #46652, #49722, #3162, .T. ) ;
#10339=LINE ( 'NONE', #17029, #21616 ) ;
#10343=CARTESIAN_POINT ( 'NONE',  ( 30.00000000000000000, -9.454754784057099570, -17.53999999999999915 ) ) ;
#10350=DIRECTION ( 'NONE',  ( 0.000000000000000000, 0.000000000000000000, -1.000000000000000000 ) ) ;
#10357=DIRECTION ( 'NONE',  ( 0.000000000000000000, -1.000000000000000000, 0.000000000000000000 ) ) ;
#10359=DIRECTION ( 'NONE',  ( -1.000000000000000000, 0.000000000000000000, 0.000000000000000000 ) ) ;
#10361=EDGE_CURVE ( 'NONE', #10509, #66537, #3541, .T. ) ;
#10366=DIRECTION ( 'NONE',  ( 0.000000000000000000, 0.000000000000000000, 1.000000000000000000 ) ) ;
#10381=CARTESIAN_POINT ( 'NONE',  ( -25.50000000000000355, -15.50000000000000000, -22.50000000000000000 ) ) ;
#10393=CARTESIAN_POINT ( 'NONE',  ( 16.75000000000000000, -0.3156864504677172611, 22.74361999681791602 ) ) ;
#10394=FACE_OUTER_BOUND ( 'NONE', #68154, .T. ) ;
#10395=EDGE_CURVE ( 'NONE', #10, #54618, #25075, .T. ) ;
#10396=CARTESIAN_POINT ( 'NONE',  ( 30.00000000000000000, -16.64230188589299786, -14.64519951917100116 ) ) ;
#10397=CARTESIAN_POINT ( 'NONE',  ( 11.50000000000000000, -12.00000000000000000, -11.00000000000000000 ) ) ;
#10402=CARTESIAN_POINT ( 'NONE',  ( 30.00000000000000000, -12.00000000000000000, -10.52786404500095863 ) ) ;
#10403=EDGE_CURVE ( 'NONE', #47349, #27438, #52660, .T. ) ;
#10404=FACE_OUTER_BOUND ( 'NONE', #63044, .T. ) ;
#10423=CARTESIAN_POINT ( 'NONE',  ( -17.00000000000000000, -15.50000000000000000, 14.50000000000000000 ) ) ;
#10425=DIRECTION ( 'NONE',  ( 0.000000000000000000, 0.000000000000000000, -1.000000000000000000 ) ) ;
#10427=CARTESIAN_POINT ( 'NONE',  ( 11.75000000000000000, -5.000000000000000000, -26.25000000000000000 ) ) ;
#10454=CIRCLE ( 'NONE', #52192, 0.4000000000000617506 ) ;
#10461=VECTOR ( 'NONE', #32194, 1000.000000000000000 ) ;
#10465=LINE ( 'NONE', #42645, #42602 ) ;
#10471=EDGE_CURVE ( 'NONE', #43574, #11904, #32483, .T. ) ;
#10473=EDGE_CURVE ( 'NONE', #54618, #50768, #64306, .T. ) ;
#10494=VECTOR ( 'NONE', #37223, 1000.000000000000114 ) ;
#10499=FACE_OUTER_BOUND ( 'NONE', #5224, .T. ) ;
#10505=ORIENTED_EDGE ( 'NONE', *, *, #39519, .F. ) ;
#10506=CIRCLE ( 'NONE', #34154, 4.000000000000000888 ) ;
#10509=VERTEX_POINT ( 'NONE', #32125 ) ;
#10511=CARTESIAN_POINT ( 'NONE',  ( -15.50000000000129852, -15.50000000000000000, 22.50000000000000000 ) ) ;
#10535=EDGE_LOOP ( 'NONE', ( #42693, #16764, #21632, #60790 ) ) ;
#10539=FACE_OUTER_BOUND ( 'NONE', #18475, .T. ) ;
#10544=VECTOR ( 'NONE', #57644, 1000.000000000000000 ) ;
#10563=CARTESIAN_POINT ( 'NONE',  ( -18.85410196625000268, -15.50000000000000000, -21.50000000000000000 ) ) ;
#10564=EDGE_LOOP ( 'NONE', ( #29197, #60201, #62002, #39138 ) ) ;
#10567=FACE_OUTER_BOUND ( 'NONE', #6918, .T. ) ;
#10568=DIRECTION ( 'NONE',  ( 0.000000000000000000, 0.000000000000000000, 1.000000000000000000 ) ) ;
#10569=CARTESIAN_POINT ( 'NONE',  ( 11.50000000000000000, -15.97213595500069871, 14.50000000000000000 ) ) ;
#10570=ORIENTED_EDGE ( 'NONE', *, *, #38115, .T. ) ;
#10575=FACE_OUTER_BOUND ( 'NONE', #44652, .T. ) ;
#10579=ADVANCED_FACE ( 'NONE', ( #22891 ), #16902, .F. ) ;
#10585=DIRECTION ( 'NONE',  ( 0.000000000000000000, 0.000000000000000000, 1.000000000000000000 ) ) ;
#10587=DIRECTION ( 'NONE',  ( 0.000000000000000000, 0.000000000000000000, 1.000000000000000000 ) ) ;
#10632=DIRECTION ( 'NONE',  ( 0.000000000000000000, -0.1249999999999996531, -0.9921567416492215186 ) ) ;
#10633=CARTESIAN_POINT ( 'NONE',  ( 11.50000000000000000, -11.50000000000000000, 19.00000000000000000 ) ) ;
#10634=VECTOR ( 'NONE', #52323, 1000.000000000000114 ) ;
#10640=CARTESIAN_POINT ( 'NONE',  ( 30.00000000000000000, 0.000000000000000000, 27.00000000000000000 ) ) ;
#10655=EDGE_CURVE ( 'NONE', #27235, #29819, #54048, .T. ) ;
#10663=CONICAL_SURFACE ( 'NONE', #27570, 2.000000000000001776, 0.7853981633974503884 ) ;
#10664=LINE ( 'NONE', #37543, #56248 ) ;
#10668=CARTESIAN_POINT ( 'NONE',  ( -11.75000000000000000, -5.200000000000001066, -26.25000000000000000 ) ) ;
#10689=DIRECTION ( 'NONE',  ( 0.7142857142857395036, 0.000000000000000000, 0.6998542122237394469 ) ) ;
#10695=DIRECTION ( 'NONE',  ( -1.000000000000000000, 0.000000000000000000, 0.000000000000000000 ) ) ;
#10699=CARTESIAN_POINT ( 'NONE',  ( 30.00000000000000000, -14.33999999999999986, 14.50000000000000000 ) ) ;
#10700=EDGE_LOOP ( 'NONE', ( #53271, #26628, #43458, #65671 ) ) ;
#10711=AXIS2_PLACEMENT_3D ( 'NONE', #23622, #45183, #34579 ) ;
#10714=EDGE_LOOP ( 'NONE', ( #52251, #67966, #27681, #64199 ) ) ;
#10716=DIRECTION ( 'NONE',  ( -1.000000000000000000, 0.000000000000000000, 0.000000000000000000 ) ) ;
#10717=ADVANCED_FACE ( 'NONE', ( #17232 ), #61048, .F. ) ;
#10721=ORIENTED_EDGE ( 'NONE', *, *, #39239, .F. ) ;
#10724=DIRECTION ( 'NONE',  ( 0.000000000000000000, -1.000000000000000000, 0.000000000000000000 ) ) ;
#10725=ADVANCED_FACE ( 'NONE', ( #7307 ), #26468, .F. ) ;
#10729=CARTESIAN_POINT ( 'NONE',  ( 25.50000000000000355, 0.000000000000000000, -22.50000000000000000 ) ) ;
#10731=CARTESIAN_POINT ( 'NONE',  ( -29.50000000000000355, -15.46862696659690073, 14.50000000000000000 ) ) ;
#10737=VECTOR ( 'NONE', #11105, 1000.000000000000000 ) ;
#10738=ORIENTED_EDGE ( 'NONE', *, *, #34961, .F. ) ;
#10740=DIRECTION ( 'NONE',  ( -1.000000000000000000, 0.000000000000000000, 0.000000000000000000 ) ) ;
#10745=FACE_OUTER_BOUND ( 'NONE', #47529, .T. ) ;
#10755=AXIS2_PLACEMENT_3D ( 'NONE', #31583, #26615, #25930 ) ;
#10758=DIRECTION ( 'NONE',  ( 0.000000000000000000, 0.000000000000000000, 1.000000000000000000 ) ) ;
#10766=CARTESIAN_POINT ( 'NONE',  ( 25.50000000000000355, -5.578999999999999737, -24.12099999999999866 ) ) ;
#10786=CARTESIAN_POINT ( 'NONE',  ( 11.00000000000000000, -9.200000000000120082, 17.30000000000000071 ) ) ;
#10792=AXIS2_PLACEMENT_3D ( 'NONE', #55436, #33516, #66387 ) ;
#10799=VECTOR ( 'NONE', #42334, 1000.000000000000000 ) ;
#10804=CIRCLE ( 'NONE', #58255, 0.4000000000000609179 ) ;
#10805=CARTESIAN_POINT ( 'NONE',  ( -25.50000000000000355, -5.578999999999999737, -22.50000000000000000 ) ) ;
#10823=EDGE_CURVE ( 'NONE', #16848, #44232, #25415, .T. ) ;
#10827=CARTESIAN_POINT ( 'NONE',  ( 17.51999999999999957, -15.50000000000000000, 26.00000000000000355 ) ) ;
#10834=DIRECTION ( 'NONE',  ( 1.000000000000000000, 0.000000000000000000, 0.000000000000000000 ) ) ;
#10836=VECTOR ( 'NONE', #34462, 1000.000000000000000 ) ;
#10838=CARTESIAN_POINT ( 'NONE',  ( 30.00000000000000000, -15.46862696659690073, -14.50000000000000000 ) ) ;
#10843=ORIENTED_EDGE ( 'NONE', *, *, #14921, .F. ) ;
#10848=VECTOR ( 'NONE', #38713, 1000.000000000000000 ) ;
#10851=PLANE ( 'NONE',  #30681 ) ;
#10852=VERTEX_POINT ( 'NONE', #9421 ) ;
#10854=CARTESIAN_POINT ( 'NONE',  ( -15.50000000000000000, -1.037157890325000054, -26.50000000000000000 ) ) ;
#10857=DIRECTION ( 'NONE',  ( 0.000000000000000000, -0.9938079899998859545, 0.1111111111112941946 ) ) ;
#10859=DIRECTION ( 'NONE',  ( 0.000000000000000000, 1.000000000000000000, 0.000000000000000000 ) ) ;
#10860=EDGE_CURVE ( 'NONE', #66251, #32707, #52528, .T. ) ;
#10870=DIRECTION ( 'NONE',  ( -1.000000000000000000, 0.000000000000000000, 0.000000000000000000 ) ) ;
#10873=ORIENTED_EDGE ( 'NONE', *, *, #57423, .T. ) ;
#10883=DIRECTION ( 'NONE',  ( 0.000000000000000000, 0.000000000000000000, -1.000000000000000000 ) ) ;
#10885=VECTOR ( 'NONE', #21700, 1000.000000000000000 ) ;
#10895=AXIS2_PLACEMENT_3D ( 'NONE', #50573, #55529, #61505 ) ;
#10900=EDGE_LOOP ( 'NONE', ( #5598, #65875, #65025, #8087 ) ) ;
#10915=ORIENTED_EDGE ( 'NONE', *, *, #26015, .T. ) ;
#10923=ORIENTED_EDGE ( 'NONE', *, *, #35671, .T. ) ;
#10924=CARTESIAN_POINT ( 'NONE',  ( -24.00000000000000000, -15.50000000000000000, 19.33772233983200195 ) ) ;
#10931=CYLINDRICAL_SURFACE ( 'NONE', #48819, 4.500000000000188294 ) ;
#10935=ORIENTED_EDGE ( 'NONE', *, *, #19740, .F. ) ;
#10941=VECTOR ( 'NONE', #9168, 1000.000000000000000 ) ;
#10942=VECTOR ( 'NONE', #11564, 1000.000000000000000 ) ;
#10953=DIRECTION ( 'NONE',  ( 1.000000000000000000, -0.000000000000000000, -0.000000000000000000 ) ) ;
#10959=CARTESIAN_POINT ( 'NONE',  ( 30.00000000000000000, -17.35230188589299871, -15.35019951917099945 ) ) ;
#10962=DIRECTION ( 'NONE',  ( 0.000000000000000000, 1.000000000000000000, 0.000000000000000000 ) ) ;
#10963=EDGE_LOOP ( 'NONE', ( #68723, #60655, #49210, #24241 ) ) ;
#10964=EDGE_CURVE ( 'NONE', #46013, #57327, #38910, .T. ) ;
#10968=EDGE_CURVE ( 'NONE', #60323, #9139, #18498, .T. ) ;
#10971=VECTOR ( 'NONE', #54737, 1000.000000000000000 ) ;
#10981=CARTESIAN_POINT ( 'NONE',  ( -17.00000000000000000, -15.50000000000000000, -14.50000000000000000 ) ) ;
#10983=VERTEX_POINT ( 'NONE', #19553 ) ;
#10991=PLANE ( 'NONE',  #11054 ) ;
#10993=CARTESIAN_POINT ( 'NONE',  ( -30.00000000000000000, -9.199999999999999289, -12.34999999999989839 ) ) ;
#10995=CARTESIAN_POINT ( 'NONE',  ( -13.00000000000000178, -16.28999999999710369, -14.50000000000000000 ) ) ;
#10996=AXIS2_PLACEMENT_3D ( 'NONE', #56462, #67071, #61057 ) ;
#11001=LINE ( 'NONE', #11673, #37937 ) ;
#11002=ORIENTED_EDGE ( 'NONE', *, *, #7740, .T. ) ;
#11008=EDGE_CURVE ( 'NONE', #4595, #30792, #67040, .T. ) ;
#11012=EDGE_LOOP ( 'NONE', ( #65996, #24457, #61322, #62164 ) ) ;
#11014=DIRECTION ( 'NONE',  ( 1.000000000000000000, -0.000000000000000000, -0.000000000000000000 ) ) ;
#11022=FACE_OUTER_BOUND ( 'NONE', #39130, .T. ) ;
#11028=CARTESIAN_POINT ( 'NONE',  ( -25.50000000000000355, -5.200000000000001066, -20.24999999999999645 ) ) ;
#11029=ORIENTED_EDGE ( 'NONE', *, *, #58341, .T. ) ;
#11031=CARTESIAN_POINT ( 'NONE',  ( 30.00000000000000000, -17.14999999999999858, 27.00000000000000000 ) ) ;
#11046=DIRECTION ( 'NONE',  ( 0.000000000000000000, 0.000000000000000000, 1.000000000000000000 ) ) ;
#11047=CARTESIAN_POINT ( 'NONE',  ( 25.50000000000000355, 0.000000000000000000, 24.75000000000000000 ) ) ;
#11053=ORIENTED_EDGE ( 'NONE', *, *, #23005, .T. ) ;
#11054=AXIS2_PLACEMENT_3D ( 'NONE', #27262, #69703, #37521 ) ;
#11057=VERTEX_POINT ( 'NONE', #68004 ) ;
#11065=VERTEX_POINT ( 'NONE', #40059 ) ;
#11075=EDGE_LOOP ( 'NONE', ( #64592, #53329, #43412, #53389, #40729, #3388 ) ) ;
#11085=DIRECTION ( 'NONE',  ( 0.000000000000000000, 0.7046037717862339012, 0.7096009616570518874 ) ) ;
#11090=DIRECTION ( 'NONE',  ( -1.000000000000000000, 0.000000000000000000, 0.000000000000000000 ) ) ;
#11092=ORIENTED_EDGE ( 'NONE', *, *, #8216, .F. ) ;
#11099=ORIENTED_EDGE ( 'NONE', *, *, #24357, .F. ) ;
#11100=CIRCLE ( 'NONE', #59661, 4.500000000000190958 ) ;
#11104=ORIENTED_EDGE ( 'NONE', *, *, #56578, .F. ) ;
#11105=DIRECTION ( 'NONE',  ( 0.000000000000000000, -0.7096009616570518874, -0.7046037717862339012 ) ) ;
#11107=CARTESIAN_POINT ( 'NONE',  ( -25.50000000000000355, -15.50000000000000000, 22.50000000000000000 ) ) ;
#11109=DIRECTION ( 'NONE',  ( 0.000000000000000000, -0.1111111111108840643, -0.9938079899999319178 ) ) ;
#11117=ORIENTED_EDGE ( 'NONE', *, *, #37017, .F. ) ;
#11118=CARTESIAN_POINT ( 'NONE',  ( 30.00000000000000000, -5.200000000000001066, 9.400000000000000355 ) ) ;
#11121=ORIENTED_EDGE ( 'NONE', *, *, #18884, .T. ) ;
#11127=ORIENTED_EDGE ( 'NONE', *, *, #28824, .T. ) ;
#11132=ADVANCED_FACE ( 'NONE', ( #64122 ), #63759, .F. ) ;
#11135=ORIENTED_EDGE ( 'NONE', *, *, #36837, .T. ) ;
#11136=CARTESIAN_POINT ( 'NONE',  ( -13.00000000000000178, -17.50000000000000000, -15.70500000000000007 ) ) ;
#11142=AXIS2_PLACEMENT_3D ( 'NONE', #43020, #62320, #8929 ) ;
#11149=DIRECTION ( 'NONE',  ( -1.000000000000000000, 0.000000000000000000, 0.000000000000000000 ) ) ;
#11156=ORIENTED_EDGE ( 'NONE', *, *, #5292, .F. ) ;
#11160=EDGE_CURVE ( 'NONE', #1121, #18785, #64802, .T. ) ;
#11180=EDGE_CURVE ( 'NONE', #18662, #26875, #20959, .T. ) ;
#11185=CARTESIAN_POINT ( 'NONE',  ( 30.00000000000000000, -12.00000000000000000, 12.20000000000000107 ) ) ;
#11188=ORIENTED_EDGE ( 'NONE', *, *, #28106, .F. ) ;
#11189=EDGE_CURVE ( 'NONE', #10241, #974, #5051, .T. ) ;
#11190=AXIS2_PLACEMENT_3D ( 'NONE', #28716, #23064, #54572 ) ;
#11213=CARTESIAN_POINT ( 'NONE',  ( -11.00000000000000000, -16.28999999999710369, -15.00000000000794920 ) ) ;
#11224=VERTEX_POINT ( 'NONE', #17048 ) ;
#11232=CARTESIAN_POINT ( 'NONE',  ( 30.00000000000000000, -16.64230188589299786, 14.64519951917100116 ) ) ;
#11241=ORIENTED_EDGE ( 'NONE', *, *, #30216, .T. ) ;
#11249=CARTESIAN_POINT ( 'NONE',  ( 24.00000000000000000, -17.35230188589299871, -15.35019951917099945 ) ) ;
#11255=ORIENTED_EDGE ( 'NONE', *, *, #53137, .F. ) ;
#11258=DIRECTION ( 'NONE',  ( 0.000000000000000000, 0.7096009616570518874, -0.7046037717862339012 ) ) ;
#11263=EDGE_CURVE ( 'NONE', #45628, #5787, #22010, .T. ) ;
#11269=AXIS2_PLACEMENT_3D ( 'NONE', #28854, #55742, #1997 ) ;
#11277=ORIENTED_EDGE ( 'NONE', *, *, #19813, .F. ) ;
#11303=CARTESIAN_POINT ( 'NONE',  ( 25.50000000000000355, -15.12100000000000044, -20.87900000000000134 ) ) ;
#11304=ORIENTED_EDGE ( 'NONE', *, *, #38372, .T. ) ;
#11308=AXIS2_PLACEMENT_3D ( 'NONE', #26019, #30961, #68796 ) ;
#11317=AXIS2_PLACEMENT_3D ( 'NONE', #68181, #25403, #8067 ) ;
#11322=ORIENTED_EDGE ( 'NONE', *, *, #66270, .F. ) ;
#11323=DIRECTION ( 'NONE',  ( 0.000000000000000000, 1.000000000000000000, 0.000000000000000000 ) ) ;
#11324=LINE ( 'NONE', #27593, #240 ) ;
#11326=FACE_OUTER_BOUND ( 'NONE', #34838, .T. ) ;
#11329=CARTESIAN_POINT ( 'NONE',  ( 29.50000000000000355, -12.00000000000000000, -11.00000000000000000 ) ) ;
#11334=ORIENTED_EDGE ( 'NONE', *, *, #30391, .T. ) ;
#11336=DIRECTION ( 'NONE',  ( -1.000000000000000000, 0.000000000000000000, 0.000000000000000000 ) ) ;
#11337=ORIENTED_EDGE ( 'NONE', *, *, #7285, .T. ) ;
#11355=AXIS2_PLACEMENT_3D ( 'NONE', #25945, #64813, #47496 ) ;
#11358=VERTEX_POINT ( 'NONE', #24368 ) ;
#11365=VECTOR ( 'NONE', #28770, 1000.000000000000000 ) ;
#11369=VERTEX_POINT ( 'NONE', #18344 ) ;
#11370=DIRECTION ( 'NONE',  ( -1.000000000000000000, 0.000000000000000000, 0.000000000000000000 ) ) ;
#11371=ORIENTED_EDGE ( 'NONE', *, *, #29051, .F. ) ;
#11374=CARTESIAN_POINT ( 'NONE',  ( -29.50000000000000355, -11.50000000000000000, 15.00000000000000000 ) ) ;
#11387=VECTOR ( 'NONE', #31069, 1000.000000000000000 ) ;
#11391=ORIENTED_EDGE ( 'NONE', *, *, #50117, .F. ) ;
#11403=ORIENTED_EDGE ( 'NONE', *, *, #3659, .F. ) ;
#11405=LINE ( 'NONE', #69418, #15346 ) ;
#11406=VERTEX_POINT ( 'NONE', #56197 ) ;
#11408=DIRECTION ( 'NONE',  ( 1.000000000000000000, -0.000000000000000000, -0.000000000000000000 ) ) ;
#11417=DIRECTION ( 'NONE',  ( 0.000000000000000000, 1.000000000000000000, 0.000000000000000000 ) ) ;
#11426=CARTESIAN_POINT ( 'NONE',  ( 30.00000000000000000, -12.00000000000000000, 10.52786404500095863 ) ) ;
#11432=AXIS2_PLACEMENT_3D ( 'NONE', #65084, #38882, #50184 ) ;
#11437=ORIENTED_EDGE ( 'NONE', *, *, #51689, .F. ) ;
#11447=ORIENTED_EDGE ( 'NONE', *, *, #5398, .F. ) ;
#11448=DIRECTION ( 'NONE',  ( 0.000000000000000000, -1.000000000000000000, 0.000000000000000000 ) ) ;
#11451=EDGE_CURVE ( 'NONE', #37646, #4599, #28656, .T. ) ;
#11453=CARTESIAN_POINT ( 'NONE',  ( 30.00000000000000000, -5.599999999999379696, 26.60000000000059828 ) ) ;
#11454=DIRECTION ( 'NONE',  ( 0.000000000000000000, -0.1111111111108836896, 0.9938079899999319178 ) ) ;
#11461=ORIENTED_EDGE ( 'NONE', *, *, #16189, .T. ) ;
#11467=ORIENTED_EDGE ( 'NONE', *, *, #61910, .F. ) ;
#11471=VERTEX_POINT ( 'NONE', #67517 ) ;
#11473=ORIENTED_EDGE ( 'NONE', *, *, #46118, .F. ) ;
#11484=CIRCLE ( 'NONE', #4702, 3.299999999999473577 ) ;
#11488=EDGE_LOOP ( 'NONE', ( #8394, #48614, #13642, #15218 ) ) ;
#11489=DIRECTION ( 'NONE',  ( -1.000000000000000000, 0.000000000000000000, 0.000000000000000000 ) ) ;
#11498=APPLICATION_CONTEXT ( 'automotive_design' ) ;
#11499=FACE_BOUND ( 'NONE', #60596, .T. ) ;
#11500=DIRECTION ( 'NONE',  ( 0.000000000000000000, 0.000000000000000000, 1.000000000000000000 ) ) ;
#11504=ADVANCED_FACE ( 'NONE', ( #40279 ), #13404, .F. ) ;
#11508=LINE ( 'NONE', #7602, #37623 ) ;
#11509=DIRECTION ( 'NONE',  ( 0.000000000000000000, 0.000000000000000000, 1.000000000000000000 ) ) ;
#11514=AXIS2_PLACEMENT_3D ( 'NONE', #28547, #33856, #55440 ) ;
#11519=DIRECTION ( 'NONE',  ( 0.000000000000000000, -1.000000000000000000, 0.000000000000000000 ) ) ;
#11521=VERTEX_POINT ( 'NONE', #43689 ) ;
#11524=LINE ( 'NONE', #32759, #38354 ) ;
#11527=AXIS2_PLACEMENT_3D ( 'NONE', #38611, #48881, #10689 ) ;
#11531=DIRECTION ( 'NONE',  ( 0.000000000000000000, 0.000000000000000000, 1.000000000000000000 ) ) ;
#11532=ORIENTED_EDGE ( 'NONE', *, *, #17109, .F. ) ;
#11536=CYLINDRICAL_SURFACE ( 'NONE', #25239, 0.3499999999999302558 ) ;
#11544=VECTOR ( 'NONE', #13335, 1000.000000000000000 ) ;
#11551=CARTESIAN_POINT ( 'NONE',  ( 30.00000000000000000, -14.04000000000000092, -14.80000000000000071 ) ) ;
#11557=EDGE_LOOP ( 'NONE', ( #3135, #58653, #31590, #26165 ) ) ;
#11559=CARTESIAN_POINT ( 'NONE',  ( 30.00000000000000000, -9.454754784057099570, -17.53999999999999915 ) ) ;
#11563=CYLINDRICAL_SURFACE ( 'NONE', #40131, 0.2999999999998732569 ) ;
#11564=DIRECTION ( 'NONE',  ( 0.000000000000000000, -1.000000000000000000, 0.000000000000000000 ) ) ;
#11567=ORIENTED_EDGE ( 'NONE', *, *, #9777, .F. ) ;
#11571=PLANE ( 'NONE',  #5891 ) ;
#11579=CARTESIAN_POINT ( 'NONE',  ( 30.00000000000000000, -14.33999999999999986, 14.50000000000000000 ) ) ;
#11581=EDGE_CURVE ( 'NONE', #22725, #30962, #49349, .T. ) ;
#11595=VERTEX_POINT ( 'NONE', #36732 ) ;
#11598=CYLINDRICAL_SURFACE ( 'NONE', #2741, 2.250000000000001776 ) ;
#11600=AXIS2_PLACEMENT_3D ( 'NONE', #69263, #42382, #15536 ) ;
#11607=CARTESIAN_POINT ( 'NONE',  ( -29.50000000000000355, -11.50000000000000000, 11.00000000000000000 ) ) ;
#11608=VERTEX_POINT ( 'NONE', #7222 ) ;
#11621=DIRECTION ( 'NONE',  ( 0.000000000000000000, 0.000000000000000000, 1.000000000000000000 ) ) ;
#11624=CARTESIAN_POINT ( 'NONE',  ( -13.00000000000000178, -17.35230188589299871, -15.35019951917099945 ) ) ;
#11631=ORIENTED_EDGE ( 'NONE', *, *, #22615, .F. ) ;
#11632=EDGE_CURVE ( 'NONE', #17972, #18063, #28792, .T. ) ;
#11640=VECTOR ( 'NONE', #47279, 1000.000000000000000 ) ;
#11643=EDGE_CURVE ( 'NONE', #16876, #9687, #29149, .T. ) ;
#11647=FACE_OUTER_BOUND ( 'NONE', #58848, .T. ) ;
#11653=DIRECTION ( 'NONE',  ( -1.000000000000000000, 0.000000000000000000, 0.000000000000000000 ) ) ;
#11663=CARTESIAN_POINT ( 'NONE',  ( -16.75000000000000000, -2.500000000000000000, 21.77831216351300014 ) ) ;
#11673=CARTESIAN_POINT ( 'NONE',  ( -15.50000000000000000, -1.037157890325000054, -26.00000000000000000 ) ) ;
#11681=CARTESIAN_POINT ( 'NONE',  ( 14.25000000000000000, -2.500000000000000000, -23.22168783648699986 ) ) ;
#11686=CARTESIAN_POINT ( 'NONE',  ( 29.50000000000000355, -11.50000000000100009, -15.00000000000084910 ) ) ;
#11691=VERTEX_POINT ( 'NONE', #62019 ) ;
#11692=DIRECTION ( 'NONE',  ( 0.000000000000000000, -0.1111111111108840643, -0.9938079899999319178 ) ) ;
#11696=DIRECTION ( 'NONE',  ( 1.000000000000000000, -0.000000000000000000, -0.000000000000000000 ) ) ;
#11697=DIRECTION ( 'NONE',  ( 1.000000000000000000, -0.000000000000000000, -0.000000000000000000 ) ) ;
#11698=CIRCLE ( 'NONE', #48977, 0.3499999999999597877 ) ;
#11703=DIRECTION ( 'NONE',  ( -0.4999999999999832356, 0.000000000000000000, -0.8660254037844483666 ) ) ;
#11704=VERTEX_POINT ( 'NONE', #44355 ) ;
#11725=ORIENTED_EDGE ( 'NONE', *, *, #18201, .T. ) ;
#11745=ORIENTED_EDGE ( 'NONE', *, *, #5321, .F. ) ;
#11748=CARTESIAN_POINT ( 'NONE',  ( -11.00000000000000000, -11.85423089348099879, 9.852125413066602277 ) ) ;
#11766=ORIENTED_EDGE ( 'NONE', *, *, #1277, .F. ) ;
#11768=CARTESIAN_POINT ( 'NONE',  ( 23.75054448485400016, -15.50000000000000000, 25.53140320652400064 ) ) ;
#11780=DIRECTION ( 'NONE',  ( 0.000000000000000000, -0.7071067811865474617, 0.7071067811865474617 ) ) ;
#11787=ORIENTED_EDGE ( 'NONE', *, *, #51834, .F. ) ;
#11788=AXIS2_PLACEMENT_3D ( 'NONE', #46556, #68498, #14034 ) ;
#11789=AXIS2_PLACEMENT_3D ( 'NONE', #13115, #18069, #55565 ) ;
#11802=CARTESIAN_POINT ( 'NONE',  ( 30.00000000000000000, -11.50000000000082068, -10.20500000000000007 ) ) ;
#11804=DIRECTION ( 'NONE',  ( 0.000000000000000000, 1.000000000000000000, 0.000000000000000000 ) ) ;
#11819=ADVANCED_FACE ( 'NONE', ( #41154 ), #63082, .F. ) ;
#11826=VECTOR ( 'NONE', #54088, 1000.000000000000000 ) ;
#11828=AXIS2_PLACEMENT_3D ( 'NONE', #64939, #26765, #48329 ) ;
#11830=LINE ( 'NONE', #60962, #10848 ) ;
#11831=DIRECTION ( 'NONE',  ( 0.000000000000000000, 1.000000000000000000, 0.000000000000000000 ) ) ;
#11837=DIRECTION ( 'NONE',  ( 1.000000000000000000, -0.000000000000000000, -0.000000000000000000 ) ) ;
#11840=VECTOR ( 'NONE', #27898, 1000.000000000000000 ) ;
#11846=CYLINDRICAL_SURFACE ( 'NONE', #5713, 0.3500000000002719824 ) ;
#11847=DIRECTION ( 'NONE',  ( 0.000000000000000000, -1.000000000000000000, 0.000000000000000000 ) ) ;
#11848=FACE_OUTER_BOUND ( 'NONE', #57987, .T. ) ;
#11855=VECTOR ( 'NONE', #24106, 1000.000000000000000 ) ;
#11857=EDGE_CURVE ( 'NONE', #41912, #58770, #37967, .T. ) ;
#11864=ADVANCED_FACE ( 'NONE', ( #64837 ), #32310, .F. ) ;
#11887=ORIENTED_EDGE ( 'NONE', *, *, #25616, .T. ) ;
#11890=CIRCLE ( 'NONE', #54820, 0.2999999999998732569 ) ;
#11894=VECTOR ( 'NONE', #2688, 1000.000000000000000 ) ;
#11904=VERTEX_POINT ( 'NONE', #10731 ) ;
#11910=EDGE_CURVE ( 'NONE', #28718, #69443, #20994, .T. ) ;
#11911=DIRECTION ( 'NONE',  ( 0.000000000000000000, -1.000000000000000000, 0.000000000000000000 ) ) ;
#11914=DIRECTION ( 'NONE',  ( 0.000000000000000000, 0.000000000000000000, -1.000000000000000000 ) ) ;
#11915=ORIENTED_EDGE ( 'NONE', *, *, #58013, .T. ) ;
#11919=AXIS2_PLACEMENT_3D ( 'NONE', #20411, #3800, #52602 ) ;
#11920=CARTESIAN_POINT ( 'NONE',  ( 15.50000000000000000, -15.50000000000000000, -25.99999999999985079 ) ) ;
#11922=CIRCLE ( 'NONE', #28830, 4.500000000000190958 ) ;
#11924=VERTEX_POINT ( 'NONE', #6128 ) ;
#11935=CARTESIAN_POINT ( 'NONE',  ( -14.10805890929250062, -5.000000000000000000, -26.25000000000000000 ) ) ;
#11952=ADVANCED_FACE ( 'NONE', ( #16387 ), #42566, .F. ) ;
#11957=ORIENTED_EDGE ( 'NONE', *, *, #51736, .T. ) ;
#11960=ORIENTED_EDGE ( 'NONE', *, *, #27842, .T. ) ;
#11968=CARTESIAN_POINT ( 'NONE',  ( 30.00000000000000000, -17.14999999999900027, 26.64999999999900027 ) ) ;
#11977=AXIS2_PLACEMENT_3D ( 'NONE', #53094, #69701, #69335 ) ;
#11981=AXIS2_PLACEMENT_3D ( 'NONE', #50177, #13391, #33907 ) ;
#11983=EDGE_CURVE ( 'NONE', #18841, #58583, #38857, .T. ) ;
#11996=LINE ( 'NONE', #33236, #47480 ) ;
#11997=ORIENTED_EDGE ( 'NONE', *, *, #65563, .F. ) ;
#12000=CARTESIAN_POINT ( 'NONE',  ( 11.00000000000000000, -16.28999999999999915, 14.50000000000000000 ) ) ;
#12011=DIRECTION ( 'NONE',  ( -1.000000000000000000, 0.000000000000000000, 0.000000000000000000 ) ) ;
#12012=VERTEX_POINT ( 'NONE', #21351 ) ;
#12017=DIRECTION ( 'NONE',  ( 0.000000000000000000, 0.000000000000000000, -1.000000000000000000 ) ) ;
#12019=DIRECTION ( 'NONE',  ( 0.000000000000000000, 0.000000000000000000, 1.000000000000000000 ) ) ;
#12020=CIRCLE ( 'NONE', #51567, 4.500000000000190958 ) ;
#12030=CARTESIAN_POINT ( 'NONE',  ( -28.00000000000000000, -15.50000000000000000, -20.05051025721700242 ) ) ;
#12040=EDGE_CURVE ( 'NONE', #60221, #26009, #12442, .T. ) ;
#12046=EDGE_CURVE ( 'NONE', #51332, #67088, #66212, .T. ) ;
#12048=CARTESIAN_POINT ( 'NONE',  ( 30.00000000000000000, -16.64230188589299786, 14.64519951917100116 ) ) ;
#12066=ORIENTED_EDGE ( 'NONE', *, *, #48311, .T. ) ;
#12067=CARTESIAN_POINT ( 'NONE',  ( -17.00000000000000000, -15.50000000000000000, -19.33772233983200195 ) ) ;
#12072=ADVANCED_FACE ( 'NONE', ( #12112 ), #60202, .T. ) ;
#12075=ADVANCED_FACE ( 'NONE', ( #65857 ), #1857, .T. ) ;
#12076=DIRECTION ( 'NONE',  ( 0.000000000000000000, -1.000000000000000000, 0.000000000000000000 ) ) ;
#12080=VERTEX_POINT ( 'NONE', #23428 ) ;
#12083=ORIENTED_EDGE ( 'NONE', *, *, #27905, .T. ) ;
#12092=CIRCLE ( 'NONE', #13250, 1.620999999999997332 ) ;
#12102=AXIS2_PLACEMENT_3D ( 'NONE', #59044, #10953, #21561 ) ;
#12111=VECTOR ( 'NONE', #63616, 1000.000000000000000 ) ;
#12112=FACE_OUTER_BOUND ( 'NONE', #65033, .T. ) ;
#12118=ORIENTED_EDGE ( 'NONE', *, *, #49654, .T. ) ;
#12127=CARTESIAN_POINT ( 'NONE',  ( 30.00000000000000000, -5.599999999999379696, -26.60000000000059828 ) ) ;
#12130=DIRECTION ( 'NONE',  ( -1.000000000000000000, 0.000000000000000000, 0.000000000000000000 ) ) ;
#12142=CIRCLE ( 'NONE', #881, 4.000000000000000888 ) ;
#12143=CARTESIAN_POINT ( 'NONE',  ( -30.00000000000000000, -11.50000000000100009, -10.50000000000065903 ) ) ;
#12144=DIRECTION ( 'NONE',  ( 0.000000000000000000, 0.7096009616570518874, -0.7046037717862339012 ) ) ;
#12150=FACE_BOUND ( 'NONE', #31765, .T. ) ;
#12152=EDGE_LOOP ( 'NONE', ( #23088, #28369, #50666, #678 ) ) ;
#12154=ADVANCED_FACE ( 'NONE', ( #41071 ), #3250, .T. ) ;
#12158=CARTESIAN_POINT ( 'NONE',  ( 14.10805890929250062, -5.000000000000000000, 26.25000000000000000 ) ) ;
#12171=ADVANCED_FACE ( 'NONE', ( #63357 ), #56642, .F. ) ;
#12179=ADVANCED_FACE ( 'NONE', ( #19855 ), #14205, .T. ) ;
#12182=FACE_OUTER_BOUND ( 'NONE', #66102, .T. ) ;
#12189=ORIENTED_EDGE ( 'NONE', *, *, #1324, .T. ) ;
#12198=CARTESIAN_POINT ( 'NONE',  ( 30.00000000000000000, -13.79999999999979998, -17.30000000000000071 ) ) ;
#12200=ADVANCED_FACE ( 'NONE', ( #35771 ), #46378, .F. ) ;
#12207=ORIENTED_EDGE ( 'NONE', *, *, #35160, .F. ) ;
#12208=CARTESIAN_POINT ( 'NONE',  ( 11.00000000000000000, -8.959999999999999076, 12.95475478405700009 ) ) ;
#12225=EDGE_LOOP ( 'NONE', ( #36366, #37241 ) ) ;
#12227=CARTESIAN_POINT ( 'NONE',  ( 15.50000000000000000, -0.2038245569916604938, 23.94337567297399971 ) ) ;
#12234=CARTESIAN_POINT ( 'NONE',  ( -23.48000000000000043, -15.50000000000000000, -26.00000000000000355 ) ) ;
#12235=AXIS2_PLACEMENT_3D ( 'NONE', #14996, #68034, #19591 ) ;
#12239=ORIENTED_EDGE ( 'NONE', *, *, #16137, .F. ) ;
#12275=DIRECTION ( 'NONE',  ( 0.000000000000000000, 1.000000000000000000, 0.000000000000000000 ) ) ;
#12276=VERTEX_POINT ( 'NONE', #29759 ) ;
#12290=CARTESIAN_POINT ( 'NONE',  ( -30.00000000000000000, -9.487228132326899654, -12.50000000000000000 ) ) ;
#12292=ADVANCED_FACE ( 'NONE', ( #54145 ), #5709, .F. ) ;
#12293=DIRECTION ( 'NONE',  ( -1.000000000000000000, 0.000000000000000000, 0.000000000000000000 ) ) ;
#12295=ORIENTED_EDGE ( 'NONE', *, *, #35160, .T. ) ;
#12299=CARTESIAN_POINT ( 'NONE',  ( 30.00000000000000000, -5.599999999999999645, -9.000000000000001776 ) ) ;
#12302=DIRECTION ( 'NONE',  ( -1.000000000000000000, 0.000000000000000000, 0.000000000000000000 ) ) ;
#12305=EDGE_LOOP ( 'NONE', ( #7871, #31292, #48530, #8076 ) ) ;
#12306=DIRECTION ( 'NONE',  ( 1.000000000000000000, -0.000000000000000000, -0.000000000000000000 ) ) ;
#12311=CARTESIAN_POINT ( 'NONE',  ( 30.00000000000000000, -16.64230188589299786, -14.64519951917100116 ) ) ;
#12320=AXIS2_PLACEMENT_3D ( 'NONE', #19692, #25021, #15114 ) ;
#12329=ORIENTED_EDGE ( 'NONE', *, *, #52465, .F. ) ;
#12333=CARTESIAN_POINT ( 'NONE',  ( 15.50000000000000000, -15.50000000000000000, -25.99999999999985079 ) ) ;
#12337=CARTESIAN_POINT ( 'NONE',  ( -11.00000000000000000, -15.97213595500069871, 14.50000000000000000 ) ) ;
#12344=ADVANCED_FACE ( 'NONE', ( #58752 ), #53450, .F. ) ;
#12347=CARTESIAN_POINT ( 'NONE',  ( 15.50000000000000000, -0.4000000000000000222, -22.50000000000000000 ) ) ;
#12353=CYLINDRICAL_SURFACE ( 'NONE', #37884, 4.500000000000188294 ) ;
#12354=DIRECTION ( 'NONE',  ( 0.000000000000000000, 1.000000000000000000, 0.000000000000000000 ) ) ;
#12368=EDGE_CURVE ( 'NONE', #39654, #57686, #18600, .T. ) ;
#12372=ADVANCED_FACE ( 'NONE', ( #42122 ), #43169, .F. ) ;
#12377=AXIS2_PLACEMENT_3D ( 'NONE', #43082, #69959, #47696 ) ;
#12378=DIRECTION ( 'NONE',  ( 0.000000000000000000, 0.000000000000000000, 1.000000000000000000 ) ) ;
#12379=FACE_OUTER_BOUND ( 'NONE', #1875, .T. ) ;
#12399=PLANE ( 'NONE',  #14031 ) ;
#12401=VERTEX_POINT ( 'NONE', #15267 ) ;
#12402=CARTESIAN_POINT ( 'NONE',  ( 25.50000000000000355, 0.000000000000000000, 22.50000000000000000 ) ) ;
#12409=CARTESIAN_POINT ( 'NONE',  ( -15.50000000000000000, -2.500000000000000000, -23.94337567297399971 ) ) ;
#12413=CARTESIAN_POINT ( 'NONE',  ( 30.00000000000000000, -17.14999999999900027, -26.64999999999900027 ) ) ;
#12416=VERTEX_POINT ( 'NONE', #47781 ) ;
#12419=CARTESIAN_POINT ( 'NONE',  ( -30.00000000000000000, -8.959999999999999076, 12.95475478405700009 ) ) ;
#12423=AXIS2_PLACEMENT_3D ( 'NONE', #33096, #6228, #23173 ) ;
#12429=CARTESIAN_POINT ( 'NONE',  ( 29.50000000000000355, -11.50000000000000000, 15.00000000000000000 ) ) ;
#12442=LINE ( 'NONE', #6481, #46780 ) ;
#12448=DIRECTION ( 'NONE',  ( 1.000000000000000000, 0.000000000000000000, 0.000000000000000000 ) ) ;
#12456=ORIENTED_EDGE ( 'NONE', *, *, #16860, .F. ) ;
#12464=LINE ( 'NONE', #7159, #50806 ) ;
#12468=DIRECTION ( 'NONE',  ( 1.000000000000000000, -0.000000000000000000, -0.000000000000000000 ) ) ;
#12469=FACE_BOUND ( 'NONE', #49304, .T. ) ;
#12471=FACE_BOUND ( 'NONE', #35644, .T. ) ;
#12479=ORIENTED_EDGE ( 'NONE', *, *, #56136, .F. ) ;
#12486=ORIENTED_EDGE ( 'NONE', *, *, #69077, .T. ) ;
#12490=VERTEX_POINT ( 'NONE', #750 ) ;
#12492=VECTOR ( 'NONE', #11519, 1000.000000000000000 ) ;
#12508=EDGE_CURVE ( 'NONE', #57228, #58960, #66044, .T. ) ;
#12511=CYLINDRICAL_SURFACE ( 'NONE', #36805, 4.000000000000000000 ) ;
#12512=ORIENTED_EDGE ( 'NONE', *, *, #67100, .T. ) ;
#12516=VECTOR ( 'NONE', #44093, 1000.000000000000000 ) ;
#12518=EDGE_CURVE ( 'NONE', #12650, #52657, #33931, .T. ) ;
#12527=ORIENTED_EDGE ( 'NONE', *, *, #17412, .F. ) ;
#12536=CARTESIAN_POINT ( 'NONE',  ( -30.00000000000000000, -15.46862696659690073, 14.50000000000000000 ) ) ;
#12540=ORIENTED_EDGE ( 'NONE', *, *, #41030, .T. ) ;
#12543=DIRECTION ( 'NONE',  ( 0.000000000000000000, 0.000000000000000000, -1.000000000000000000 ) ) ;
#12545=CYLINDRICAL_SURFACE ( 'NONE', #40570, 0.5000000000079367624 ) ;
#12557=EDGE_CURVE ( 'NONE', #51508, #2931, #3172, .T. ) ;
#12560=EDGE_CURVE ( 'NONE', #35777, #2319, #69446, .T. ) ;
#12561=DIRECTION ( 'NONE',  ( 1.000000000000000000, -0.000000000000000000, -0.000000000000000000 ) ) ;
#12562=VECTOR ( 'NONE', #51846, 1000.000000000000000 ) ;
#12565=DIRECTION ( 'NONE',  ( 0.000000000000000000, 0.000000000000000000, 1.000000000000000000 ) ) ;
#12575=ORIENTED_EDGE ( 'NONE', *, *, #55889, .T. ) ;
#12586=VERTEX_POINT ( 'NONE', #40984 ) ;
#12588=ADVANCED_FACE ( 'NONE', ( #8451 ), #35677, .F. ) ;
#12595=ADVANCED_FACE ( 'NONE', ( #24735 ), #35315, .T. ) ;
#12602=EDGE_CURVE ( 'NONE', #21845, #28990, #68216, .T. ) ;
#12603=LINE ( 'NONE', #55421, #52582 ) ;
#12609=FACE_OUTER_BOUND ( 'NONE', #21156, .T. ) ;
#12614=DIRECTION ( 'NONE',  ( 1.000000000000000000, -0.000000000000000000, -0.000000000000000000 ) ) ;
#12624=DIRECTION ( 'NONE',  ( 0.000000000000000000, 0.000000000000000000, 1.000000000000000000 ) ) ;
#12630=LINE ( 'NONE', #33863, #9533 ) ;
#12633=VECTOR ( 'NONE', #24328, 1000.000000000000000 ) ;
#12643=CIRCLE ( 'NONE', #30745, 4.000000000000001776 ) ;
#12648=ORIENTED_EDGE ( 'NONE', *, *, #11263, .F. ) ;
#12650=VERTEX_POINT ( 'NONE', #57605 ) ;
#12651=ORIENTED_EDGE ( 'NONE', *, *, #10473, .F. ) ;
#12661=ORIENTED_EDGE ( 'NONE', *, *, #7164, .F. ) ;
#12672=ORIENTED_EDGE ( 'NONE', *, *, #1324, .F. ) ;
#12673=CIRCLE ( 'NONE', #11527, 3.499999999999855227 ) ;
#12678=CARTESIAN_POINT ( 'NONE',  ( 11.50000000000000000, -11.50000000000100009, -15.00000000000084910 ) ) ;
#12680=EDGE_CURVE ( 'NONE', #50148, #61414, #24383, .T. ) ;
#12687=CARTESIAN_POINT ( 'NONE',  ( 14.25000000000000000, -0.2038245569916330158, -23.22168783648699986 ) ) ;
#12698=VECTOR ( 'NONE', #7055, 1000.000000000000000 ) ;
#12703=DIRECTION ( 'NONE',  ( 1.000000000000000000, 0.000000000000000000, 0.000000000000000000 ) ) ;
#12707=VECTOR ( 'NONE', #19136, 1000.000000000000000 ) ;
#12710=DIRECTION ( 'NONE',  ( 0.000000000000000000, 0.6857142857142869419, -0.7278708115918273158 ) ) ;
#12713=ORIENTED_EDGE ( 'NONE', *, *, #3751, .T. ) ;
#12715=DIRECTION ( 'NONE',  ( 1.000000000000000000, 0.000000000000000000, 0.000000000000000000 ) ) ;
#12716=DIRECTION ( 'NONE',  ( 0.000000000000000000, 1.000000000000000000, 0.000000000000000000 ) ) ;
#12719=DIRECTION ( 'NONE',  ( 0.000000000000000000, 0.000000000000000000, 1.000000000000000000 ) ) ;
#12727=DIRECTION ( 'NONE',  ( 0.000000000000000000, -0.7071067811865454633, -0.7071067811865496822 ) ) ;
#12740=CIRCLE ( 'NONE', #39841, 3.499999999999054534 ) ;
#12742=CARTESIAN_POINT ( 'NONE',  ( 16.89194109070750116, -5.000000000000000000, -26.25000000000000000 ) ) ;
#12759=CARTESIAN_POINT ( 'NONE',  ( 30.00000000000000000, -17.50000000000000000, 15.70500000000000007 ) ) ;
#12769=CARTESIAN_POINT ( 'NONE',  ( -25.50000000000000355, -15.50000000000000000, -20.49999999999999645 ) ) ;
#12770=EDGE_CURVE ( 'NONE', #54447, #55741, #32251, .T. ) ;
#12777=LINE ( 'NONE', #65850, #26141 ) ;
#12788=ORIENTED_EDGE ( 'NONE', *, *, #19735, .T. ) ;
#12814=CARTESIAN_POINT ( 'NONE',  ( -15.50000000000000000, -17.50000000000000000, -22.50000000000000000 ) ) ;
#12815=DIRECTION ( 'NONE',  ( 0.000000000000000000, 0.000000000000000000, 1.000000000000000000 ) ) ;
#12821=CARTESIAN_POINT ( 'NONE',  ( 11.00000000000000000, -9.487228132326899654, -12.50000000000000000 ) ) ;
#12824=PLANE ( 'NONE',  #14998 ) ;
#12827=FACE_OUTER_BOUND ( 'NONE', #23887, .T. ) ;
#12828=EDGE_LOOP ( 'NONE', ( #23707, #54320, #50330, #26174 ) ) ;
#12831=EDGE_CURVE ( 'NONE', #55252, #56315, #63625, .T. ) ;
#12841=VERTEX_POINT ( 'NONE', #10563 ) ;
#12842=DIRECTION ( 'NONE',  ( -1.000000000000000000, 0.000000000000000000, 0.000000000000000000 ) ) ;
#12847=ADVANCED_FACE ( 'NONE', ( #48399 ), #69963, .F. ) ;
#12848=ORIENTED_EDGE ( 'NONE', *, *, #40177, .T. ) ;
#12856=ADVANCED_FACE ( 'NONE', ( #20476 ), #36747, .F. ) ;
#12860=CIRCLE ( 'NONE', #37730, 4.500000000000191847 ) ;
#12863=FACE_OUTER_BOUND ( 'NONE', #49697, .T. ) ;
#12864=CARTESIAN_POINT ( 'NONE',  ( 25.50000000000000355, -5.578999999999999737, 22.50000000000000000 ) ) ;
#12870=CARTESIAN_POINT ( 'NONE',  ( -25.50000000000000355, -15.50000000000000000, -22.50000000000000000 ) ) ;
#12877=AXIS2_PLACEMENT_3D ( 'NONE', #47012, #62928, #19776 ) ;
#12880=DIRECTION ( 'NONE',  ( -1.000000000000000000, 0.000000000000000000, 0.000000000000000000 ) ) ;
#12883=CIRCLE ( 'NONE', #37808, 3.499999999999850342 ) ;
#12891=AXIS2_PLACEMENT_3D ( 'NONE', #2139, #45262, #50233 ) ;
#12892=ORIENTED_EDGE ( 'NONE', *, *, #51773, .F. ) ;
#12913=CARTESIAN_POINT ( 'NONE',  ( -14.24999999999999822, -0.2715193793361436736, -22.01281590054916038 ) ) ;
#12924=PLANE ( 'NONE',  #61712 ) ;
#12925=EDGE_CURVE ( 'NONE', #68975, #34031, #27703, .T. ) ;
#12927=ORIENTED_EDGE ( 'NONE', *, *, #61405, .T. ) ;
#12952=LINE ( 'NONE', #29214, #64065 ) ;
#12955=VERTEX_POINT ( 'NONE', #27871 ) ;
#12961=DIRECTION ( 'NONE',  ( 0.000000000000000000, 0.7071067811865450192, 0.7071067811865500152 ) ) ;
#12967=DIRECTION ( 'NONE',  ( 0.000000000000000000, 1.000000000000000000, 0.000000000000000000 ) ) ;
#12969=CARTESIAN_POINT ( 'NONE',  ( -15.50000000000000000, -0.4000000000000000222, -22.50000000000000000 ) ) ;
#12988=DIRECTION ( 'NONE',  ( 0.000000000000000000, -1.000000000000000000, 0.000000000000000000 ) ) ;
#13001=EDGE_CURVE ( 'NONE', #11369, #19166, #23199, .T. ) ;
#13016=EDGE_LOOP ( 'NONE', ( #25897, #45377, #18902, #60180 ) ) ;
#13026=CARTESIAN_POINT ( 'NONE',  ( 23.75054448485400016, -15.50000000000000000, -25.53140320652400064 ) ) ;
#13046=DIRECTION ( 'NONE',  ( 0.000000000000000000, -0.7096009616570518874, -0.7046037717862339012 ) ) ;
#13052=DIRECTION ( 'NONE',  ( 1.000000000000000000, -0.000000000000000000, -0.000000000000000000 ) ) ;
#13055=VERTEX_POINT ( 'NONE', #8014 ) ;
#13057=PLANE ( 'NONE',  #59806 ) ;
#13061=VECTOR ( 'NONE', #6985, 1000.000000000000000 ) ;
#13062=DIRECTION ( 'NONE',  ( 1.000000000000000000, 0.000000000000000000, 0.000000000000000000 ) ) ;
#13063=EDGE_CURVE ( 'NONE', #14787, #55576, #18989, .T. ) ;
#13070=DIRECTION ( 'NONE',  ( -1.000000000000000000, 0.000000000000000000, 0.000000000000000000 ) ) ;
#13072=CARTESIAN_POINT ( 'NONE',  ( 11.50000000000000000, -15.46862696659690073, 14.50000000000000000 ) ) ;
#13075=DIRECTION ( 'NONE',  ( -1.000000000000000000, 0.000000000000000000, 0.000000000000000000 ) ) ;
#13077=DIRECTION ( 'NONE',  ( 0.000000000000000000, 0.000000000000000000, 1.000000000000000000 ) ) ;
#13080=ORIENTED_EDGE ( 'NONE', *, *, #56051, .T. ) ;
#13082=EDGE_CURVE ( 'NONE', #2465, #54584, #61591, .T. ) ;
#13093=DIRECTION ( 'NONE',  ( 0.000000000000000000, 0.000000000000000000, 1.000000000000000000 ) ) ;
#13096=VECTOR ( 'NONE', #16678, 1000.000000000000000 ) ;
#13097=VECTOR ( 'NONE', #65417, 1000.000000000000000 ) ;
#13098=DIRECTION ( 'NONE',  ( -1.000000000000000000, 0.000000000000000000, 0.000000000000000000 ) ) ;
#13102=VERTEX_POINT ( 'NONE', #40899 ) ;
#13106=VECTOR ( 'NONE', #702, 1000.000000000000000 ) ;
#13115=CARTESIAN_POINT ( 'NONE',  ( 30.00000000000000000, -16.28999999999999915, 14.50000000000000000 ) ) ;
#13126=ORIENTED_EDGE ( 'NONE', *, *, #68120, .F. ) ;
#13131=ADVANCED_FACE ( 'NONE', ( #62452, #13331 ), #19673, .T. ) ;
#13136=CARTESIAN_POINT ( 'NONE',  ( -11.00000000000000000, -11.70000000000000284, -12.50000000000000000 ) ) ;
#13140=CARTESIAN_POINT ( 'NONE',  ( 17.24945551514599984, -17.50000000000000000, -25.53140320652400064 ) ) ;
#13148=DIRECTION ( 'NONE',  ( 0.000000000000000000, 0.000000000000000000, 1.000000000000000000 ) ) ;
#13155=DIRECTION ( 'NONE',  ( -1.000000000000000000, 0.000000000000000000, 0.000000000000000000 ) ) ;
#13156=DIRECTION ( 'NONE',  ( 0.000000000000000000, 1.000000000000000000, 0.000000000000000000 ) ) ;
#13158=VECTOR ( 'NONE', #15824, 999.9999999999998863 ) ;
#13168=ORIENTED_EDGE ( 'NONE', *, *, #55805, .T. ) ;
#13171=EDGE_LOOP ( 'NONE', ( #47311, #56926, #2434, #11766 ) ) ;
#13190=EDGE_CURVE ( 'NONE', #52180, #41930, #22109, .T. ) ;
#13202=EDGE_CURVE ( 'NONE', #60150, #59731, #42654, .T. ) ;
#13205=CIRCLE ( 'NONE', #18861, 4.000000000000000888 ) ;
#13207=EDGE_LOOP ( 'NONE', ( #55238, #59916, #52359, #56992, #52413, #29460, #50423 ) ) ;
#13210=DIRECTION ( 'NONE',  ( 0.000000000000000000, 0.000000000000000000, 1.000000000000000000 ) ) ;
#13223=VECTOR ( 'NONE', #61855, 1000.000000000000000 ) ;
#13224=DIRECTION ( 'NONE',  ( 0.000000000000000000, 0.000000000000000000, -1.000000000000000000 ) ) ;
#13228=VERTEX_POINT ( 'NONE', #69871 ) ;
#13237=VECTOR ( 'NONE', #657, 1000.000000000000000 ) ;
#13241=FACE_OUTER_BOUND ( 'NONE', #57104, .T. ) ;
#13250=AXIS2_PLACEMENT_3D ( 'NONE', #38670, #39352, #64854 ) ;
#13259=PLANE ( 'NONE',  #65785 ) ;
#13261=CARTESIAN_POINT ( 'NONE',  ( -30.00000000000000000, -5.000000000000000000, 27.00000000000000000 ) ) ;
#13262=DIRECTION ( 'NONE',  ( 0.000000000000000000, -1.000000000000000000, 0.000000000000000000 ) ) ;
#13264=LINE ( 'NONE', #34821, #57161 ) ;
#13274=ORIENTED_EDGE ( 'NONE', *, *, #43445, .T. ) ;
#13280=ORIENTED_EDGE ( 'NONE', *, *, #11983, .T. ) ;
#13289=EDGE_LOOP ( 'NONE', ( #12788, #52463, #18699, #60669 ) ) ;
#13290=ORIENTED_EDGE ( 'NONE', *, *, #39086, .F. ) ;
#13303=EDGE_CURVE ( 'NONE', #43882, #30792, #38065, .T. ) ;
#13304=AXIS2_PLACEMENT_3D ( 'NONE', #23326, #65765, #44887 ) ;
#13305=ORIENTED_EDGE ( 'NONE', *, *, #7728, .T. ) ;
#13307=AXIS2_PLACEMENT_3D ( 'NONE', #14646, #37275, #47867 ) ;
#13312=FACE_OUTER_BOUND ( 'NONE', #2827, .T. ) ;
#13315=DIRECTION ( 'NONE',  ( 0.000000000000000000, -0.7071067811865454633, -0.7071067811865496822 ) ) ;
#13320=ADVANCED_FACE ( 'NONE', ( #60292 ), #27087, .F. ) ;
#13325=ADVANCED_FACE ( 'NONE', ( #11848 ), #223, .F. ) ;
#13331=FACE_BOUND ( 'NONE', #42166, .T. ) ;
#13335=DIRECTION ( 'NONE',  ( -1.000000000000000000, 0.000000000000000000, 0.000000000000000000 ) ) ;
#13338=ORIENTED_EDGE ( 'NONE', *, *, #38391, .T. ) ;
#13351=EDGE_CURVE ( 'NONE', #37678, #50851, #38731, .T. ) ;
#13353=DIRECTION ( 'NONE',  ( 1.000000000000000000, 0.000000000000000000, 0.000000000000000000 ) ) ;
#13356=LINE ( 'NONE', #29252, #43538 ) ;
#13357=ORIENTED_EDGE ( 'NONE', *, *, #61910, .T. ) ;
#13358=PLANE ( 'NONE',  #63081 ) ;
#13359=EDGE_CURVE ( 'NONE', #48929, #65032, #50033, .T. ) ;
#13360=AXIS2_PLACEMENT_3D ( 'NONE', #51209, #3491, #2773 ) ;
#13367=ORIENTED_EDGE ( 'NONE', *, *, #30540, .F. ) ;
#13376=PLANE ( 'NONE',  #30446 ) ;
#13391=DIRECTION ( 'NONE',  ( -1.000000000000000000, 0.000000000000000000, 0.000000000000000000 ) ) ;
#13394=CARTESIAN_POINT ( 'NONE',  ( -13.00000000000000178, -16.28999999999999915, 14.50000000000000000 ) ) ;
#13404=PLANE ( 'NONE',  #35415 ) ;
#13407=CARTESIAN_POINT ( 'NONE',  ( -24.00000000000000000, -16.64230188589299786, -14.64519951917100116 ) ) ;
#13429=DIRECTION ( 'NONE',  ( -1.000000000000000000, 0.000000000000000000, 0.000000000000000000 ) ) ;
#13441=CARTESIAN_POINT ( 'NONE',  ( -30.00000000000000000, -5.599999999999999645, 9.400000000000000355 ) ) ;
#13443=CARTESIAN_POINT ( 'NONE',  ( 30.00000000000000000, -14.04000000000000092, -14.80000000000000071 ) ) ;
#13445=ORIENTED_EDGE ( 'NONE', *, *, #17855, .F. ) ;
#13447=FACE_OUTER_BOUND ( 'NONE', #31897, .T. ) ;
#13448=EDGE_CURVE ( 'NONE', #32678, #34396, #25182, .T. ) ;
#13451=ADVANCED_FACE ( 'NONE', ( #56384 ), #3616, .F. ) ;
#13464=ORIENTED_EDGE ( 'NONE', *, *, #17572, .T. ) ;
#13468=VECTOR ( 'NONE', #52139, 1000.000000000000114 ) ;
#13469=DIRECTION ( 'NONE',  ( 1.000000000000000000, 0.000000000000000000, 0.000000000000000000 ) ) ;
#13471=ORIENTED_EDGE ( 'NONE', *, *, #34055, .T. ) ;
#13506=LINE ( 'NONE', #35062, #49310 ) ;
#13510=VECTOR ( 'NONE', #68213, 1000.000000000000000 ) ;
#13516=DIRECTION ( 'NONE',  ( 0.000000000000000000, 0.000000000000000000, -1.000000000000000000 ) ) ;
#13523=ORIENTED_EDGE ( 'NONE', *, *, #51413, .F. ) ;
#13525=FACE_BOUND ( 'NONE', #38549, .T. ) ;
#13540=CARTESIAN_POINT ( 'NONE',  ( -25.50000000000000355, -5.578999999999999737, 22.50000000000000000 ) ) ;
#13542=EDGE_CURVE ( 'NONE', #50249, #30827, #4145, .T. ) ;
#13546=ORIENTED_EDGE ( 'NONE', *, *, #7813, .F. ) ;
#13548=ORIENTED_EDGE ( 'NONE', *, *, #18471, .F. ) ;
#13549=ORIENTED_EDGE ( 'NONE', *, *, #32518, .T. ) ;
#13552=DIRECTION ( 'NONE',  ( 0.000000000000000000, 1.000000000000000000, 0.000000000000000000 ) ) ;
#13555=CARTESIAN_POINT ( 'NONE',  ( -16.54686605390243059, -0.2715358723599923807, 23.33896727494797929 ) ) ;
#13556=AXIS2_PLACEMENT_3D ( 'NONE', #32500, #37114, #21196 ) ;
#13557=VERTEX_POINT ( 'NONE', #26582 ) ;
#13561=DIRECTION ( 'NONE',  ( 0.000000000000000000, 1.000000000000000000, 0.000000000000000000 ) ) ;
#13562=ORIENTED_EDGE ( 'NONE', *, *, #41204, .T. ) ;
#13564=LINE ( 'NONE', #35119, #34434 ) ;
#13567=ORIENTED_EDGE ( 'NONE', *, *, #57462, .F. ) ;
#13570=CARTESIAN_POINT ( 'NONE',  ( 25.49999999999869971, -15.50000000000000000, 22.50000000000000000 ) ) ;
#13579=ORIENTED_EDGE ( 'NONE', *, *, #33756, .T. ) ;
#13594=DIRECTION ( 'NONE',  ( -1.000000000000000000, 0.000000000000000000, 0.000000000000000000 ) ) ;
#13600=DIRECTION ( 'NONE',  ( 0.000000000000000000, 0.000000000000000000, -1.000000000000000000 ) ) ;
#13602=VECTOR ( 'NONE', #56743, 1000.000000000000000 ) ;
#13605=CARTESIAN_POINT ( 'NONE',  ( 30.00000000000000000, -17.50000000000000000, -15.70500000000000007 ) ) ;
#13609=DIRECTION ( 'NONE',  ( 0.000000000000000000, -1.000000000000000000, 0.000000000000000000 ) ) ;
#13610=ORIENTED_EDGE ( 'NONE', *, *, #38044, .T. ) ;
#13613=LINE ( 'NONE', #56052, #18697 ) ;
#13615=PLANE ( 'NONE',  #63671 ) ;
#13619=ORIENTED_EDGE ( 'NONE', *, *, #15687, .F. ) ;
#13623=EDGE_CURVE ( 'NONE', #29287, #8225, #59452, .T. ) ;
#13642=ORIENTED_EDGE ( 'NONE', *, *, #17923, .T. ) ;
#13643=EDGE_CURVE ( 'NONE', #34775, #54337, #5382, .T. ) ;
#13659=DIRECTION ( 'NONE',  ( 0.000000000000000000, -1.000000000000000000, 0.000000000000000000 ) ) ;
#13666=EDGE_CURVE ( 'NONE', #8802, #47752, #31893, .T. ) ;
#13667=DIRECTION ( 'NONE',  ( 0.000000000000000000, 0.000000000000000000, 1.000000000000000000 ) ) ;
#13672=VECTOR ( 'NONE', #64645, 1000.000000000000000 ) ;
#13674=EDGE_CURVE ( 'NONE', #54447, #12080, #64754, .T. ) ;
#13685=CARTESIAN_POINT ( 'NONE',  ( -11.75000000000000000, -5.000000000000000000, -11.75000000000000000 ) ) ;
#13686=LINE ( 'NONE', #55778, #1386 ) ;
#13689=CARTESIAN_POINT ( 'NONE',  ( -30.00000000000000000, -8.959999999999999076, 17.04524521594300523 ) ) ;
#13696=VECTOR ( 'NONE', #3679, 1000.000000000000000 ) ;
#13702=DIRECTION ( 'NONE',  ( 0.000000000000000000, -1.000000000000000000, 0.000000000000000000 ) ) ;
#13704=ORIENTED_EDGE ( 'NONE', *, *, #62041, .T. ) ;
#13717=B_SPLINE_CURVE_WITH_KNOTS ( 'NONE', 3,
 ( #19338, #19680, #36663, #47274, #68137, #57873 ),
 .UNSPECIFIED., .F., .F.,
 ( 4, 2, 4 ),
 ( 0.0002380763768115301549, 0.7291065797294569162, 1.457975083082102330 ),
 .UNSPECIFIED. ) ;
#13719=ORIENTED_EDGE ( 'NONE', *, *, #5921, .T. ) ;
#13722=FACE_OUTER_BOUND ( 'NONE', #44601, .T. ) ;
#13726=ORIENTED_EDGE ( 'NONE', *, *, #19740, .T. ) ;
#13727=ORIENTED_EDGE ( 'NONE', *, *, #65606, .F. ) ;
#13731=CYLINDRICAL_SURFACE ( 'NONE', #49467, 3.499999999999850342 ) ;
#13735=ADVANCED_FACE ( 'NONE', ( #50906 ), #18372, .F. ) ;
#13745=AXIS2_PLACEMENT_3D ( 'NONE', #16290, #65432, #38558 ) ;
#13749=EDGE_CURVE ( 'NONE', #48624, #36267, #28950, .T. ) ;
#13756=DIRECTION ( 'NONE',  ( 0.000000000000000000, 0.000000000000000000, -1.000000000000000000 ) ) ;
#13765=VECTOR ( 'NONE', #55204, 1000.000000000000000 ) ;
#13773=ORIENTED_EDGE ( 'NONE', *, *, #20766, .F. ) ;
#13775=CARTESIAN_POINT ( 'NONE',  ( 30.00000000000000000, -9.199999999999999289, -12.69999999999986073 ) ) ;
#13779=CARTESIAN_POINT ( 'NONE',  ( 11.00000000000000000, -11.50000000000082068, 10.20500000000000007 ) ) ;
#13786=DIRECTION ( 'NONE',  ( 0.000000000000000000, 0.000000000000000000, 1.000000000000000000 ) ) ;
#13789=CIRCLE ( 'NONE', #11514, 0.5000000000001392220 ) ;
#13794=ORIENTED_EDGE ( 'NONE', *, *, #34729, .T. ) ;
#13805=EDGE_CURVE ( 'NONE', #58919, #8225, #27805, .T. ) ;
#13824=EDGE_CURVE ( 'NONE', #10241, #30976, #63277, .T. ) ;
#13825=AXIS2_PLACEMENT_3D ( 'NONE', #44120, #65698, #27525 ) ;
#13827=CARTESIAN_POINT ( 'NONE',  ( 30.00000000000000000, -11.10796162543699950, -9.102987789146602893 ) ) ;
#13830=EDGE_CURVE ( 'NONE', #18780, #46315, #45961, .T. ) ;
#13833=CARTESIAN_POINT ( 'NONE',  ( -25.50000000000000355, -15.12100000000000044, -22.50000000000000000 ) ) ;
#13834=ORIENTED_EDGE ( 'NONE', *, *, #46080, .F. ) ;
#13855=ORIENTED_EDGE ( 'NONE', *, *, #32802, .F. ) ;
#13857=LINE ( 'NONE', #40731, #45894 ) ;
#13858=DIRECTION ( 'NONE',  ( 1.000000000000000000, -0.000000000000000000, -0.000000000000000000 ) ) ;
#13859=DIRECTION ( 'NONE',  ( 0.000000000000000000, 0.000000000000000000, -1.000000000000000000 ) ) ;
#13860=DIRECTION ( 'NONE',  ( 0.000000000000000000, -1.000000000000000000, 0.000000000000000000 ) ) ;
#13862=DIRECTION ( 'NONE',  ( -1.000000000000000000, 0.000000000000000000, 0.000000000000000000 ) ) ;
#13867=AXIS2_PLACEMENT_3D ( 'NONE', #26959, #15301, #59129 ) ;
#13875=CARTESIAN_POINT ( 'NONE',  ( -14.25000000000000000, -2.500000000000000000, 21.77831216351300014 ) ) ;
#13885=EDGE_CURVE ( 'NONE', #11924, #46765, #48154, .T. ) ;
#13887=VECTOR ( 'NONE', #39901, 1000.000000000000000 ) ;
#13891=EDGE_CURVE ( 'NONE', #4079, #28664, #24306, .T. ) ;
#13893=FACE_OUTER_BOUND ( 'NONE', #31432, .T. ) ;
#13899=ORIENTED_EDGE ( 'NONE', *, *, #61727, .F. ) ;
#13901=CARTESIAN_POINT ( 'NONE',  ( 30.00000000000000000, -17.14999999999999858, -27.00000000000000000 ) ) ;
#13904=TOROIDAL_SURFACE ( 'NONE', #60182, 3.299999999999474909, 0.2000000000005234813 ) ;
#13908=ORIENTED_EDGE ( 'NONE', *, *, #29756, .F. ) ;
#13910=DIRECTION ( 'NONE',  ( 0.000000000000000000, -1.000000000000000000, 0.000000000000000000 ) ) ;
#13915=VERTEX_POINT ( 'NONE', #24745 ) ;
#13922=CARTESIAN_POINT ( 'NONE',  ( -11.00000000000000000, -5.200000000000001066, -9.400000000000005684 ) ) ;
#13929=AXIS2_PLACEMENT_3D ( 'NONE', #64457, #47826, #42172 ) ;
#13931=FACE_OUTER_BOUND ( 'NONE', #43130, .T. ) ;
#13935=VERTEX_POINT ( 'NONE', #40651 ) ;
#13953=VECTOR ( 'NONE', #41171, 1000.000000000000000 ) ;
#13958=CARTESIAN_POINT ( 'NONE',  ( -25.50000000000000355, -15.50000000000000000, 22.50000000000000000 ) ) ;
#13966=VECTOR ( 'NONE', #39590, 1000.000000000000000 ) ;
#13975=VERTEX_POINT ( 'NONE', #47359 ) ;
#13978=ORIENTED_EDGE ( 'NONE', *, *, #28042, .T. ) ;
#13986=EDGE_CURVE ( 'NONE', #12586, #30907, #10233, .T. ) ;
#13989=PLANE ( 'NONE',  #54984 ) ;
#13991=ORIENTED_EDGE ( 'NONE', *, *, #34009, .T. ) ;
#13994=ORIENTED_EDGE ( 'NONE', *, *, #51274, .F. ) ;
#13998=CARTESIAN_POINT ( 'NONE',  ( 16.75000000000000000, -2.500000000000000000, -21.77831216351300014 ) ) ;
#14000=EDGE_LOOP ( 'NONE', ( #57859, #52707, #58890, #59657, #15265, #28385, #13994, #12118, #65367, #8391, #11135, #37322, #55653, #61972, #963, #31776, #3302, #7312, #32676, #47219 ) ) ;
#14002=CIRCLE ( 'NONE', #55798, 0.5000000000079362072 ) ;
#14007=CARTESIAN_POINT ( 'NONE',  ( -25.49999999999869971, -17.50000000000000000, -22.50000000000000000 ) ) ;
#14009=DIRECTION ( 'NONE',  ( -1.000000000000000000, 0.000000000000000000, 0.000000000000000000 ) ) ;
#14012=EDGE_CURVE ( 'NONE', #58992, #48298, #37118, .T. ) ;
#14013=CARTESIAN_POINT ( 'NONE',  ( 15.50000000000000000, -2.500000000000000000, 21.05662432702600029 ) ) ;
#14021=EDGE_CURVE ( 'NONE', #18603, #11471, #20489, .T. ) ;
#14030=LINE ( 'NONE', #13685, #31918 ) ;
#14031=AXIS2_PLACEMENT_3D ( 'NONE', #34672, #55555, #45990 ) ;
#14034=DIRECTION ( 'NONE',  ( 0.000000000000000000, -1.000000000000000000, -6.036837696397607468E-13 ) ) ;
#14043=DIRECTION ( 'NONE',  ( 0.000000000000000000, -0.9938079899998859545, 0.1111111111112941946 ) ) ;
#14047=DIRECTION ( 'NONE',  ( -1.000000000000000000, 0.000000000000000000, 0.000000000000000000 ) ) ;
#14053=DIRECTION ( 'NONE',  ( 0.000000000000000000, 0.7278708115913771204, 0.6857142857147648929 ) ) ;
#14063=VECTOR ( 'NONE', #14264, 1000.000000000000000 ) ;
#14066=EDGE_CURVE ( 'NONE', #55064, #8160, #31813, .T. ) ;
#14076=ORIENTED_EDGE ( 'NONE', *, *, #68255, .F. ) ;
#14081=ADVANCED_FACE ( 'NONE', ( #10575 ), #4932, .F. ) ;
#14082=DIRECTION ( 'NONE',  ( 0.000000000000000000, 1.000000000000000000, 0.000000000000000000 ) ) ;
#14085=AXIS2_PLACEMENT_3D ( 'NONE', #17242, #7315, #29230 ) ;
#14097=CARTESIAN_POINT ( 'NONE',  ( 30.00000000000000000, -14.04000000000000092, -17.04524521594300523 ) ) ;
#14098=LINE ( 'NONE', #35298, #16761 ) ;
#14099=AXIS2_PLACEMENT_3D ( 'NONE', #36062, #9554, #31129 ) ;
#14100=DIRECTION ( 'NONE',  ( 0.000000000000000000, 1.000000000000000000, 0.000000000000000000 ) ) ;
#14101=VERTEX_POINT ( 'NONE', #15556 ) ;
#14103=ORIENTED_EDGE ( 'NONE', *, *, #24449, .F. ) ;
#14106=CIRCLE ( 'NONE', #29904, 3.499999999999849454 ) ;
#14107=CARTESIAN_POINT ( 'NONE',  ( 22.14589803375000088, -15.50000000000000000, 21.50000000000000000 ) ) ;
#14108=LINE ( 'NONE', #41330, #32810 ) ;
#14121=AXIS2_PLACEMENT_3D ( 'NONE', #23627, #45899, #8777 ) ;
#14124=ORIENTED_EDGE ( 'NONE', *, *, #6444, .T. ) ;
#14133=DIRECTION ( 'NONE',  ( 0.9583148474998867128, 0.000000000000000000, -0.2857142857143631365 ) ) ;
#14140=CARTESIAN_POINT ( 'NONE',  ( -23.75054448485400016, -15.50000000000000000, -25.53140320652400064 ) ) ;
#14144=ORIENTED_EDGE ( 'NONE', *, *, #52256, .T. ) ;
#14147=EDGE_LOOP ( 'NONE', ( #55490, #21362, #1723, #57677 ) ) ;
#14151=DIRECTION ( 'NONE',  ( 0.000000000000000000, -0.1111111111108840643, -0.9938079899999319178 ) ) ;
#14152=EDGE_CURVE ( 'NONE', #36987, #3267, #22239, .T. ) ;
#14168=VECTOR ( 'NONE', #27752, 1000.000000000000000 ) ;
#14180=ORIENTED_EDGE ( 'NONE', *, *, #44525, .T. ) ;
#14186=CIRCLE ( 'NONE', #55978, 0.3499999999998879008 ) ;
#14187=DIRECTION ( 'NONE',  ( 0.000000000000000000, 0.000000000000000000, 1.000000000000000000 ) ) ;
#14188=CARTESIAN_POINT ( 'NONE',  ( 15.50000000000000000, -5.000000000000000000, -19.00000000000000000 ) ) ;
#14192=ORIENTED_EDGE ( 'NONE', *, *, #38108, .F. ) ;
#14193=CARTESIAN_POINT ( 'NONE',  ( 30.00000000000000000, -14.04000000000000092, 14.80000000000000071 ) ) ;
#14199=DIRECTION ( 'NONE',  ( 0.000000000000000000, 0.6857142857146703019, -0.7278708115914659382 ) ) ;
#14205=CYLINDRICAL_SURFACE ( 'NONE', #55859, 0.5000000000001357803 ) ;
#14206=FACE_OUTER_BOUND ( 'NONE', #59409, .T. ) ;
#14231=AXIS2_PLACEMENT_3D ( 'NONE', #43685, #65265, #33749 ) ;
#14232=DIRECTION ( 'NONE',  ( 0.000000000000000000, 0.000000000000000000, -1.000000000000000000 ) ) ;
#14236=EDGE_CURVE ( 'NONE', #68170, #2518, #17606, .T. ) ;
#14238=ADVANCED_FACE ( 'NONE', ( #34553 ), #33862, .T. ) ;
#14241=LINE ( 'NONE', #68692, #21662 ) ;
#14245=ORIENTED_EDGE ( 'NONE', *, *, #61716, .F. ) ;
#14250=DIRECTION ( 'NONE',  ( -0.8660254037844485886, 0.000000000000000000, -0.4999999999999827360 ) ) ;
#14252=EDGE_CURVE ( 'NONE', #14966, #36267, #67452, .T. ) ;
#14256=CARTESIAN_POINT ( 'NONE',  ( 11.00000000000000000, -17.50000000000000000, 60.00000000000000000 ) ) ;
#14264=DIRECTION ( 'NONE',  ( -1.000000000000000000, 0.000000000000000000, 0.000000000000000000 ) ) ;
#14267=CARTESIAN_POINT ( 'NONE',  ( -11.50000000000000000, -12.00000000000000000, -10.69999999999999929 ) ) ;
#14270=ORIENTED_EDGE ( 'NONE', *, *, #43401, .F. ) ;
#14273=ORIENTED_EDGE ( 'NONE', *, *, #2157, .F. ) ;
#14279=DIRECTION ( 'NONE',  ( 0.000000000000000000, 0.000000000000000000, 1.000000000000000000 ) ) ;
#14298=VECTOR ( 'NONE', #32557, 1000.000000000000000 ) ;
#14302=VECTOR ( 'NONE', #19578, 1000.000000000000000 ) ;
#14311=ORIENTED_EDGE ( 'NONE', *, *, #17808, .F. ) ;
#14326=LINE ( 'NONE', #7610, #10836 ) ;
#14330=DIRECTION ( 'NONE',  ( 1.000000000000000000, -0.000000000000000000, -0.000000000000000000 ) ) ;
#14334=ORIENTED_EDGE ( 'NONE', *, *, #59723, .F. ) ;
#14335=CIRCLE ( 'NONE', #3024, 0.2000000000005226763 ) ;
#14337=DIRECTION ( 'NONE',  ( 0.000000000000000000, -1.000000000000000000, 0.000000000000000000 ) ) ;
#14340=ORIENTED_EDGE ( 'NONE', *, *, #15323, .F. ) ;
#14346=EDGE_LOOP ( 'NONE', ( #42724, #36184, #26823, #31652 ) ) ;
#14354=EDGE_LOOP ( 'NONE', ( #64393, #26836 ) ) ;
#14357=CARTESIAN_POINT ( 'NONE',  ( -11.00000000000000000, -12.00000000000000000, -12.20000000000000107 ) ) ;
#14358=DIRECTION ( 'NONE',  ( 0.000000000000000000, 1.000000000000000000, 0.000000000000000000 ) ) ;
#14363=DIRECTION ( 'NONE',  ( 0.000000000000000000, 0.000000000000000000, -1.000000000000000000 ) ) ;
#14364=DIRECTION ( 'NONE',  ( -1.000000000000000000, 0.000000000000000000, 0.000000000000000000 ) ) ;
#14372=AXIS2_PLACEMENT_3D ( 'NONE', #49843, #34256, #23657 ) ;
#14382=DIRECTION ( 'NONE',  ( 0.000000000000000000, -0.7046037717859445770, 0.7096009616573392131 ) ) ;
#14395=CARTESIAN_POINT ( 'NONE',  ( -25.50000000000000355, -5.578999999999999737, 24.12099999999999511 ) ) ;
#14396=CARTESIAN_POINT ( 'NONE',  ( -25.50000000000000355, -5.200000000000001066, 22.50000000000000000 ) ) ;
#14399=CARTESIAN_POINT ( 'NONE',  ( -29.50000000000000355, -12.00000000000000000, -11.03137303340310282 ) ) ;
#14403=ORIENTED_EDGE ( 'NONE', *, *, #44870, .F. ) ;
#14416=VECTOR ( 'NONE', #6811, 1000.000000000000000 ) ;
#14417=ORIENTED_EDGE ( 'NONE', *, *, #46608, .F. ) ;
#14418=DIRECTION ( 'NONE',  ( 0.000000000000000000, -0.7071067811865496822, -0.7071067811865454633 ) ) ;
#14419=CARTESIAN_POINT ( 'NONE',  ( 24.00000000000000000, -15.50000000000000000, 14.50000000000000000 ) ) ;
#14424=ORIENTED_EDGE ( 'NONE', *, *, #3754, .F. ) ;
#14427=ORIENTED_EDGE ( 'NONE', *, *, #7285, .F. ) ;
#14428=VERTEX_POINT ( 'NONE', #52591 ) ;
#14431=CARTESIAN_POINT ( 'NONE',  ( -11.00000000000000000, -13.79999999999979998, 17.64999999999988844 ) ) ;
#14435=VECTOR ( 'NONE', #11323, 1000.000000000000000 ) ;
#14440=AXIS2_PLACEMENT_3D ( 'NONE', #44984, #13858, #2544 ) ;
#14452=AXIS2_PLACEMENT_3D ( 'NONE', #27430, #37695, #17160 ) ;
#14456=ORIENTED_EDGE ( 'NONE', *, *, #3089, .T. ) ;
#14467=ORIENTED_EDGE ( 'NONE', *, *, #13063, .F. ) ;
#14490=VERTEX_POINT ( 'NONE', #43354 ) ;
#14496=CARTESIAN_POINT ( 'NONE',  ( -11.00000000000000000, -9.487228132326899654, 12.50000000000000000 ) ) ;
#14502=DIRECTION ( 'NONE',  ( -1.000000000000000000, 0.000000000000000000, 0.000000000000000000 ) ) ;
#14503=CARTESIAN_POINT ( 'NONE',  ( 13.00000000000000178, -16.28999999999999915, -14.50000000000000000 ) ) ;
#14507=FACE_OUTER_BOUND ( 'NONE', #17735, .T. ) ;
#14508=ORIENTED_EDGE ( 'NONE', *, *, #29057, .F. ) ;
#14521=EDGE_CURVE ( 'NONE', #47155, #26513, #11922, .T. ) ;
#14524=PLANE ( 'NONE',  #64338 ) ;
#14536=ORIENTED_EDGE ( 'NONE', *, *, #37882, .F. ) ;
#14544=CARTESIAN_POINT ( 'NONE',  ( 28.00000000000000000, -16.28999999999710369, -14.50000000000000000 ) ) ;
#14546=DIRECTION ( 'NONE',  ( 0.000000000000000000, 1.000000000000000000, 0.000000000000000000 ) ) ;
#14551=EDGE_CURVE ( 'NONE', #20459, #60747, #22500, .T. ) ;
#14569=ADVANCED_FACE ( 'NONE', ( #45081 ), #946, .T. ) ;
#14577=LINE ( 'NONE', #37553, #15562 ) ;
#14578=DIRECTION ( 'NONE',  ( 1.000000000000000000, 0.000000000000000000, 0.000000000000000000 ) ) ;
#14579=LINE ( 'NONE', #30493, #58182 ) ;
#14586=VERTEX_POINT ( 'NONE', #50044 ) ;
#14589=AXIS2_PLACEMENT_3D ( 'NONE', #34862, #30286, #29209 ) ;
#14591=CARTESIAN_POINT ( 'NONE',  ( -30.00000000000000000, -5.599999999999999645, 27.00000000000000000 ) ) ;
#14607=EDGE_LOOP ( 'NONE', ( #12479, #9765, #41396, #60716 ) ) ;
#14611=ORIENTED_EDGE ( 'NONE', *, *, #55739, .T. ) ;
#14628=ORIENTED_EDGE ( 'NONE', *, *, #47434, .F. ) ;
#14630=EDGE_LOOP ( 'NONE', ( #69922, #31996, #37487, #3835 ) ) ;
#14645=ORIENTED_EDGE ( 'NONE', *, *, #11180, .T. ) ;
#14646=CARTESIAN_POINT ( 'NONE',  ( 29.50000000000000355, -11.50000000000100009, -15.00000000000084910 ) ) ;
#14651=ORIENTED_EDGE ( 'NONE', *, *, #65102, .F. ) ;
#14652=EDGE_CURVE ( 'NONE', #38222, #66537, #13613, .T. ) ;
#14655=CARTESIAN_POINT ( 'NONE',  ( -30.00000000000000000, -12.00000000000000000, -11.03137303340310282 ) ) ;
#14667=CARTESIAN_POINT ( 'NONE',  ( -15.50000000000000000, -0.4000000000005236034, 19.20000000000052509 ) ) ;
#14688=VECTOR ( 'NONE', #29827, 1000.000000000000000 ) ;
#14689=CARTESIAN_POINT ( 'NONE',  ( 30.00000000000000000, -5.000000000000000000, 27.00000000000000000 ) ) ;
#14694=VERTEX_POINT ( 'NONE', #24584 ) ;
#14696=CARTESIAN_POINT ( 'NONE',  ( 16.75000000000000000, -0.2038245569916320166, 21.77831216351300014 ) ) ;
#14698=DIRECTION ( 'NONE',  ( 0.8660254037844485886, 0.000000000000000000, -0.4999999999999827360 ) ) ;
#14702=ORIENTED_EDGE ( 'NONE', *, *, #67947, .F. ) ;
#14705=DIRECTION ( 'NONE',  ( 0.000000000000000000, 0.000000000000000000, 1.000000000000000000 ) ) ;
#14707=ADVANCED_FACE ( 'NONE', ( #23875 ), #24925, .T. ) ;
#14716=EDGE_CURVE ( 'NONE', #17555, #15458, #50349, .T. ) ;
#14717=EDGE_CURVE ( 'NONE', #62442, #44065, #14326, .T. ) ;
#14732=LINE ( 'NONE', #24989, #3143 ) ;
#14735=ORIENTED_EDGE ( 'NONE', *, *, #21587, .F. ) ;
#14737=DIRECTION ( 'NONE',  ( -1.000000000000000000, 0.000000000000000000, 0.000000000000000000 ) ) ;
#14739=EDGE_CURVE ( 'NONE', #7353, #35907, #8661, .T. ) ;
#14741=CARTESIAN_POINT ( 'NONE',  ( -11.00000000000000000, -14.04000000000000092, -17.04524521594300523 ) ) ;
#14744=DIRECTION ( 'NONE',  ( 0.000000000000000000, 1.000000000000000000, 0.000000000000000000 ) ) ;
#14755=CARTESIAN_POINT ( 'NONE',  ( -11.00000000000000000, -14.04000000000000092, 14.80000000000000071 ) ) ;
#14774=EDGE_CURVE ( 'NONE', #58038, #48042, #13264, .T. ) ;
#14784=CYLINDRICAL_SURFACE ( 'NONE', #55915, 3.499999999999853895 ) ;
#14786=LINE ( 'NONE', #36345, #36526 ) ;
#14787=VERTEX_POINT ( 'NONE', #57098 ) ;
#14788=EDGE_CURVE ( 'NONE', #64, #52369, #7437, .T. ) ;
#14792=VECTOR ( 'NONE', #45887, 1000.000000000000000 ) ;
#14793=EDGE_CURVE ( 'NONE', #20570, #20601, #27798, .T. ) ;
#14802=ORIENTED_EDGE ( 'NONE', *, *, #18733, .F. ) ;
#14807=DIRECTION ( 'NONE',  ( -1.000000000000000000, 0.000000000000000000, 0.000000000000000000 ) ) ;
#14821=DIRECTION ( 'NONE',  ( 0.000000000000000000, 1.000000000000000000, 0.000000000000000000 ) ) ;
#14829=ORIENTED_EDGE ( 'NONE', *, *, #59154, .T. ) ;
#14831=CIRCLE ( 'NONE', #11432, 0.5000000000001362244 ) ;
#14839=DIRECTION ( 'NONE',  ( 1.000000000000000000, 0.000000000000000000, 0.000000000000000000 ) ) ;
#14841=VERTEX_POINT ( 'NONE', #9364 ) ;
#14858=DIRECTION ( 'NONE',  ( 1.000000000000000000, 0.000000000000000000, 0.000000000000000000 ) ) ;
#14871=CARTESIAN_POINT ( 'NONE',  ( -25.50000000000000355, -5.578999999999999737, -22.50000000000000000 ) ) ;
#14877=VERTEX_POINT ( 'NONE', #63813 ) ;
#14878=ADVANCED_FACE ( 'NONE', ( #36577 ), #31645, .F. ) ;
#14887=DIRECTION ( 'NONE',  ( 1.000000000000000000, 0.000000000000000000, 0.000000000000000000 ) ) ;
#14890=AXIS2_PLACEMENT_3D ( 'NONE', #37907, #11703, #58779 ) ;
#14893=LINE ( 'NONE', #58727, #30857 ) ;
#14894=CARTESIAN_POINT ( 'NONE',  ( -25.50000000000000355, 0.000000000000000000, -20.24999999999999645 ) ) ;
#14896=VECTOR ( 'NONE', #2489, 1000.000000000000000 ) ;
#14904=CARTESIAN_POINT ( 'NONE',  ( 15.50000000000000000, -1.037157890325000054, 19.00000000000000000 ) ) ;
#14913=DIRECTION ( 'NONE',  ( 0.000000000000000000, 0.000000000000000000, 1.000000000000000000 ) ) ;
#14914=VERTEX_POINT ( 'NONE', #48592 ) ;
#14919=EDGE_CURVE ( 'NONE', #21874, #64942, #39096, .T. ) ;
#14920=CARTESIAN_POINT ( 'NONE',  ( -28.00000000000000000, -15.50000000000000000, -20.05051025721700242 ) ) ;
#14921=EDGE_CURVE ( 'NONE', #14787, #1760, #23294, .T. ) ;
#14923=VERTEX_POINT ( 'NONE', #5810 ) ;
#14931=CARTESIAN_POINT ( 'NONE',  ( 28.00000000000000000, -17.50000000000000000, 20.05051025721700242 ) ) ;
#14932=VERTEX_POINT ( 'NONE', #6504 ) ;
#14934=ORIENTED_EDGE ( 'NONE', *, *, #62662, .F. ) ;
#14935=VERTEX_POINT ( 'NONE', #65881 ) ;
#14938=DIRECTION ( 'NONE',  ( -1.000000000000000000, 0.000000000000000000, 0.000000000000000000 ) ) ;
#14941=CARTESIAN_POINT ( 'NONE',  ( -16.75000000000000000, -2.500000000000000000, 21.77831216351300014 ) ) ;
#14948=FACE_OUTER_BOUND ( 'NONE', #50331, .T. ) ;
#14950=DIRECTION ( 'NONE',  ( 1.000000000000000000, 0.000000000000000000, 0.000000000000000000 ) ) ;
#14957=ORIENTED_EDGE ( 'NONE', *, *, #63145, .T. ) ;
#14965=EDGE_LOOP ( 'NONE', ( #34053, #68781, #42539, #14144 ) ) ;
#14966=VERTEX_POINT ( 'NONE', #16417 ) ;
#14976=VERTEX_POINT ( 'NONE', #870 ) ;
#14983=ORIENTED_EDGE ( 'NONE', *, *, #5901, .F. ) ;
#14985=EDGE_LOOP ( 'NONE', ( #69714, #45351 ) ) ;
#14988=DIRECTION ( 'NONE',  ( 0.000000000000000000, -0.7046037717806115097, -0.7096009616626348659 ) ) ;
#14991=CARTESIAN_POINT ( 'NONE',  ( 14.45366306705350112, -0.2717122460102528447, 21.66072723692567692 ) ) ;
#14996=CARTESIAN_POINT ( 'NONE',  ( -29.50000000000000355, -11.50000000000100009, -15.00000000000084910 ) ) ;
#14998=AXIS2_PLACEMENT_3D ( 'NONE', #28402, #60926, #39367 ) ;
#14999=PLANE ( 'NONE',  #21029 ) ;
#15003=AXIS2_PLACEMENT_3D ( 'NONE', #35424, #50304, #7515 ) ;
#15006=VECTOR ( 'NONE', #46636, 1000.000000000000000 ) ;
#15017=ORIENTED_EDGE ( 'NONE', *, *, #5608, .T. ) ;
#15018=CARTESIAN_POINT ( 'NONE',  ( 15.50000000000000000, -0.2000000000000000111, 19.19999999702029925 ) ) ;
#15022=DIRECTION ( 'NONE',  ( 0.000000000000000000, 0.000000000000000000, 1.000000000000000000 ) ) ;
#15023=ADVANCED_FACE ( 'NONE', ( #28393 ), #39012, .F. ) ;
#15047=ORIENTED_EDGE ( 'NONE', *, *, #17340, .F. ) ;
#15048=DIRECTION ( 'NONE',  ( 0.000000000000000000, 0.000000000000000000, 1.000000000000000000 ) ) ;
#15050=LINE ( 'NONE', #36611, #29365 ) ;
#15053=ORIENTED_EDGE ( 'NONE', *, *, #47138, .F. ) ;
#15054=VERTEX_POINT ( 'NONE', #59075 ) ;
#15058=AXIS2_PLACEMENT_3D ( 'NONE', #50466, #56459, #40543 ) ;
#15064=DIRECTION ( 'NONE',  ( -1.000000000000000000, 0.000000000000000000, 0.000000000000000000 ) ) ;
#15071=AXIS2_PLACEMENT_3D ( 'NONE', #12969, #62116, #24297 ) ;
#15073=ORIENTED_EDGE ( 'NONE', *, *, #27013, .F. ) ;
#15083=EDGE_CURVE ( 'NONE', #27322, #42854, #33449, .T. ) ;
#15090=DIRECTION ( 'NONE',  ( 0.000000000000000000, 1.000000000000000000, 0.000000000000000000 ) ) ;
#15093=EDGE_LOOP ( 'NONE', ( #64432, #4577, #54458, #42531, #24057, #65944 ) ) ;
#15094=CARTESIAN_POINT ( 'NONE',  ( 30.00000000000000000, -5.200000000000001066, 9.399999999999998579 ) ) ;
#15096=ADVANCED_FACE ( 'NONE', ( #42110, #68987 ), #42811, .T. ) ;
#15101=LINE ( 'NONE', #30311, #52396 ) ;
#15107=AXIS2_PLACEMENT_3D ( 'NONE', #34307, #33967, #18761 ) ;
#15114=DIRECTION ( 'NONE',  ( 0.000000000000000000, -0.8206518066484758123, 0.5714285714283042772 ) ) ;
#15120=LINE ( 'NONE', #37384, #206 ) ;
#15125=EDGE_LOOP ( 'NONE', ( #46429, #46341, #31602, #25583, #47323, #23533, #20786 ) ) ;
#15133=EDGE_LOOP ( 'NONE', ( #68942, #43022, #56198, #26007, #3633, #8329, #32089 ) ) ;
#15139=ORIENTED_EDGE ( 'NONE', *, *, #1152, .F. ) ;
#15143=DIRECTION ( 'NONE',  ( -1.000000000000000000, 0.000000000000000000, 0.000000000000000000 ) ) ;
#15145=CARTESIAN_POINT ( 'NONE',  ( 16.75000000000000355, -0.2715193793361411756, -22.01281590054916038 ) ) ;
#15165=DIRECTION ( 'NONE',  ( 0.000000000000000000, 0.000000000000000000, 1.000000000000000000 ) ) ;
#15176=B_SPLINE_CURVE_WITH_KNOTS ( 'NONE', 3,
 ( #19593, #53197, #10393, #4742, #31963, #15703 ),
 .UNSPECIFIED., .F., .F.,
 ( 4, 2, 4 ),
 ( 1.820537833122030991, 2.555393473688635453, 3.290249114255240137 ),
 .UNSPECIFIED. ) ;
#15184=DIRECTION ( 'NONE',  ( -1.000000000000000000, 0.000000000000000000, 0.000000000000000000 ) ) ;
#15191=ADVANCED_FACE ( 'NONE', ( #28621 ), #736, .T. ) ;
#15193=CIRCLE ( 'NONE', #12877, 3.499999999999849454 ) ;
#15218=ORIENTED_EDGE ( 'NONE', *, *, #55332, .T. ) ;
#15224=CARTESIAN_POINT ( 'NONE',  ( 30.00000000000000000, -5.000000000000000000, -27.00000000000000000 ) ) ;
#15227=ORIENTED_EDGE ( 'NONE', *, *, #3139, .F. ) ;
#15231=CYLINDRICAL_SURFACE ( 'NONE', #23144, 0.3499999999999614531 ) ;
#15235=ORIENTED_EDGE ( 'NONE', *, *, #35608, .F. ) ;
#15236=CIRCLE ( 'NONE', #59242, 1.449999999999996403 ) ;
#15237=EDGE_CURVE ( 'NONE', #26720, #59384, #31255, .T. ) ;
#15242=EDGE_LOOP ( 'NONE', ( #5061, #13855, #66522, #68320 ) ) ;
#15246=AXIS2_PLACEMENT_3D ( 'NONE', #5002, #65099, #10310 ) ;
#15249=DIRECTION ( 'NONE',  ( 0.000000000000000000, -0.7046037717806115097, -0.7096009616626348659 ) ) ;
#15262=ORIENTED_EDGE ( 'NONE', *, *, #3751, .F. ) ;
#15263=DIRECTION ( 'NONE',  ( -0.000000000000000000, 1.000000000000000000, -0.000000000000000000 ) ) ;
#15265=ORIENTED_EDGE ( 'NONE', *, *, #9587, .T. ) ;
#15267=CARTESIAN_POINT ( 'NONE',  ( 15.50000000000000000, -0.2038245569916610489, -23.94337567297399971 ) ) ;
#15268=CARTESIAN_POINT ( 'NONE',  ( 30.00000000000000000, -13.79999999999979998, -17.30000000000000071 ) ) ;
#15286=ORIENTED_EDGE ( 'NONE', *, *, #37741, .T. ) ;
#15292=VECTOR ( 'NONE', #24304, 1000.000000000000000 ) ;
#15294=ORIENTED_EDGE ( 'NONE', *, *, #11451, .F. ) ;
#15296=CARTESIAN_POINT ( 'NONE',  ( 15.50000000000000000, -1.037157890325000054, 22.50000000000000000 ) ) ;
#15297=ORIENTED_EDGE ( 'NONE', *, *, #39265, .F. ) ;
#15301=DIRECTION ( 'NONE',  ( 0.000000000000000000, 1.000000000000000000, 0.000000000000000000 ) ) ;
#15303=AXIS2_PLACEMENT_3D ( 'NONE', #11213, #23204, #27136 ) ;
#15308=VERTEX_POINT ( 'NONE', #8099 ) ;
#15311=EDGE_CURVE ( 'NONE', #33396, #44394, #28981, .T. ) ;
#15314=ORIENTED_EDGE ( 'NONE', *, *, #14788, .T. ) ;
#15321=VERTEX_POINT ( 'NONE', #22981 ) ;
#15322=CARTESIAN_POINT ( 'NONE',  ( -11.00000000000000000, -17.35230188589299871, 15.35019951917099945 ) ) ;
#15323=EDGE_CURVE ( 'NONE', #611, #64746, #51242, .T. ) ;
#15343=ORIENTED_EDGE ( 'NONE', *, *, #66736, .T. ) ;
#15346=VECTOR ( 'NONE', #27338, 1000.000000000000000 ) ;
#15351=CARTESIAN_POINT ( 'NONE',  ( -15.50000000000000000, -0.1999999999999999556, -22.50000000000000000 ) ) ;
#15354=AXIS2_PLACEMENT_3D ( 'NONE', #59293, #43372, #22169 ) ;
#15362=EDGE_CURVE ( 'NONE', #58695, #67917, #65114, .T. ) ;
#15363=AXIS2_PLACEMENT_3D ( 'NONE', #18287, #45870, #67451 ) ;
#15366=VERTEX_POINT ( 'NONE', #2800 ) ;
#15372=DIRECTION ( 'NONE',  ( 1.000000000000000000, -0.000000000000000000, -0.000000000000000000 ) ) ;
#15374=PLANE ( 'NONE',  #58091 ) ;
#15375=FACE_OUTER_BOUND ( 'NONE', #15509, .T. ) ;
#15378=EDGE_CURVE ( 'NONE', #32123, #66059, #56890, .T. ) ;
#15381=DIRECTION ( 'NONE',  ( -0.3479852726768751237, 0.000000000000000000, -0.9375000000000004441 ) ) ;
#15383=EDGE_CURVE ( 'NONE', #19227, #51892, #7489, .T. ) ;
#15385=LINE ( 'NONE', #63117, #5194 ) ;
#15388=VECTOR ( 'NONE', #2992, 1000.000000000000114 ) ;
#15394=AXIS2_PLACEMENT_3D ( 'NONE', #40482, #35167, #62751 ) ;
#15395=ORIENTED_EDGE ( 'NONE', *, *, #19846, .T. ) ;
#15399=VECTOR ( 'NONE', #12715, 1000.000000000000000 ) ;
#15400=VECTOR ( 'NONE', #69689, 999.9999999999998863 ) ;
#15403=LINE ( 'NONE', #3736, #28263 ) ;
#15415=DIRECTION ( 'NONE',  ( 0.000000000000000000, 0.7096009616570518874, -0.7046037717862339012 ) ) ;
#15416=ORIENTED_EDGE ( 'NONE', *, *, #38619, .F. ) ;
#15420=CARTESIAN_POINT ( 'NONE',  ( 28.00000000000000000, -17.35230188589299516, -15.35019951917100478 ) ) ;
#15426=DIRECTION ( 'NONE',  ( 0.000000000000000000, 0.000000000000000000, 1.000000000000000000 ) ) ;
#15432=DIRECTION ( 'NONE',  ( 1.000000000000000000, -0.000000000000000000, -0.000000000000000000 ) ) ;
#15445=EDGE_CURVE ( 'NONE', #50590, #64280, #24380, .T. ) ;
#15446=VECTOR ( 'NONE', #6580, 1000.000000000000000 ) ;
#15447=VECTOR ( 'NONE', #5968, 1000.000000000000000 ) ;
#15449=EDGE_CURVE ( 'NONE', #7103, #30626, #39143, .T. ) ;
#15456=AXIS2_PLACEMENT_3D ( 'NONE', #2680, #56084, #44757 ) ;
#15458=VERTEX_POINT ( 'NONE', #29318 ) ;
#15463=AXIS2_PLACEMENT_3D ( 'NONE', #21249, #15604, #26546 ) ;
#15469=EDGE_CURVE ( 'NONE', #12841, #58919, #62912, .T. ) ;
#15486=CARTESIAN_POINT ( 'NONE',  ( 11.00000000000000000, -10.85999999999999943, -9.350000000000269651 ) ) ;
#15488=CIRCLE ( 'NONE', #39136, 4.000000000000000888 ) ;
#15489=ORIENTED_EDGE ( 'NONE', *, *, #40632, .T. ) ;
#15499=AXIS2_PLACEMENT_3D ( 'NONE', #44435, #50791, #61387 ) ;
#15500=CARTESIAN_POINT ( 'NONE',  ( 30.00000000000000000, -5.599999999999999645, 27.00000000000000000 ) ) ;
#15504=AXIS2_PLACEMENT_3D ( 'NONE', #6143, #22746, #44301 ) ;
#15505=CIRCLE ( 'NONE', #32463, 4.000000000000000888 ) ;
#15509=EDGE_LOOP ( 'NONE', ( #39746, #57757, #9966, #39003, #10101, #23207, #63902 ) ) ;
#15515=ORIENTED_EDGE ( 'NONE', *, *, #43543, .F. ) ;
#15519=CARTESIAN_POINT ( 'NONE',  ( 15.50000000000129852, -17.50000000000000000, -22.50000000000000000 ) ) ;
#15531=EDGE_CURVE ( 'NONE', #62094, #44371, #41685, .T. ) ;
#15535=CARTESIAN_POINT ( 'NONE',  ( 30.00000000000000000, -16.28999999999999915, 14.50000000000000000 ) ) ;
#15536=DIRECTION ( 'NONE',  ( 0.4998444328988824181, 0.000000000000000000, -0.8661152018640445593 ) ) ;
#15543=ORIENTED_EDGE ( 'NONE', *, *, #60603, .F. ) ;
#15544=CARTESIAN_POINT ( 'NONE',  ( 30.00000000000000000, -12.00000000000000000, -12.20000000000000107 ) ) ;
#15545=ADVANCED_FACE ( 'NONE', ( #9881 ), #47695, .F. ) ;
#15556=CARTESIAN_POINT ( 'NONE',  ( -25.50000000000000355, -15.50000000000000000, 20.49999999999999645 ) ) ;
#15558=DIRECTION ( 'NONE',  ( -0.4999999999999832356, 0.000000000000000000, 0.8660254037844483666 ) ) ;
#15562=VECTOR ( 'NONE', #58773, 1000.000000000000000 ) ;
#15569=ORIENTED_EDGE ( 'NONE', *, *, #23491, .T. ) ;
#15571=CIRCLE ( 'NONE', #13307, 4.500000000000191847 ) ;
#15574=CARTESIAN_POINT ( 'NONE',  ( 11.50000000000000000, -11.50000000000000000, 15.00000000000000000 ) ) ;
#15578=ORIENTED_EDGE ( 'NONE', *, *, #41468, .T. ) ;
#15584=ORIENTED_EDGE ( 'NONE', *, *, #3509, .T. ) ;
#15585=CARTESIAN_POINT ( 'NONE',  ( 30.00000000000000000, -5.599999999999379696, 26.60000000000059828 ) ) ;
#15594=EDGE_CURVE ( 'NONE', #11358, #27679, #302, .T. ) ;
#15600=LINE ( 'NONE', #31855, #13097 ) ;
#15602=ORIENTED_EDGE ( 'NONE', *, *, #3659, .T. ) ;
#15604=DIRECTION ( 'NONE',  ( -1.000000000000000000, 0.000000000000000000, 0.000000000000000000 ) ) ;
#15607=EDGE_LOOP ( 'NONE', ( #50161, #47400 ) ) ;
#15614=DIRECTION ( 'NONE',  ( 0.000000000000000000, 1.000000000000000000, 0.000000000000000000 ) ) ;
#15620=LINE ( 'NONE', #48833, #58774 ) ;
#15623=FACE_OUTER_BOUND ( 'NONE', #51386, .T. ) ;
#15626=DIRECTION ( 'NONE',  ( 0.000000000000000000, 0.000000000000000000, 1.000000000000000000 ) ) ;
#15632=ORIENTED_EDGE ( 'NONE', *, *, #38201, .F. ) ;
#15635=ADVANCED_FACE ( 'NONE', ( #43782 ), #65354, .F. ) ;
#15637=DIRECTION ( 'NONE',  ( -1.000000000000000000, 0.000000000000000000, 0.000000000000000000 ) ) ;
#15638=ORIENTED_EDGE ( 'NONE', *, *, #67464, .F. ) ;
#15639=DIRECTION ( 'NONE',  ( 1.000000000000000000, 0.000000000000000000, 0.000000000000000000 ) ) ;
#15645=CARTESIAN_POINT ( 'NONE',  ( -30.00000000000000000, -8.959999999999999076, 17.04524521594300523 ) ) ;
#15656=DIRECTION ( 'NONE',  ( 0.000000000000000000, -0.7046037717859411353, -0.7096009616573427659 ) ) ;
#15672=EDGE_CURVE ( 'NONE', #51391, #5551, #3066, .T. ) ;
#15686=DIRECTION ( 'NONE',  ( 0.000000000000000000, 1.000000000000000000, 0.000000000000000000 ) ) ;
#15687=EDGE_CURVE ( 'NONE', #12012, #58158, #6455, .T. ) ;
#15694=CARTESIAN_POINT ( 'NONE',  ( -30.00000000000000000, -11.50000000000082068, 10.20500000000000007 ) ) ;
#15703=CARTESIAN_POINT ( 'NONE',  ( 16.75000000000000000, -0.2038245569916320166, 21.77831216351300014 ) ) ;
#15712=EDGE_CURVE ( 'NONE', #52459, #27455, #61771, .T. ) ;
#15718=EDGE_CURVE ( 'NONE', #5551, #51391, #47084, .T. ) ;
#15719=CARTESIAN_POINT ( 'NONE',  ( -30.00000000000000000, -10.85999999999999943, -9.000000000000001776 ) ) ;
#15733=CARTESIAN_POINT ( 'NONE',  ( 15.29633693294940677, -0.2717122460100966919, -21.17420925361164308 ) ) ;
#15735=EDGE_LOOP ( 'NONE', ( #65059, #26731, #24282, #57485 ) ) ;
#15738=EDGE_LOOP ( 'NONE', ( #17632, #55378, #34630, #50602 ) ) ;
#15749=VECTOR ( 'NONE', #23671, 1000.000000000000000 ) ;
#15760=DIRECTION ( 'NONE',  ( 0.000000000000000000, 1.000000000000000000, -1.500535806722257514E-12 ) ) ;
#15761=DIRECTION ( 'NONE',  ( 0.000000000000000000, 0.000000000000000000, 1.000000000000000000 ) ) ;
#15767=DIRECTION ( 'NONE',  ( 0.000000000000000000, 0.000000000000000000, 1.000000000000000000 ) ) ;
#15783=CIRCLE ( 'NONE', #25948, 4.500000000000191847 ) ;
#15799=LINE ( 'NONE', #38081, #31027 ) ;
#15801=CARTESIAN_POINT ( 'NONE',  ( 25.50000000000000355, -5.578999999999999737, -22.50000000000000000 ) ) ;
#15804=B_SPLINE_CURVE_WITH_KNOTS ( 'NONE', 3,
 ( #4396, #36193, #36921, #46801, #14991, #4036 ),
 .UNSPECIFIED., .F., .F.,
 ( 4, 2, 4 ),
 ( 0.0002380763768130567115, 0.7291065797294590256, 1.457975083082104995 ),
 .UNSPECIFIED. ) ;
#15808=EDGE_LOOP ( 'NONE', ( #38734, #25856, #35683, #32446 ) ) ;
#15811=DIRECTION ( 'NONE',  ( 0.000000000000000000, 1.000000000000000000, 0.000000000000000000 ) ) ;
#15812=ORIENTED_EDGE ( 'NONE', *, *, #2909, .F. ) ;
#15813=ADVANCED_FACE ( 'NONE', ( #66384 ), #39496, .T. ) ;
#15815=ORIENTED_EDGE ( 'NONE', *, *, #63833, .T. ) ;
#15824=DIRECTION ( 'NONE',  ( -0.4999999999989361843, 0.000000000000000000, -0.8660254037850529940 ) ) ;
#15839=EDGE_CURVE ( 'NONE', #40705, #65652, #68484, .T. ) ;
#15840=ORIENTED_EDGE ( 'NONE', *, *, #40001, .F. ) ;
#15842=ORIENTED_EDGE ( 'NONE', *, *, #39443, .T. ) ;
#15849=LINE ( 'NONE', #57929, #30220 ) ;
#15850=CARTESIAN_POINT ( 'NONE',  ( 13.00000000000000178, -15.50000000000000000, -14.50000000000000000 ) ) ;
#15857=CIRCLE ( 'NONE', #64262, 4.500000000000190958 ) ;
#15859=CARTESIAN_POINT ( 'NONE',  ( -11.50000000000000000, -12.00000000000000000, 10.69999999999999929 ) ) ;
#15871=DIRECTION ( 'NONE',  ( -1.000000000000000000, 0.000000000000000000, 0.000000000000000000 ) ) ;
#15875=ORIENTED_EDGE ( 'NONE', *, *, #17714, .T. ) ;
#15876=DIRECTION ( 'NONE',  ( 0.000000000000000000, 0.000000000000000000, 1.000000000000000000 ) ) ;
#15878=CARTESIAN_POINT ( 'NONE',  ( 11.00000000000000000, -5.599999999999999645, 9.000000000000001776 ) ) ;
#15879=CARTESIAN_POINT ( 'NONE',  ( 11.00000000000000000, -5.599999999999999645, -9.400000000000000355 ) ) ;
#15893=ORIENTED_EDGE ( 'NONE', *, *, #48923, .T. ) ;
#15904=CARTESIAN_POINT ( 'NONE',  ( -25.50000000000000355, -5.578999999999999737, -22.50000000000000000 ) ) ;
#15906=EDGE_LOOP ( 'NONE', ( #64261, #49548, #48341, #31371 ) ) ;
#15907=LINE ( 'NONE', #42425, #33010 ) ;
#15910=ORIENTED_EDGE ( 'NONE', *, *, #18191, .F. ) ;
#15912=CARTESIAN_POINT ( 'NONE',  ( -29.50000000000000355, -11.50000000000100009, 15.00000000000084910 ) ) ;
#15914=EDGE_CURVE ( 'NONE', #49081, #45591, #53909, .T. ) ;
#15916=DIRECTION ( 'NONE',  ( 0.000000000000000000, 0.000000000000000000, -1.000000000000000000 ) ) ;
#15925=CARTESIAN_POINT ( 'NONE',  ( 30.00000000000000000, -9.199999999999999289, -12.69999999999986073 ) ) ;
#15947=DIRECTION ( 'NONE',  ( 0.000000000000000000, 0.000000000000000000, 1.000000000000000000 ) ) ;
#15951=DIRECTION ( 'NONE',  ( 0.000000000000000000, -1.000000000000000000, 0.000000000000000000 ) ) ;
#15953=LINE ( 'NONE', #37523, #51592 ) ;
#15960=DIRECTION ( 'NONE',  ( 0.000000000000000000, 0.000000000000000000, -1.000000000000000000 ) ) ;
#15962=ORIENTED_EDGE ( 'NONE', *, *, #1899, .F. ) ;
#15969=DIRECTION ( 'NONE',  ( 0.000000000000000000, 1.000000000000000000, 0.000000000000000000 ) ) ;
#15970=ORIENTED_EDGE ( 'NONE', *, *, #57345, .F. ) ;
#15971=ADVANCED_FACE ( 'NONE', ( #31372 ), #68831, .F. ) ;
#15977=CIRCLE ( 'NONE', #67907, 0.3499999999999611200 ) ;
#15982=DIRECTION ( 'NONE',  ( -1.000000000000000000, 0.000000000000000000, 0.000000000000000000 ) ) ;
#15998=CARTESIAN_POINT ( 'NONE',  ( -11.00000000000000000, -13.54524521594299991, 17.53999999999999915 ) ) ;
#15999=ADVANCED_FACE ( 'NONE', ( #42651 ), #54313, .T. ) ;
#16003=LINE ( 'NONE', #21309, #48164 ) ;
#16006=ORIENTED_EDGE ( 'NONE', *, *, #40224, .T. ) ;
#16008=ORIENTED_EDGE ( 'NONE', *, *, #23716, .F. ) ;
#16017=CARTESIAN_POINT ( 'NONE',  ( -25.50000000000000355, -5.578999999999999737, -24.12099999999999866 ) ) ;
#16018=ORIENTED_EDGE ( 'NONE', *, *, #29548, .T. ) ;
#16022=DIRECTION ( 'NONE',  ( 0.000000000000000000, -5.800915303574361727E-12, 1.000000000000000000 ) ) ;
#16030=CARTESIAN_POINT ( 'NONE',  ( -16.33565937784311828, -0.3156604612129161880, -23.46090750622545684 ) ) ;
#16031=ORIENTED_EDGE ( 'NONE', *, *, #56553, .T. ) ;
#16044=VERTEX_POINT ( 'NONE', #6215 ) ;
#16045=FACE_OUTER_BOUND ( 'NONE', #2406, .T. ) ;
#16047=DIRECTION ( 'NONE',  ( 0.000000000000000000, -0.7096009616570518874, 0.7046037717862339012 ) ) ;
#16051=FACE_OUTER_BOUND ( 'NONE', #29705, .T. ) ;
#16059=ORIENTED_EDGE ( 'NONE', *, *, #45284, .T. ) ;
#16060=CARTESIAN_POINT ( 'NONE',  ( 30.00000000000000000, -9.454754784057099570, 17.53999999999999915 ) ) ;
#16063=EDGE_LOOP ( 'NONE', ( #20338, #15842, #8161, #62231, #24752, #46865 ) ) ;
#16065=CARTESIAN_POINT ( 'NONE',  ( 11.50000000000000000, -11.50000000000000000, -15.00000000000000000 ) ) ;
#16074=LINE ( 'NONE', #27029, #29461 ) ;
#16078=ORIENTED_EDGE ( 'NONE', *, *, #29541, .F. ) ;
#16086=EDGE_LOOP ( 'NONE', ( #14403, #17485, #7632, #66234 ) ) ;
#16087=EDGE_LOOP ( 'NONE', ( #7081, #58548, #14270, #59120 ) ) ;
#16101=FACE_OUTER_BOUND ( 'NONE', #18428, .T. ) ;
#16105=LINE ( 'NONE', #59239, #23260 ) ;
#16109=LINE ( 'NONE', #4467, #43705 ) ;
#16111=ORIENTED_EDGE ( 'NONE', *, *, #23528, .F. ) ;
#16115=PLANE ( 'NONE',  #10104 ) ;
#16127=DIRECTION ( 'NONE',  ( 0.000000000000000000, 0.000000000000000000, 1.000000000000000000 ) ) ;
#16130=CARTESIAN_POINT ( 'NONE',  ( -29.50000000000000355, -12.00000000000000000, 10.69999999999999929 ) ) ;
#16131=DIRECTION ( 'NONE',  ( 0.000000000000000000, 0.000000000000000000, 1.000000000000000000 ) ) ;
#16134=LINE ( 'NONE', #225, #7759 ) ;
#16137=EDGE_CURVE ( 'NONE', #34366, #27404, #46043, .T. ) ;
#16141=DIRECTION ( 'NONE',  ( -1.000000000000000000, 0.000000000000000000, 0.000000000000000000 ) ) ;
#16155=CARTESIAN_POINT ( 'NONE',  ( 29.50000000000000355, -11.50000000000100009, -10.50000000000065903 ) ) ;
#16163=ORIENTED_EDGE ( 'NONE', *, *, #63145, .F. ) ;
#16169=DIRECTION ( 'NONE',  ( 0.000000000000000000, -1.000000000000000000, 0.000000000000000000 ) ) ;
#16181=LINE ( 'NONE', #27142, #45759 ) ;
#16183=DIRECTION ( 'NONE',  ( 0.000000000000000000, 1.000000000000000000, 0.000000000000000000 ) ) ;
#16184=VERTEX_POINT ( 'NONE', #6571 ) ;
#16187=ORIENTED_EDGE ( 'NONE', *, *, #12508, .F. ) ;
#16189=EDGE_CURVE ( 'NONE', #8473, #21794, #57316, .T. ) ;
#16198=VECTOR ( 'NONE', #17337, 1000.000000000000000 ) ;
#16200=CARTESIAN_POINT ( 'NONE',  ( 30.00000000000000000, -14.33999999999999986, -14.50000000000000000 ) ) ;
#16201=CARTESIAN_POINT ( 'NONE',  ( -17.00000000000000000, -16.28999999999710369, 15.00000000000794920 ) ) ;
#16204=AXIS2_PLACEMENT_3D ( 'NONE', #19439, #51626, #46659 ) ;
#16210=CIRCLE ( 'NONE', #52362, 2.250000000000001776 ) ;
#16221=EDGE_LOOP ( 'NONE', ( #9119, #23496, #38767, #44673 ) ) ;
#16226=DIRECTION ( 'NONE',  ( -1.000000000000000000, 0.000000000000000000, 0.000000000000000000 ) ) ;
#16241=DIRECTION ( 'NONE',  ( -0.000000000000000000, 1.000000000000000000, -0.000000000000000000 ) ) ;
#16245=CARTESIAN_POINT ( 'NONE',  ( -15.50000000000000000, -15.50000000000000000, -22.50000000000000000 ) ) ;
#16247=ORIENTED_EDGE ( 'NONE', *, *, #45910, .T. ) ;
#16253=ORIENTED_EDGE ( 'NONE', *, *, #66398, .T. ) ;
#16257=ORIENTED_EDGE ( 'NONE', *, *, #25405, .F. ) ;
#16262=EDGE_LOOP ( 'NONE', ( #28011, #11104, #14536, #7929 ) ) ;
#16273=LINE ( 'NONE', #49149, #66211 ) ;
#16276=ADVANCED_FACE ( 'NONE', ( #53808 ), #53117, .T. ) ;
#16278=LINE ( 'NONE', #16641, #24487 ) ;
#16284=DIRECTION ( 'NONE',  ( -1.000000000000000000, 0.000000000000000000, 0.000000000000000000 ) ) ;
#16290=CARTESIAN_POINT ( 'NONE',  ( 11.00000000000000000, -13.79999999999979998, -17.30000000000000071 ) ) ;
#16292=CARTESIAN_POINT ( 'NONE',  ( -16.75000000000000000, -0.3156864504677179273, -22.74361999681790536 ) ) ;
#16298=CARTESIAN_POINT ( 'NONE',  ( -29.50000000000000355, -12.00000000000000000, -10.52786404500095863 ) ) ;
#16302=VERTEX_POINT ( 'NONE', #69360 ) ;
#16308=AXIS2_PLACEMENT_3D ( 'NONE', #57713, #9281, #31220 ) ;
#16309=VECTOR ( 'NONE', #26302, 1000.000000000000000 ) ;
#16313=EDGE_CURVE ( 'NONE', #37811, #48332, #47099, .T. ) ;
#16314=VERTEX_POINT ( 'NONE', #68672 ) ;
#16323=VECTOR ( 'NONE', #51319, 1000.000000000000000 ) ;
#16326=DIRECTION ( 'NONE',  ( 0.000000000000000000, -1.000000000000000000, 2.854859206170826497E-12 ) ) ;
#16329=FACE_BOUND ( 'NONE', #12225, .T. ) ;
#16336=ORIENTED_EDGE ( 'NONE', *, *, #13643, .T. ) ;
#16341=CARTESIAN_POINT ( 'NONE',  ( 11.00000000000000000, -14.04000000000000092, -17.04524521594300523 ) ) ;
#16345=ORIENTED_EDGE ( 'NONE', *, *, #21587, .T. ) ;
#16349=CARTESIAN_POINT ( 'NONE',  ( 15.50000000000000000, -1.037157890325000054, 22.50000000000000000 ) ) ;
#16350=DIRECTION ( 'NONE',  ( 0.000000000000000000, 0.000000000000000000, 1.000000000000000000 ) ) ;
#16352=CIRCLE ( 'NONE', #42343, 4.500000000000190958 ) ;
#16355=EDGE_CURVE ( 'NONE', #67088, #4595, #66063, .T. ) ;
#16358=LINE ( 'NONE', #56519, #49729 ) ;
#16361=DIRECTION ( 'NONE',  ( 0.000000000000000000, -1.000000000000000000, 0.000000000000000000 ) ) ;
#16362=ORIENTED_EDGE ( 'NONE', *, *, #48263, .F. ) ;
#16364=ORIENTED_EDGE ( 'NONE', *, *, #9407, .T. ) ;
#16365=CYLINDRICAL_SURFACE ( 'NONE', #39548, 0.3499999999999302558 ) ;
#16366=AXIS2_PLACEMENT_3D ( 'NONE', #15486, #39375, #33039 ) ;
#16367=PLANE ( 'NONE',  #62775 ) ;
#16375=CIRCLE ( 'NONE', #33332, 3.499999999999850342 ) ;
#16387=FACE_OUTER_BOUND ( 'NONE', #14965, .T. ) ;
#16388=CARTESIAN_POINT ( 'NONE',  ( -11.00000000000000000, -9.454754784057099570, -17.53999999999999915 ) ) ;
#16407=DIRECTION ( 'NONE',  ( -1.000000000000000000, 0.000000000000000000, 0.000000000000000000 ) ) ;
#16409=ORIENTED_EDGE ( 'NONE', *, *, #37463, .F. ) ;
#16414=VECTOR ( 'NONE', #54266, 1000.000000000000000 ) ;
#16417=CARTESIAN_POINT ( 'NONE',  ( 11.50000000000000000, -11.50000000000000000, -19.00000000000000000 ) ) ;
#16422=ORIENTED_EDGE ( 'NONE', *, *, #29845, .T. ) ;
#16436=ORIENTED_EDGE ( 'NONE', *, *, #47893, .F. ) ;
#16450=AXIS2_PLACEMENT_3D ( 'NONE', #44045, #1272, #50398 ) ;
#16451=CYLINDRICAL_SURFACE ( 'NONE', #66587, 4.000000000000000000 ) ;
#16452=CARTESIAN_POINT ( 'NONE',  ( -30.00000000000000000, -9.199999999999999289, -12.69999999999986073 ) ) ;
#16455=DIRECTION ( 'NONE',  ( 0.000000000000000000, -0.1111111111108840643, -0.9938079899999319178 ) ) ;
#16456=CIRCLE ( 'NONE', #5153, 0.3499999999999597877 ) ;
#16457=AXIS2_PLACEMENT_3D ( 'NONE', #21867, #4576, #69627 ) ;
#16462=ORIENTED_EDGE ( 'NONE', *, *, #980, .T. ) ;
#16464=AXIS2_PLACEMENT_3D ( 'NONE', #28922, #24325, #14053 ) ;
#16469=EDGE_CURVE ( 'NONE', #17972, #25470, #27963, .T. ) ;
#16470=ORIENTED_EDGE ( 'NONE', *, *, #27800, .T. ) ;
#16480=EDGE_CURVE ( 'NONE', #20953, #7495, #1095, .T. ) ;
#16488=AXIS2_PLACEMENT_3D ( 'NONE', #51779, #2628, #23848 ) ;
#16489=CARTESIAN_POINT ( 'NONE',  ( -30.00000000000000000, -15.46862696659690073, -14.50000000000000000 ) ) ;
#16491=DIRECTION ( 'NONE',  ( -1.000000000000000000, 0.000000000000000000, 0.000000000000000000 ) ) ;
#16492=EDGE_LOOP ( 'NONE', ( #65045, #5562, #54377, #32769 ) ) ;
#16503=ADVANCED_FACE ( 'NONE', ( #1771, #34636 ), #35323, .T. ) ;
#16516=CARTESIAN_POINT ( 'NONE',  ( -15.50000000000000000, 0.000000000000000000, 22.50000000000000000 ) ) ;
#16517=ORIENTED_EDGE ( 'NONE', *, *, #60886, .F. ) ;
#16519=CARTESIAN_POINT ( 'NONE',  ( -30.00000000000000000, -11.85423089348099879, 9.852125413066602277 ) ) ;
#16521=DIRECTION ( 'NONE',  ( 0.000000000000000000, 0.000000000000000000, 1.000000000000000000 ) ) ;
#16523=DIRECTION ( 'NONE',  ( 0.000000000000000000, -1.000000000000000000, 0.000000000000000000 ) ) ;
#16524=VECTOR ( 'NONE', #39510, 1000.000000000000000 ) ;
#16531=ORIENTED_EDGE ( 'NONE', *, *, #20942, .T. ) ;
#16536=ORIENTED_EDGE ( 'NONE', *, *, #5120, .T. ) ;
#16549=LINE ( 'NONE', #11559, #45055 ) ;
#16554=EDGE_CURVE ( 'NONE', #32897, #2702, #34983, .T. ) ;
#16558=EDGE_CURVE ( 'NONE', #17972, #46144, #26398, .T. ) ;
#16562=ORIENTED_EDGE ( 'NONE', *, *, #10860, .T. ) ;
#16563=CARTESIAN_POINT ( 'NONE',  ( -29.50000000000000355, -11.50000000000100009, 15.00000000000084910 ) ) ;
#16571=ORIENTED_EDGE ( 'NONE', *, *, #18681, .T. ) ;
#16572=DIRECTION ( 'NONE',  ( 0.000000000000000000, 1.000000000000000000, 0.000000000000000000 ) ) ;
#16578=CARTESIAN_POINT ( 'NONE',  ( 30.00000000000000000, -13.54524521594299991, 17.53999999999999915 ) ) ;
#16581=DIRECTION ( 'NONE',  ( 0.000000000000000000, 0.7071067811865454633, 0.7071067811865496822 ) ) ;
#16582=VERTEX_POINT ( 'NONE', #46299 ) ;
#16585=ORIENTED_EDGE ( 'NONE', *, *, #5113, .T. ) ;
#16586=B_SPLINE_CURVE_WITH_KNOTS ( 'NONE', 3,
 ( #65002, #17582, #22217, #49438, #6290, #17926 ),
 .UNSPECIFIED., .F., .F.,
 ( 4, 2, 4 ),
 ( 0.0002380763768129734448, 0.7291065797294591366, 1.457975083082105439 ),
 .UNSPECIFIED. ) ;
#16587=DIRECTION ( 'NONE',  ( 0.000000000000000000, 0.7278708115913771204, 0.6857142857147648929 ) ) ;
#16592=EDGE_CURVE ( 'NONE', #373, #43590, #18367, .T. ) ;
#16601=CARTESIAN_POINT ( 'NONE',  ( 15.50000000000000000, -1.037157890325000054, -22.50000000000000000 ) ) ;
#16608=CARTESIAN_POINT ( 'NONE',  ( 15.50000000000000000, -17.50000000000000000, -22.50000000000000000 ) ) ;
#16610=EDGE_LOOP ( 'NONE', ( #21556, #15602, #63803, #26514, #16006, #29617, #18176, #18660, #38945, #27742, #27673, #32545, #22146, #42238, #58853, #36482, #29033, #30783, #47655, #11745 ) ) ;
#16617=DIRECTION ( 'NONE',  ( -1.000000000000000000, 0.000000000000000000, 0.000000000000000000 ) ) ;
#16627=ORIENTED_EDGE ( 'NONE', *, *, #15718, .T. ) ;
#16638=CARTESIAN_POINT ( 'NONE',  ( -14.25000000000000000, -2.500000000000000000, -23.22168783648699986 ) ) ;
#16641=CARTESIAN_POINT ( 'NONE',  ( -11.00000000000000000, -8.959999999999999076, 12.95475478405700009 ) ) ;
#16642=DIRECTION ( 'NONE',  ( 0.000000000000000000, 1.000000000000000000, -1.500535806722257514E-12 ) ) ;
#16643=EDGE_CURVE ( 'NONE', #42714, #12586, #40298, .T. ) ;
#16648=( GEOMETRIC_REPRESENTATION_CONTEXT ( 3 ) GLOBAL_UNCERTAINTY_ASSIGNED_CONTEXT ( ( #9048 ) ) GLOBAL_UNIT_ASSIGNED_CONTEXT ( ( #29858, #50723, #30223 ) ) REPRESENTATION_CONTEXT ( 'NONE', 'WORKASPACE' ) );
#16654=LINE ( 'NONE', #20900, #60031 ) ;
#16661=EDGE_LOOP ( 'NONE', ( #3820, #53255, #23229, #36490 ) ) ;
#16662=LINE ( 'NONE', #22645, #46264 ) ;
#16668=ORIENTED_EDGE ( 'NONE', *, *, #47533, .F. ) ;
#16673=VECTOR ( 'NONE', #42341, 1000.000000000000114 ) ;
#16678=DIRECTION ( 'NONE',  ( -1.000000000000000000, 0.000000000000000000, 0.000000000000000000 ) ) ;
#16688=LINE ( 'NONE', #48860, #60226 ) ;
#16690=DIRECTION ( 'NONE',  ( 0.000000000000000000, -1.000000000000000000, 6.036837696397648868E-13 ) ) ;
#16696=VERTEX_POINT ( 'NONE', #4927 ) ;
#16703=DIRECTION ( 'NONE',  ( 0.000000000000000000, 1.000000000000000000, 0.000000000000000000 ) ) ;
#16706=EDGE_LOOP ( 'NONE', ( #31787, #9427 ) ) ;
#16707=ORIENTED_EDGE ( 'NONE', *, *, #38202, .F. ) ;
#16711=CARTESIAN_POINT ( 'NONE',  ( 30.00000000000000000, -17.00000000000000000, 15.70499999999969809 ) ) ;
#16730=EDGE_CURVE ( 'NONE', #65451, #64280, #63988, .T. ) ;
#16731=LINE ( 'NONE', #6463, #33601 ) ;
#16732=ADVANCED_FACE ( 'NONE', ( #57961 ), #36395, .F. ) ;
#16733=DIRECTION ( 'NONE',  ( -0.000000000000000000, 1.000000000000000000, -0.000000000000000000 ) ) ;
#16743=ORIENTED_EDGE ( 'NONE', *, *, #24275, .F. ) ;
#16750=CARTESIAN_POINT ( 'NONE',  ( 17.24945551514599984, -15.50000000000000000, -25.53140320652400064 ) ) ;
#16758=EDGE_CURVE ( 'NONE', #27322, #5636, #41122, .T. ) ;
#16760=ORIENTED_EDGE ( 'NONE', *, *, #59966, .F. ) ;
#16761=VECTOR ( 'NONE', #34614, 1000.000000000000000 ) ;
#16764=ORIENTED_EDGE ( 'NONE', *, *, #42126, .T. ) ;
#16775=CARTESIAN_POINT ( 'NONE',  ( 14.45313394609757296, -0.2715358723599907709, -21.66103272505201005 ) ) ;
#16776=FACE_OUTER_BOUND ( 'NONE', #47588, .T. ) ;
#16782=ORIENTED_EDGE ( 'NONE', *, *, #38279, .F. ) ;
#16790=EDGE_CURVE ( 'NONE', #37085, #8763, #25282, .T. ) ;
#16794=ORIENTED_EDGE ( 'NONE', *, *, #12046, .F. ) ;
#16797=EDGE_CURVE ( 'NONE', #45889, #2965, #47707, .T. ) ;
#16807=DIRECTION ( 'NONE',  ( 0.000000000000000000, 0.7046037717862339012, -0.7096009616570518874 ) ) ;
#16809=EDGE_CURVE ( 'NONE', #48070, #67547, #5285, .T. ) ;
#16812=EDGE_CURVE ( 'NONE', #57801, #11904, #53563, .T. ) ;
#16813=CIRCLE ( 'NONE', #22466, 4.000000000000000888 ) ;
#16829=LINE ( 'NONE', #64926, #59267 ) ;
#16830=CARTESIAN_POINT ( 'NONE',  ( -15.50000000000000000, -2.500000000000000000, 23.94337567297399971 ) ) ;
#16832=CARTESIAN_POINT ( 'NONE',  ( 11.50000000000000000, -15.46862696659690073, -14.50000000000000000 ) ) ;
#16835=FACE_OUTER_BOUND ( 'NONE', #30485, .T. ) ;
#16840=VECTOR ( 'NONE', #23211, 1000.000000000000000 ) ;
#16841=ADVANCED_FACE ( 'NONE', ( #22910 ), #17253, .T. ) ;
#16848=VERTEX_POINT ( 'NONE', #60378 ) ;
#16850=CARTESIAN_POINT ( 'NONE',  ( -30.00000000000000000, -11.50000000000082068, -10.20500000000000007 ) ) ;
#16860=EDGE_CURVE ( 'NONE', #6937, #11406, #51758, .T. ) ;
#16864=LINE ( 'NONE', #27127, #30892 ) ;
#16869=EDGE_CURVE ( 'NONE', #4107, #4626, #37455, .T. ) ;
#16870=VERTEX_POINT ( 'NONE', #10924 ) ;
#16874=CARTESIAN_POINT ( 'NONE',  ( -15.50000000000000000, 0.000000000000000000, -26.50000000000000000 ) ) ;
#16876=VERTEX_POINT ( 'NONE', #5624 ) ;
#16877=ADVANCED_FACE ( 'NONE', ( #33175 ), #65368, .F. ) ;
#16885=CARTESIAN_POINT ( 'NONE',  ( -11.00000000000000000, -17.35230188589299871, -15.35019951917099945 ) ) ;
#16890=DIRECTION ( 'NONE',  ( 0.000000000000000000, 1.000000000000000000, 0.000000000000000000 ) ) ;
#16893=ORIENTED_EDGE ( 'NONE', *, *, #30659, .T. ) ;
#16902=PLANE ( 'NONE',  #24965 ) ;
#16905=DIRECTION ( 'NONE',  ( -1.000000000000000000, 0.000000000000000000, 0.000000000000000000 ) ) ;
#16906=CARTESIAN_POINT ( 'NONE',  ( 30.00000000000000000, -11.50000000000082068, 10.20500000000000007 ) ) ;
#16907=AXIS2_PLACEMENT_3D ( 'NONE', #52325, #61509, #9187 ) ;
#16913=CIRCLE ( 'NONE', #16968, 0.5000000000001362244 ) ;
#16914=CARTESIAN_POINT ( 'NONE',  ( 15.50000000000000000, -5.000000000000000000, 22.50000000000000000 ) ) ;
#16943=ADVANCED_FACE ( 'NONE', ( #2383 ), #45156, .T. ) ;
#16947=AXIS2_PLACEMENT_3D ( 'NONE', #69469, #68775, #3721 ) ;
#16948=EDGE_LOOP ( 'NONE', ( #60126, #22786, #4468, #65748 ) ) ;
#16951=LINE ( 'NONE', #65731, #33789 ) ;
#16953=CIRCLE ( 'NONE', #43038, 0.5000000000079367624 ) ;
#16962=ORIENTED_EDGE ( 'NONE', *, *, #15445, .F. ) ;
#16968=AXIS2_PLACEMENT_3D ( 'NONE', #51714, #67971, #30141 ) ;
#16970=ORIENTED_EDGE ( 'NONE', *, *, #40632, .F. ) ;
#16974=CARTESIAN_POINT ( 'NONE',  ( 24.00000000000000000, -17.50000000000000000, -15.70500000000000007 ) ) ;
#16976=FACE_OUTER_BOUND ( 'NONE', #13171, .T. ) ;
#16977=LINE ( 'NONE', #56874, #44745 ) ;
#16984=EDGE_CURVE ( 'NONE', #21951, #17134, #18635, .T. ) ;
#16988=CARTESIAN_POINT ( 'NONE',  ( 29.50000000000000355, -11.50000000000000000, 11.00000000000000000 ) ) ;
#16990=CARTESIAN_POINT ( 'NONE',  ( -16.75000000000000000, -0.2038245569916330158, -23.22168783648699986 ) ) ;
#17003=VECTOR ( 'NONE', #3709, 1000.000000000000000 ) ;
#17004=DIRECTION ( 'NONE',  ( 0.000000000000000000, 1.000000000000000000, 0.000000000000000000 ) ) ;
#17008=ORIENTED_EDGE ( 'NONE', *, *, #14793, .F. ) ;
#17012=CARTESIAN_POINT ( 'NONE',  ( -16.89194109070750116, -5.000000000000000000, 26.25000000000000000 ) ) ;
#17028=ADVANCED_FACE ( 'NONE', ( #40556 ), #62118, .F. ) ;
#17029=CARTESIAN_POINT ( 'NONE',  ( 28.00000000000000000, -15.50000000000000000, -20.05051025721700242 ) ) ;
#17031=ORIENTED_EDGE ( 'NONE', *, *, #27655, .T. ) ;
#17036=DIRECTION ( 'NONE',  ( 0.000000000000000000, 0.000000000000000000, 1.000000000000000000 ) ) ;
#17045=CARTESIAN_POINT ( 'NONE',  ( 24.00000000000000000, -17.50000000000000000, 19.33772233983200195 ) ) ;
#17048=CARTESIAN_POINT ( 'NONE',  ( 15.50000000000000000, -2.500000000000000000, 23.94337567297399971 ) ) ;
#17058=ORIENTED_EDGE ( 'NONE', *, *, #2611, .T. ) ;
#17065=EDGE_CURVE ( 'NONE', #59731, #9744, #15101, .T. ) ;
#17067=EDGE_LOOP ( 'NONE', ( #65601, #16794, #50583, #27116 ) ) ;
#17071=LINE ( 'NONE', #11748, #31204 ) ;
#17082=CARTESIAN_POINT ( 'NONE',  ( -11.00000000000000000, -17.00000000000000000, -15.70499999999969809 ) ) ;
#17087=CARTESIAN_POINT ( 'NONE',  ( 29.50000000000000355, -11.50000000000000000, 15.00000000000000000 ) ) ;
#17101=DIRECTION ( 'NONE',  ( 0.000000000000000000, 0.000000000000000000, -1.000000000000000000 ) ) ;
#17106=VECTOR ( 'NONE', #7090, 1000.000000000000000 ) ;
#17109=EDGE_CURVE ( 'NONE', #38679, #10292, #21954, .T. ) ;
#17115=CARTESIAN_POINT ( 'NONE',  ( -11.00000000000000000, -5.599999999999999645, -27.00000000000000000 ) ) ;
#17122=FACE_OUTER_BOUND ( 'NONE', #15242, .T. ) ;
#17125=EDGE_CURVE ( 'NONE', #26101, #1993, #13717, .T. ) ;
#17126=DIRECTION ( 'NONE',  ( -1.000000000000000000, 0.000000000000000000, 0.000000000000000000 ) ) ;
#17127=( NAMED_UNIT ( * ) PLANE_ANGLE_UNIT ( ) SI_UNIT ( $, .RADIAN. ) );
#17129=ORIENTED_EDGE ( 'NONE', *, *, #57412, .F. ) ;
#17134=VERTEX_POINT ( 'NONE', #46907 ) ;
#17137=DIRECTION ( 'NONE',  ( 0.000000000000000000, 1.000000000000000000, 0.000000000000000000 ) ) ;
#17154=LINE ( 'NONE', #22479, #67309 ) ;
#17160=DIRECTION ( 'NONE',  ( 0.000000000000000000, 0.000000000000000000, 1.000000000000000000 ) ) ;
#17168=CARTESIAN_POINT ( 'NONE',  ( -30.00000000000000000, -11.50000000000100009, -19.50000000000103739 ) ) ;
#17171=CARTESIAN_POINT ( 'NONE',  ( -11.00000000000000000, -12.00000000000000000, -11.03137303340310282 ) ) ;
#17172=CARTESIAN_POINT ( 'NONE',  ( 25.50000000000000355, 0.000000000000000000, 24.12099999999999866 ) ) ;
#17180=LINE ( 'NONE', #948, #12492 ) ;
#17186=DIRECTION ( 'NONE',  ( 0.000000000000000000, 0.000000000000000000, 1.000000000000000000 ) ) ;
#17192=CARTESIAN_POINT ( 'NONE',  ( 30.00000000000000000, -16.28999999999999915, -14.50000000000000000 ) ) ;
#17203=ORIENTED_EDGE ( 'NONE', *, *, #30536, .T. ) ;
#17212=FACE_OUTER_BOUND ( 'NONE', #33667, .T. ) ;
#17218=ORIENTED_EDGE ( 'NONE', *, *, #48686, .T. ) ;
#17227=DIRECTION ( 'NONE',  ( 0.000000000000000000, -1.000000000000000000, 0.000000000000000000 ) ) ;
#17232=FACE_OUTER_BOUND ( 'NONE', #31836, .T. ) ;
#17236=DIRECTION ( 'NONE',  ( 0.000000000000000000, 0.7046037717862339012, -0.7096009616570518874 ) ) ;
#17237=EDGE_CURVE ( 'NONE', #4729, #55345, #12883, .T. ) ;
#17239=ORIENTED_EDGE ( 'NONE', *, *, #4549, .F. ) ;
#17242=CARTESIAN_POINT ( 'NONE',  ( 25.50000000000000355, 0.000000000000000000, 22.50000000000000000 ) ) ;
#17249=ADVANCED_FACE ( 'NONE', ( #5192 ), #38408, .T. ) ;
#17253=CYLINDRICAL_SURFACE ( 'NONE', #50152, 4.000000000000000000 ) ;
#17254=CARTESIAN_POINT ( 'NONE',  ( -14.10805890929250239, -5.000000000000000000, -26.25000000000000000 ) ) ;
#17273=DIRECTION ( 'NONE',  ( 0.000000000000000000, 1.000000000000000000, 0.000000000000000000 ) ) ;
#17278=DIRECTION ( 'NONE',  ( 1.000000000000000000, -0.000000000000000000, -0.000000000000000000 ) ) ;
#17280=EDGE_LOOP ( 'NONE', ( #69325, #51977, #53422, #46500, #14417, #1929, #46436, #14273, #19761, #45888, #44085, #16668, #63769, #40161, #54535, #50511 ) ) ;
#17287=CARTESIAN_POINT ( 'NONE',  ( 28.00000000000000000, -16.28999999999710369, 15.00000000000794920 ) ) ;
#17297=VERTEX_POINT ( 'NONE', #37715 ) ;
#17307=AXIS2_PLACEMENT_3D ( 'NONE', #28195, #45132, #11914 ) ;
#17310=VERTEX_POINT ( 'NONE', #49704 ) ;
#17317=VERTEX_POINT ( 'NONE', #12208 ) ;
#17318=EDGE_CURVE ( 'NONE', #43516, #52725, #60993, .T. ) ;
#17320=CARTESIAN_POINT ( 'NONE',  ( -23.48000000000000043, -17.50000000000000000, -26.00000000000000355 ) ) ;
#17321=EDGE_CURVE ( 'NONE', #55345, #50247, #45785, .T. ) ;
#17323=DIRECTION ( 'NONE',  ( 0.000000000000000000, -0.9938079899998859545, 0.1111111111112941946 ) ) ;
#17337=DIRECTION ( 'NONE',  ( -1.000000000000000000, 0.000000000000000000, 0.000000000000000000 ) ) ;
#17340=EDGE_CURVE ( 'NONE', #39153, #59373, #39098, .T. ) ;
#17349=ORIENTED_EDGE ( 'NONE', *, *, #58388, .T. ) ;
#17368=DIRECTION ( 'NONE',  ( 0.000000000000000000, -0.9938079899998859545, 0.1111111111112941946 ) ) ;
#17374=ORIENTED_EDGE ( 'NONE', *, *, #13891, .T. ) ;
#17379=FACE_OUTER_BOUND ( 'NONE', #12305, .T. ) ;
#17380=DIRECTION ( 'NONE',  ( 1.000000000000000000, -0.000000000000000000, -0.000000000000000000 ) ) ;
#17395=AXIS2_PLACEMENT_3D ( 'NONE', #65702, #32142, #27193 ) ;
#17403=AXIS2_PLACEMENT_3D ( 'NONE', #59533, #11085, #16047 ) ;
#17412=EDGE_CURVE ( 'NONE', #41539, #66591, #7607, .T. ) ;
#17422=CIRCLE ( 'NONE', #35484, 0.3499999999999285905 ) ;
#17432=VERTEX_POINT ( 'NONE', #30239 ) ;
#17436=DIRECTION ( 'NONE',  ( 0.000000000000000000, 0.000000000000000000, 1.000000000000000000 ) ) ;
#17444=EDGE_CURVE ( 'NONE', #47285, #9687, #25638, .T. ) ;
#17454=DIRECTION ( 'NONE',  ( 0.000000000000000000, -0.9938079899998859545, 0.1111111111112941946 ) ) ;
#17458=ORIENTED_EDGE ( 'NONE', *, *, #18482, .F. ) ;
#17477=VERTEX_POINT ( 'NONE', #15018 ) ;
#17485=ORIENTED_EDGE ( 'NONE', *, *, #16643, .T. ) ;
#17488=LINE ( 'NONE', #59599, #37972 ) ;
#17490=ADVANCED_FACE ( 'NONE', ( #46832 ), #15374, .F. ) ;
#17493=AXIS2_PLACEMENT_3D ( 'NONE', #20911, #69002, #43515 ) ;
#17497=EDGE_CURVE ( 'NONE', #1158, #47752, #19709, .T. ) ;
#17500=ORIENTED_EDGE ( 'NONE', *, *, #16554, .T. ) ;
#17516=PLANE ( 'NONE',  #51889 ) ;
#17517=DIRECTION ( 'NONE',  ( 1.000000000000000000, -0.000000000000000000, -0.000000000000000000 ) ) ;
#17518=AXIS2_PLACEMENT_3D ( 'NONE', #29412, #61575, #13148 ) ;
#17530=ORIENTED_EDGE ( 'NONE', *, *, #21595, .F. ) ;
#17539=DIRECTION ( 'NONE',  ( -0.8660254037844482555, 0.000000000000000000, -0.4999999999999831801 ) ) ;
#17542=CARTESIAN_POINT ( 'NONE',  ( 30.00000000000000000, -16.28999999999710369, 15.00000000000794920 ) ) ;
#17546=ORIENTED_EDGE ( 'NONE', *, *, #46633, .F. ) ;
#17548=CARTESIAN_POINT ( 'NONE',  ( 17.51999999999999957, -15.50000000000000000, 26.00000000000000355 ) ) ;
#17549=LINE ( 'NONE', #59992, #27712 ) ;
#17555=VERTEX_POINT ( 'NONE', #35514 ) ;
#17559=CARTESIAN_POINT ( 'NONE',  ( 30.00000000000000000, -11.70000000000000284, 12.50000000000000000 ) ) ;
#17569=LINE ( 'NONE', #44777, #61965 ) ;
#17572=EDGE_CURVE ( 'NONE', #2931, #51393, #36738, .T. ) ;
#17574=VECTOR ( 'NONE', #60635, 1000.000000000000000 ) ;
#17582=CARTESIAN_POINT ( 'NONE',  ( -15.70313394609756585, -0.2715358723600081459, 21.17390376548697262 ) ) ;
#17599=VECTOR ( 'NONE', #51652, 1000.000000000000000 ) ;
#17600=LINE ( 'NONE', #54066, #66990 ) ;
#17602=CARTESIAN_POINT ( 'NONE',  ( -11.00000000000000000, -14.04000000000000092, 14.80000000000000071 ) ) ;
#17606=LINE ( 'NONE', #7682, #61704 ) ;
#17608=DIRECTION ( 'NONE',  ( 1.000000000000000000, 0.000000000000000000, 0.000000000000000000 ) ) ;
#17611=ORIENTED_EDGE ( 'NONE', *, *, #46640, .F. ) ;
#17616=EDGE_CURVE ( 'NONE', #35460, #58904, #14106, .T. ) ;
#17617=ORIENTED_EDGE ( 'NONE', *, *, #35341, .T. ) ;
#17618=VECTOR ( 'NONE', #42738, 1000.000000000000000 ) ;
#17621=CARTESIAN_POINT ( 'NONE',  ( 25.50000000000000355, 0.000000000000000000, -22.50000000000000000 ) ) ;
#17632=ORIENTED_EDGE ( 'NONE', *, *, #13202, .F. ) ;
#17638=VERTEX_POINT ( 'NONE', #58857 ) ;
#17642=AXIS2_PLACEMENT_3D ( 'NONE', #20320, #53908, #57797 ) ;
#17650=EDGE_CURVE ( 'NONE', #51110, #9490, #10070, .T. ) ;
#17666=ORIENTED_EDGE ( 'NONE', *, *, #33628, .T. ) ;
#17678=PLANE ( 'NONE',  #63308 ) ;
#17682=DIRECTION ( 'NONE',  ( 0.000000000000000000, 0.000000000000000000, -1.000000000000000000 ) ) ;
#17687=ORIENTED_EDGE ( 'NONE', *, *, #22054, .F. ) ;
#17689=CIRCLE ( 'NONE', #47073, 3.499999999999040323 ) ;
#17691=AXIS2_PLACEMENT_3D ( 'NONE', #11453, #54960, #60235 ) ;
#17700=AXIS2_PLACEMENT_3D ( 'NONE', #60102, #27586, #49159 ) ;
#17703=CIRCLE ( 'NONE', #41427, 0.5000000000001386669 ) ;
#17707=FACE_OUTER_BOUND ( 'NONE', #6087, .T. ) ;
#17713=AXIS2_PLACEMENT_3D ( 'NONE', #29193, #67399, #18953 ) ;
#17714=EDGE_CURVE ( 'NONE', #58012, #1031, #60225, .T. ) ;
#17719=CARTESIAN_POINT ( 'NONE',  ( 30.00000000000000000, -10.85999999999999943, 9.350000000000269651 ) ) ;
#17721=EDGE_CURVE ( 'NONE', #67547, #8948, #18470, .T. ) ;
#17734=ORIENTED_EDGE ( 'NONE', *, *, #6868, .F. ) ;
#17735=EDGE_LOOP ( 'NONE', ( #62653, #52151, #19919, #43200 ) ) ;
#17744=DIRECTION ( 'NONE',  ( -1.000000000000000000, 0.000000000000000000, 0.000000000000000000 ) ) ;
#17751=EDGE_LOOP ( 'NONE', ( #60511, #8262, #35100, #7517 ) ) ;
#17753=CIRCLE ( 'NONE', #30174, 0.5000000000079362072 ) ;
#17762=CONICAL_SURFACE ( 'NONE', #8726, 1.621000000000000885, 0.7853981633974518317 ) ;
#17763=DIRECTION ( 'NONE',  ( 0.000000000000000000, 0.000000000000000000, 1.000000000000000000 ) ) ;
#17769=DIRECTION ( 'NONE',  ( 1.000000000000000000, -0.000000000000000000, -0.000000000000000000 ) ) ;
#17772=VERTEX_POINT ( 'NONE', #49958 ) ;
#17780=ORIENTED_EDGE ( 'NONE', *, *, #60881, .F. ) ;
#17781=PLANE ( 'NONE',  #8754 ) ;
#17785=CARTESIAN_POINT ( 'NONE',  ( 25.50000000000000355, -15.50000000000000000, 22.50000000000000000 ) ) ;
#17789=FACE_BOUND ( 'NONE', #63864, .T. ) ;
#17791=DIRECTION ( 'NONE',  ( 0.000000000000000000, 1.000000000000000000, 0.000000000000000000 ) ) ;
#17801=EDGE_CURVE ( 'NONE', #23311, #2132, #38673, .T. ) ;
#17808=EDGE_CURVE ( 'NONE', #5431, #58583, #7524, .T. ) ;
#17813=ADVANCED_FACE ( 'NONE', ( #12471, #1520 ), #66235, .F. ) ;
#17814=ORIENTED_EDGE ( 'NONE', *, *, #12368, .F. ) ;
#17818=CARTESIAN_POINT ( 'NONE',  ( -11.75000000000000000, -5.000000000000000000, 21.10805890929250239 ) ) ;
#17822=CARTESIAN_POINT ( 'NONE',  ( -25.50000000000000355, 0.000000000000000000, 22.50000000000000000 ) ) ;
#17829=DIRECTION ( 'NONE',  ( 0.000000000000000000, -5.800915303574361727E-12, 1.000000000000000000 ) ) ;
#17840=VECTOR ( 'NONE', #1777, 1000.000000000000000 ) ;
#17855=EDGE_CURVE ( 'NONE', #2815, #24537, #51354, .T. ) ;
#17857=CARTESIAN_POINT ( 'NONE',  ( -30.00000000000000000, 0.000000000000000000, -27.00000000000000000 ) ) ;
#17864=DIRECTION ( 'NONE',  ( 0.000000000000000000, 0.7046037717862339012, -0.7096009616570518874 ) ) ;
#17868=CARTESIAN_POINT ( 'NONE',  ( 24.00000000000000000, -16.28999999999999915, 14.50000000000000000 ) ) ;
#17885=ORIENTED_EDGE ( 'NONE', *, *, #13674, .F. ) ;
#17889=DIRECTION ( 'NONE',  ( 0.000000000000000000, 0.000000000000000000, 1.000000000000000000 ) ) ;
#17890=EDGE_CURVE ( 'NONE', #6488, #54299, #19883, .T. ) ;
#17891=EDGE_CURVE ( 'NONE', #5599, #43126, #8917, .T. ) ;
#17894=CYLINDRICAL_SURFACE ( 'NONE', #7780, 0.3499999999999614531 ) ;
#17921=EDGE_CURVE ( 'NONE', #57822, #64699, #14579, .T. ) ;
#17923=EDGE_CURVE ( 'NONE', #31847, #59233, #27697, .T. ) ;
#17926=CARTESIAN_POINT ( 'NONE',  ( -16.75000000000000000, -0.2038245569916330158, 21.77831216351300014 ) ) ;
#17931=DIRECTION ( 'NONE',  ( 0.000000000000000000, 0.000000000000000000, 1.000000000000000000 ) ) ;
#17936=FACE_BOUND ( 'NONE', #29030, .T. ) ;
#17948=EDGE_CURVE ( 'NONE', #59852, #34424, #61583, .T. ) ;
#17955=EDGE_LOOP ( 'NONE', ( #45350, #48731, #26799, #68399 ) ) ;
#17956=DIRECTION ( 'NONE',  ( 1.000000000000000000, -0.000000000000000000, -0.000000000000000000 ) ) ;
#17965=ORIENTED_EDGE ( 'NONE', *, *, #13885, .F. ) ;
#17971=EDGE_CURVE ( 'NONE', #51926, #62351, #8501, .T. ) ;
#17972=VERTEX_POINT ( 'NONE', #25554 ) ;
#17995=ORIENTED_EDGE ( 'NONE', *, *, #6722, .F. ) ;
#18002=DIRECTION ( 'NONE',  ( 0.000000000000000000, 1.000000000000000000, 0.000000000000000000 ) ) ;
#18008=LINE ( 'NONE', #49166, #53963 ) ;
#18011=DIRECTION ( 'NONE',  ( -0.7142857142857395036, 0.000000000000000000, -0.6998542122237394469 ) ) ;
#18013=LINE ( 'NONE', #30026, #12698 ) ;
#18016=DIRECTION ( 'NONE',  ( -1.000000000000000000, 0.000000000000000000, 0.000000000000000000 ) ) ;
#18022=DIRECTION ( 'NONE',  ( 1.000000000000000000, -0.000000000000000000, -0.000000000000000000 ) ) ;
#18025=DIRECTION ( 'NONE',  ( -1.000000000000000000, 0.000000000000000000, 0.000000000000000000 ) ) ;
#18026=CARTESIAN_POINT ( 'NONE',  ( -11.50000000000000000, -12.00000000000000000, 11.00000000000000000 ) ) ;
#18032=DIRECTION ( 'NONE',  ( 0.000000000000000000, 0.000000000000000000, -1.000000000000000000 ) ) ;
#18037=VERTEX_POINT ( 'NONE', #20581 ) ;
#18041=ORIENTED_EDGE ( 'NONE', *, *, #24197, .T. ) ;
#18043=CARTESIAN_POINT ( 'NONE',  ( -16.75000000000000000, -2.500000000000000000, -23.22168783648699986 ) ) ;
#18050=CIRCLE ( 'NONE', #27109, 4.000000000000000888 ) ;
#18051=CARTESIAN_POINT ( 'NONE',  ( -11.50000000000000000, -15.46862696659690073, 14.50000000000000000 ) ) ;
#18052=ORIENTED_EDGE ( 'NONE', *, *, #56447, .F. ) ;
#18054=DIRECTION ( 'NONE',  ( 0.000000000000000000, 0.7071067811865495711, 0.7071067811865455743 ) ) ;
#18059=VECTOR ( 'NONE', #44615, 1000.000000000000000 ) ;
#18063=VERTEX_POINT ( 'NONE', #38171 ) ;
#18065=VERTEX_POINT ( 'NONE', #9990 ) ;
#18068=EDGE_CURVE ( 'NONE', #11057, #17477, #30004, .T. ) ;
#18069=DIRECTION ( 'NONE',  ( 0.000000000000000000, 0.000000000000000000, 1.000000000000000000 ) ) ;
#18083=CONICAL_SURFACE ( 'NONE', #50841, 2.000000000000001776, 0.7853981633974503884 ) ;
#18102=DIRECTION ( 'NONE',  ( -0.000000000000000000, 1.000000000000000000, -0.000000000000000000 ) ) ;
#18112=EDGE_CURVE ( 'NONE', #25346, #2156, #39185, .T. ) ;
#18113=ORIENTED_EDGE ( 'NONE', *, *, #23779, .F. ) ;
#18119=ORIENTED_EDGE ( 'NONE', *, *, #17444, .T. ) ;
#18120=AXIS2_PLACEMENT_3D ( 'NONE', #59839, #5426, #26981 ) ;
#18125=EDGE_CURVE ( 'NONE', #49745, #51892, #50137, .T. ) ;
#18126=DIRECTION ( 'NONE',  ( 0.000000000000000000, 0.000000000000000000, 1.000000000000000000 ) ) ;
#18130=ADVANCED_FACE ( 'NONE', ( #44823 ), #34204, .T. ) ;
#18132=DIRECTION ( 'NONE',  ( -1.000000000000000000, 0.000000000000000000, 0.000000000000000000 ) ) ;
#18138=EDGE_CURVE ( 'NONE', #20091, #36899, #13356, .T. ) ;
#18153=EDGE_CURVE ( 'NONE', #4089, #29817, #55792, .T. ) ;
#18159=ORIENTED_EDGE ( 'NONE', *, *, #14066, .F. ) ;
#18166=ORIENTED_EDGE ( 'NONE', *, *, #20103, .T. ) ;
#18176=ORIENTED_EDGE ( 'NONE', *, *, #64061, .F. ) ;
#18191=EDGE_CURVE ( 'NONE', #45736, #38019, #37904, .T. ) ;
#18194=EDGE_CURVE ( 'NONE', #35617, #57481, #40919, .T. ) ;
#18197=VECTOR ( 'NONE', #45101, 1000.000000000000000 ) ;
#18201=EDGE_CURVE ( 'NONE', #22677, #2326, #39521, .T. ) ;
#18209=VECTOR ( 'NONE', #12448, 1000.000000000000000 ) ;
#18211=LINE ( 'NONE', #39768, #56744 ) ;
#18216=DIRECTION ( 'NONE',  ( -0.8660254037844485886, 0.000000000000000000, -0.4999999999999827360 ) ) ;
#18223=CARTESIAN_POINT ( 'NONE',  ( -11.50000000000000000, -15.97213595500069871, -14.50000000000000000 ) ) ;
#18224=ORIENTED_EDGE ( 'NONE', *, *, #6431, .T. ) ;
#18231=AXIS2_PLACEMENT_3D ( 'NONE', #59079, #49169, #21264 ) ;
#18235=EDGE_CURVE ( 'NONE', #44371, #30033, #66743, .T. ) ;
#18242=ORIENTED_EDGE ( 'NONE', *, *, #23443, .F. ) ;
#18247=ORIENTED_EDGE ( 'NONE', *, *, #1113, .T. ) ;
#18251=ORIENTED_EDGE ( 'NONE', *, *, #24047, .F. ) ;
#18258=DIRECTION ( 'NONE',  ( 0.000000000000000000, 0.000000000000000000, 1.000000000000000000 ) ) ;
#18271=ORIENTED_EDGE ( 'NONE', *, *, #15469, .F. ) ;
#18274=CYLINDRICAL_SURFACE ( 'NONE', #46316, 0.5000000000079367624 ) ;
#18275=VECTOR ( 'NONE', #62537, 1000.000000000000000 ) ;
#18278=EDGE_CURVE ( 'NONE', #60747, #61956, #69555, .T. ) ;
#18279=CARTESIAN_POINT ( 'NONE',  ( 16.75000000000000000, -2.500000000000000000, 21.77831216351300014 ) ) ;
#18287=CARTESIAN_POINT ( 'NONE',  ( -25.50000000000000355, -15.50000000000000000, -22.50000000000000000 ) ) ;
#18289=DIRECTION ( 'NONE',  ( 0.000000000000000000, -0.7071067811865460184, -0.7071067811865489050 ) ) ;
#18300=CARTESIAN_POINT ( 'NONE',  ( 11.50000000000000000, -11.50000000000100009, -10.50000000000065903 ) ) ;
#18305=ORIENTED_EDGE ( 'NONE', *, *, #23080, .F. ) ;
#18308=ORIENTED_EDGE ( 'NONE', *, *, #1602, .F. ) ;
#18315=ADVANCED_FACE ( 'NONE', ( #58247 ), #46924, .F. ) ;
#18344=CARTESIAN_POINT ( 'NONE',  ( 15.50000000000000000, -0.1999999999999999556, 23.94999999999999574 ) ) ;
#18352=CARTESIAN_POINT ( 'NONE',  ( 11.00000000000000000, -17.35230188589299516, -15.35019951917100478 ) ) ;
#18354=CARTESIAN_POINT ( 'NONE',  ( 30.00000000000000000, -12.00000000000000000, 12.20000000000000107 ) ) ;
#18356=EDGE_CURVE ( 'NONE', #30792, #36191, #51622, .T. ) ;
#18360=CARTESIAN_POINT ( 'NONE',  ( -11.00000000000000000, -5.200000000000001066, -26.59999999999999787 ) ) ;
#18362=EDGE_CURVE ( 'NONE', #30827, #64746, #63905, .T. ) ;
#18364=PLANE ( 'NONE',  #51025 ) ;
#18367=LINE ( 'NONE', #39929, #13966 ) ;
#18368=DIRECTION ( 'NONE',  ( -1.000000000000000000, 0.000000000000000000, 0.000000000000000000 ) ) ;
#18372=PLANE ( 'NONE',  #69607 ) ;
#18375=ADVANCED_FACE ( 'NONE', ( #8753 ), #20064, .F. ) ;
#18384=CARTESIAN_POINT ( 'NONE',  ( 30.00000000000000000, -5.599999999999999645, -9.000000000000001776 ) ) ;
#18387=FACE_OUTER_BOUND ( 'NONE', #21157, .T. ) ;
#18389=ORIENTED_EDGE ( 'NONE', *, *, #36402, .T. ) ;
#18390=CARTESIAN_POINT ( 'NONE',  ( 30.00000000000000000, -16.28999999999710369, 15.00000000000794920 ) ) ;
#18391=EDGE_LOOP ( 'NONE', ( #8959, #47874 ) ) ;
#18400=VECTOR ( 'NONE', #29956, 1000.000000000000000 ) ;
#18401=ORIENTED_EDGE ( 'NONE', *, *, #24803, .T. ) ;
#18406=EDGE_CURVE ( 'NONE', #47285, #55064, #4165, .T. ) ;
#18409=FACE_OUTER_BOUND ( 'NONE', #14000, .T. ) ;
#18415=CYLINDRICAL_SURFACE ( 'NONE', #2912, 0.3500000000009988455 ) ;
#18419=CARTESIAN_POINT ( 'NONE',  ( -11.00000000000000000, -5.200000000000001066, 60.00000000000000000 ) ) ;
#18428=EDGE_LOOP ( 'NONE', ( #55471, #55284, #15638, #34315, #8905, #55779, #46581 ) ) ;
#18429=ORIENTED_EDGE ( 'NONE', *, *, #24047, .T. ) ;
#18430=DIRECTION ( 'NONE',  ( 0.000000000000000000, 1.000000000000000000, 0.000000000000000000 ) ) ;
#18432=DIRECTION ( 'NONE',  ( 0.000000000000000000, 0.000000000000000000, 1.000000000000000000 ) ) ;
#18435=DIRECTION ( 'NONE',  ( 0.000000000000000000, 1.000000000000000000, 0.000000000000000000 ) ) ;
#18436=CARTESIAN_POINT ( 'NONE',  ( -30.00000000000000000, -17.14999999999999858, -27.00000000000000000 ) ) ;
#18441=ORIENTED_EDGE ( 'NONE', *, *, #12560, .T. ) ;
#18455=EDGE_LOOP ( 'NONE', ( #38775, #5088, #6714, #62563 ) ) ;
#18470=LINE ( 'NONE', #55968, #33349 ) ;
#18471=EDGE_CURVE ( 'NONE', #35907, #60253, #65631, .T. ) ;
#18474=ORIENTED_EDGE ( 'NONE', *, *, #4275, .F. ) ;
#18475=EDGE_LOOP ( 'NONE', ( #36146, #24501, #34778, #25885 ) ) ;
#18476=CARTESIAN_POINT ( 'NONE',  ( -28.00000000000000000, -17.50000000000000000, 15.70499999999969809 ) ) ;
#18479=DIRECTION ( 'NONE',  ( -1.000000000000000000, 0.000000000000000000, 0.000000000000000000 ) ) ;
#18482=EDGE_CURVE ( 'NONE', #34056, #4079, #33457, .T. ) ;
#18488=VERTEX_POINT ( 'NONE', #64594 ) ;
#18489=ORIENTED_EDGE ( 'NONE', *, *, #66694, .T. ) ;
#18490=EDGE_CURVE ( 'NONE', #69553, #52350, #28148, .T. ) ;
#18491=ORIENTED_EDGE ( 'NONE', *, *, #57412, .T. ) ;
#18493=DIRECTION ( 'NONE',  ( 0.000000000000000000, 0.000000000000000000, 1.000000000000000000 ) ) ;
#18496=AXIS2_PLACEMENT_3D ( 'NONE', #6310, #48754, #43432 ) ;
#18497=CIRCLE ( 'NONE', #54663, 2.250000000000001776 ) ;
#18498=LINE ( 'NONE', #14267, #44545 ) ;
#18499=ORIENTED_EDGE ( 'NONE', *, *, #14551, .F. ) ;
#18502=EDGE_CURVE ( 'NONE', #27132, #62471, #60541, .T. ) ;
#18503=CARTESIAN_POINT ( 'NONE',  ( -15.50000000000000000, -0.4000000000005236034, -22.50000000000000000 ) ) ;
#18504=VERTEX_POINT ( 'NONE', #16155 ) ;
#18511=DIRECTION ( 'NONE',  ( 0.000000000000000000, -0.9921567416492215186, 0.1249999999999996531 ) ) ;
#18520=EDGE_CURVE ( 'NONE', #61558, #611, #36850, .T. ) ;
#18530=DIRECTION ( 'NONE',  ( -1.000000000000000000, 0.000000000000000000, 0.000000000000000000 ) ) ;
#18546=FILL_AREA_STYLE ('',( #51076 ) ) ;
#18556=CARTESIAN_POINT ( 'NONE',  ( -11.50000000000000000, -15.97213595500069871, 14.50000000000000000 ) ) ;
#18557=DIRECTION ( 'NONE',  ( 1.000000000000000000, -0.000000000000000000, 1.224646799147353207E-16 ) ) ;
#18559=AXIS2_PLACEMENT_3D ( 'NONE', #48510, #6072, #65132 ) ;
#18561=CARTESIAN_POINT ( 'NONE',  ( -15.50000000000000000, -0.2038245569916614930, -21.05662432702600029 ) ) ;
#18570=LINE ( 'NONE', #24593, #62048 ) ;
#18571=DIRECTION ( 'NONE',  ( 0.000000000000000000, -0.7046037717806115097, -0.7096009616626348659 ) ) ;
#18572=VECTOR ( 'NONE', #30105, 1000.000000000000000 ) ;
#18573=ORIENTED_EDGE ( 'NONE', *, *, #66026, .T. ) ;
#18587=EDGE_CURVE ( 'NONE', #67830, #48298, #8546, .T. ) ;
#18589=FACE_OUTER_BOUND ( 'NONE', #39256, .T. ) ;
#18600=CIRCLE ( 'NONE', #20889, 1.620999999999997332 ) ;
#18603=VERTEX_POINT ( 'NONE', #29177 ) ;
#18610=DIRECTION ( 'NONE',  ( 0.000000000000000000, 1.000000000000000000, 0.000000000000000000 ) ) ;
#18615=FACE_OUTER_BOUND ( 'NONE', #20131, .T. ) ;
#18624=ORIENTED_EDGE ( 'NONE', *, *, #32522, .F. ) ;
#18628=DIRECTION ( 'NONE',  ( 1.000000000000000000, 0.000000000000000000, 0.000000000000000000 ) ) ;
#18632=LINE ( 'NONE', #8369, #4811 ) ;
#18633=LINE ( 'NONE', #23944, #63637 ) ;
#18635=LINE ( 'NONE', #17602, #34289 ) ;
#18641=DIRECTION ( 'NONE',  ( 0.000000000000000000, 0.000000000000000000, 1.000000000000000000 ) ) ;
#18642=AXIS2_PLACEMENT_3D ( 'NONE', #32147, #4588, #20833 ) ;
#18651=ORIENTED_EDGE ( 'NONE', *, *, #53137, .T. ) ;
#18652=FACE_OUTER_BOUND ( 'NONE', #59484, .T. ) ;
#18654=AXIS2_PLACEMENT_3D ( 'NONE', #39026, #23103, #17454 ) ;
#18660=ORIENTED_EDGE ( 'NONE', *, *, #13643, .F. ) ;
#18661=CARTESIAN_POINT ( 'NONE',  ( 11.00000000000000000, -16.28999999999710369, -15.00000000000794920 ) ) ;
#18662=VERTEX_POINT ( 'NONE', #18223 ) ;
#18671=EDGE_CURVE ( 'NONE', #29287, #12416, #15385, .T. ) ;
#18673=DIRECTION ( 'NONE',  ( 0.000000000000000000, 0.000000000000000000, -1.000000000000000000 ) ) ;
#18675=ORIENTED_EDGE ( 'NONE', *, *, #434, .F. ) ;
#18681=EDGE_CURVE ( 'NONE', #51393, #47121, #8674, .T. ) ;
#18685=CARTESIAN_POINT ( 'NONE',  ( 11.50000000000000000, -11.50000000000100009, 15.00000000000084910 ) ) ;
#18688=EDGE_LOOP ( 'NONE', ( #3855, #45195 ) ) ;
#18692=LINE ( 'NONE', #7378, #27806 ) ;
#18695=FACE_OUTER_BOUND ( 'NONE', #16086, .T. ) ;
#18697=VECTOR ( 'NONE', #56396, 1000.000000000000114 ) ;
#18699=ORIENTED_EDGE ( 'NONE', *, *, #26840, .T. ) ;
#18700=VECTOR ( 'NONE', #21680, 1000.000000000000000 ) ;
#18701=CIRCLE ( 'NONE', #37915, 0.3499999999999597877 ) ;
#18703=DIRECTION ( 'NONE',  ( 0.000000000000000000, 1.000000000000000000, 0.000000000000000000 ) ) ;
#18711=AXIS2_PLACEMENT_3D ( 'NONE', #15224, #15916, #47389 ) ;
#18720=DIRECTION ( 'NONE',  ( 0.000000000000000000, 0.000000000000000000, 1.000000000000000000 ) ) ;
#18721=CARTESIAN_POINT ( 'NONE',  ( -30.00000000000000000, -9.487228132326899654, 12.50000000000000000 ) ) ;
#18730=VERTEX_POINT ( 'NONE', #24934 ) ;
#18733=EDGE_CURVE ( 'NONE', #35825, #66963, #9730, .T. ) ;
#18734=ORIENTED_EDGE ( 'NONE', *, *, #18406, .F. ) ;
#18735=DIRECTION ( 'NONE',  ( 1.000000000000000000, -0.000000000000000000, -0.000000000000000000 ) ) ;
#18753=CARTESIAN_POINT ( 'NONE',  ( 30.00000000000000000, -13.79999999999979998, 17.30000000000000071 ) ) ;
#18754=VERTEX_POINT ( 'NONE', #20332 ) ;
#18758=CIRCLE ( 'NONE', #65068, 1.449999999999996403 ) ;
#18761=DIRECTION ( 'NONE',  ( 0.7142857142857395036, 0.000000000000000000, 0.6998542122237394469 ) ) ;
#18767=DIRECTION ( 'NONE',  ( -1.000000000000000000, 0.000000000000000000, 0.000000000000000000 ) ) ;
#18768=DIRECTION ( 'NONE',  ( 1.000000000000000000, -0.000000000000000000, -0.000000000000000000 ) ) ;
#18772=ORIENTED_EDGE ( 'NONE', *, *, #22436, .T. ) ;
#18780=VERTEX_POINT ( 'NONE', #36588 ) ;
#18781=ORIENTED_EDGE ( 'NONE', *, *, #24183, .T. ) ;
#18785=VERTEX_POINT ( 'NONE', #69120 ) ;
#18796=DIRECTION ( 'NONE',  ( -1.000000000000000000, 0.000000000000000000, 0.000000000000000000 ) ) ;
#18798=DIRECTION ( 'NONE',  ( 0.000000000000000000, 0.000000000000000000, -1.000000000000000000 ) ) ;
#18803=CARTESIAN_POINT ( 'NONE',  ( -30.00000000000000000, -17.00000000000000000, 15.70499999999969809 ) ) ;
#18811=CARTESIAN_POINT ( 'NONE',  ( 30.00000000000000000, -5.000000000000000000, 27.00000000000000000 ) ) ;
#18821=ORIENTED_EDGE ( 'NONE', *, *, #50061, .T. ) ;
#18837=CARTESIAN_POINT ( 'NONE',  ( 30.00000000000000000, -8.959999999999999076, 12.95475478405700009 ) ) ;
#18841=VERTEX_POINT ( 'NONE', #22429 ) ;
#18844=CARTESIAN_POINT ( 'NONE',  ( 25.50000000000000355, -15.12100000000000044, -24.12099999999999511 ) ) ;
#18848=CARTESIAN_POINT ( 'NONE',  ( 11.00000000000000000, -11.70000000000000284, -12.50000000000000000 ) ) ;
#18855=VECTOR ( 'NONE', #54383, 1000.000000000000000 ) ;
#18856=ORIENTED_EDGE ( 'NONE', *, *, #8216, .T. ) ;
#18859=ADVANCED_FACE ( 'NONE', ( #5481 ), #173, .F. ) ;
#18861=AXIS2_PLACEMENT_3D ( 'NONE', #47585, #63856, #32031 ) ;
#18866=ORIENTED_EDGE ( 'NONE', *, *, #62841, .F. ) ;
#18874=ORIENTED_EDGE ( 'NONE', *, *, #9513, .F. ) ;
#18877=ORIENTED_EDGE ( 'NONE', *, *, #59440, .T. ) ;
#18884=EDGE_CURVE ( 'NONE', #10983, #62987, #48249, .T. ) ;
#18885=ORIENTED_EDGE ( 'NONE', *, *, #41589, .T. ) ;
#18894=FACE_OUTER_BOUND ( 'NONE', #55929, .T. ) ;
#18896=VERTEX_POINT ( 'NONE', #42599 ) ;
#18902=ORIENTED_EDGE ( 'NONE', *, *, #7251, .T. ) ;
#18903=CARTESIAN_POINT ( 'NONE',  ( -30.00000000000000000, -14.33999999999999986, 14.50000000000000000 ) ) ;
#18911=CARTESIAN_POINT ( 'NONE',  ( -15.50000000000000000, -0.2000000000000000111, 22.50000000000000000 ) ) ;
#18912=AXIS2_PLACEMENT_3D ( 'NONE', #60142, #11696, #6415 ) ;
#18915=ORIENTED_EDGE ( 'NONE', *, *, #991, .F. ) ;
#18918=DIRECTION ( 'NONE',  ( 0.000000000000000000, 1.000000000000000000, 0.000000000000000000 ) ) ;
#18927=CARTESIAN_POINT ( 'NONE',  ( -14.25000000000000000, -2.500000000000000000, 21.77831216351300014 ) ) ;
#18928=ADVANCED_FACE ( 'NONE', ( #27035 ), #69826, .T. ) ;
#18949=ADVANCED_FACE ( 'NONE', ( #33028 ), #48260, .F. ) ;
#18950=AXIS2_PLACEMENT_3D ( 'NONE', #17087, #48581, #5798 ) ;
#18951=ORIENTED_EDGE ( 'NONE', *, *, #42927, .T. ) ;
#18952=ORIENTED_EDGE ( 'NONE', *, *, #185, .F. ) ;
#18953=DIRECTION ( 'NONE',  ( 0.000000000000000000, 0.000000000000000000, -1.000000000000000000 ) ) ;
#18955=VERTEX_POINT ( 'NONE', #59213 ) ;
#18960=LINE ( 'NONE', #34508, #16840 ) ;
#18968=VECTOR ( 'NONE', #51927, 1000.000000000000000 ) ;
#18969=AXIS2_PLACEMENT_3D ( 'NONE', #45107, #61725, #30261 ) ;
#18972=DIRECTION ( 'NONE',  ( -1.000000000000000000, 0.000000000000000000, 0.000000000000000000 ) ) ;
#18989=LINE ( 'NONE', #56126, #59406 ) ;
#18990=CIRCLE ( 'NONE', #58544, 3.300000002979700753 ) ;
#19000=CARTESIAN_POINT ( 'NONE',  ( -29.25000000000000000, -5.200000000000001066, 26.25000000000000000 ) ) ;
#19002=LINE ( 'NONE', #1687, #1583 ) ;
#19009=DIRECTION ( 'NONE',  ( 1.060575238724893480E-16, 0.5000000000000189848, -0.8660254037844277164 ) ) ;
#19010=CARTESIAN_POINT ( 'NONE',  ( 17.00000000000000000, -15.50000000000000000, -19.33772233983200195 ) ) ;
#19012=ORIENTED_EDGE ( 'NONE', *, *, #39519, .T. ) ;
#19016=ORIENTED_EDGE ( 'NONE', *, *, #26809, .T. ) ;
#19028=DIRECTION ( 'NONE',  ( 0.000000000000000000, 1.000000000000000000, 0.000000000000000000 ) ) ;
#19052=DIRECTION ( 'NONE',  ( 1.000000000000000000, 0.000000000000000000, 0.000000000000000000 ) ) ;
#19062=VERTEX_POINT ( 'NONE', #7175 ) ;
#19066=CYLINDRICAL_SURFACE ( 'NONE', #57291, 4.000000000000000000 ) ;
#19068=AXIS2_PLACEMENT_3D ( 'NONE', #54512, #15639, #10324 ) ;
#19071=CARTESIAN_POINT ( 'NONE',  ( 11.00000000000000000, -13.79999999999979998, 17.30000000000000071 ) ) ;
#19086=LINE ( 'NONE', #24743, #65602 ) ;
#19087=EDGE_CURVE ( 'NONE', #3375, #56472, #1838, .T. ) ;
#19091=EDGE_CURVE ( 'NONE', #1819, #48505, #57021, .T. ) ;
#19096=CARTESIAN_POINT ( 'NONE',  ( 30.00000000000000000, -11.70000000000000284, -11.00000000000000000 ) ) ;
#19099=DIRECTION ( 'NONE',  ( -1.000000000000000000, 0.000000000000000000, 0.000000000000000000 ) ) ;
#19107=CONICAL_SURFACE ( 'NONE', #36018, 1.621000000000000885, 0.7853981633974518317 ) ;
#19114=CIRCLE ( 'NONE', #11190, 0.5000000000001386669 ) ;
#19118=ORIENTED_EDGE ( 'NONE', *, *, #6556, .F. ) ;
#19125=CIRCLE ( 'NONE', #7804, 0.5000000000001357803 ) ;
#19133=CARTESIAN_POINT ( 'NONE',  ( 15.50000000000000000, -2.500000000000000000, 23.94337567297399971 ) ) ;
#19135=ORIENTED_EDGE ( 'NONE', *, *, #21743, .F. ) ;
#19136=DIRECTION ( 'NONE',  ( 0.000000000000000000, 1.000000000000000000, 0.000000000000000000 ) ) ;
#19141=LINE ( 'NONE', #51315, #49747 ) ;
#19144=ORIENTED_EDGE ( 'NONE', *, *, #48799, .T. ) ;
#19149=DIRECTION ( 'NONE',  ( 0.000000000000000000, 1.000000000000000000, 0.000000000000000000 ) ) ;
#19152=ORIENTED_EDGE ( 'NONE', *, *, #48607, .T. ) ;
#19153=DIRECTION ( 'NONE',  ( 0.000000000000000000, 0.5000000000000189848, 0.8660254037844277164 ) ) ;
#19160=DIRECTION ( 'NONE',  ( -1.000000000000000000, 0.000000000000000000, 0.000000000000000000 ) ) ;
#19164=CIRCLE ( 'NONE', #58706, 2.250000000000001776 ) ;
#19166=VERTEX_POINT ( 'NONE', #24854 ) ;
#19172=EDGE_CURVE ( 'NONE', #7800, #67429, #12020, .T. ) ;
#19178=DIRECTION ( 'NONE',  ( -0.8660254037850523279, 0.000000000000000000, -0.4999999999989371835 ) ) ;
#19186=CARTESIAN_POINT ( 'NONE',  ( -30.00000000000000000, -16.64230188589299786, -14.64519951917100116 ) ) ;
#19187=ORIENTED_EDGE ( 'NONE', *, *, #48811, .F. ) ;
#19200=ORIENTED_EDGE ( 'NONE', *, *, #17125, .F. ) ;
#19212=VERTEX_POINT ( 'NONE', #16200 ) ;
#19214=AXIS2_PLACEMENT_3D ( 'NONE', #62450, #24292, #40193 ) ;
#19216=ADVANCED_FACE ( 'NONE', ( #58648 ), #51687, .T. ) ;
#19217=CARTESIAN_POINT ( 'NONE',  ( 13.00000000000000178, -16.28999999999999915, -14.50000000000000000 ) ) ;
#19220=DIRECTION ( 'NONE',  ( 1.000000000000000000, 0.000000000000000000, 0.000000000000000000 ) ) ;
#19227=VERTEX_POINT ( 'NONE', #3240 ) ;
#19228=EDGE_LOOP ( 'NONE', ( #45279, #68571, #52224, #3021 ) ) ;
#19231=LINE ( 'NONE', #13922, #6960 ) ;
#19235=ORIENTED_EDGE ( 'NONE', *, *, #5398, .T. ) ;
#19247=CARTESIAN_POINT ( 'NONE',  ( 11.00000000000000000, -10.85999999999999943, -9.000000000000001776 ) ) ;
#19253=CIRCLE ( 'NONE', #50836, 0.3999999999993817390 ) ;
#19254=CARTESIAN_POINT ( 'NONE',  ( -14.25000000000000000, -2.500000000000000000, -23.22168783648699986 ) ) ;
#19260=PLANE ( 'NONE',  #36571 ) ;
#19278=ADVANCED_FACE ( 'NONE', ( #54044 ), #43533, .T. ) ;
#19279=VECTOR ( 'NONE', #7171, 1000.000000000000000 ) ;
#19280=DIRECTION ( 'NONE',  ( 0.000000000000000000, -1.000000000000000000, 0.000000000000000000 ) ) ;
#19282=CARTESIAN_POINT ( 'NONE',  ( 25.50000000000000355, -15.12100000000000044, 22.50000000000000000 ) ) ;
#19285=ORIENTED_EDGE ( 'NONE', *, *, #61633, .T. ) ;
#19294=CARTESIAN_POINT ( 'NONE',  ( 15.91434062215687284, -0.3156604612129197962, 21.29584399676445727 ) ) ;
#19308=EDGE_CURVE ( 'NONE', #56028, #26101, #1757, .T. ) ;
#19317=CARTESIAN_POINT ( 'NONE',  ( 30.00000000000000000, -13.54524521594299991, 17.53999999999999915 ) ) ;
#19333=EDGE_CURVE ( 'NONE', #21794, #68853, #12603, .T. ) ;
#19338=CARTESIAN_POINT ( 'NONE',  ( 14.25000000000000000, -0.2038245569916330158, 23.22168783648699986 ) ) ;
#19340=ORIENTED_EDGE ( 'NONE', *, *, #7197, .T. ) ;
#19347=AXIS2_PLACEMENT_3D ( 'NONE', #41148, #20983, #9332 ) ;
#19349=ADVANCED_FACE ( 'NONE', ( #60014 ), #11563, .T. ) ;
#19353=DIRECTION ( 'NONE',  ( 0.000000000000000000, 0.000000000000000000, -1.000000000000000000 ) ) ;
#19356=CARTESIAN_POINT ( 'NONE',  ( -11.00000000000000000, -12.00000000000000000, -10.20500000000000007 ) ) ;
#19365=EDGE_LOOP ( 'NONE', ( #29343, #5789, #42875, #9276, #23476, #40914, #15294, #15569, #29198, #27690, #67492, #20700, #11029, #10105, #66456 ) ) ;
#19367=ORIENTED_EDGE ( 'NONE', *, *, #13986, .T. ) ;
#19371=ORIENTED_EDGE ( 'NONE', *, *, #60277, .T. ) ;
#19385=EDGE_CURVE ( 'NONE', #8573, #24168, #60352, .T. ) ;
#19391=EDGE_CURVE ( 'NONE', #25525, #61414, #28528, .T. ) ;
#19397=DIRECTION ( 'NONE',  ( 0.9375000000000006661, 0.000000000000000000, 0.3479852726768744020 ) ) ;
#19398=CIRCLE ( 'NONE', #66784, 1.449999999999999956 ) ;
#19400=CARTESIAN_POINT ( 'NONE',  ( 15.50000000000000000, -0.2038245569916604938, -21.05662432702600029 ) ) ;
#19402=EDGE_CURVE ( 'NONE', #37065, #22759, #27896, .T. ) ;
#19407=EDGE_CURVE ( 'NONE', #44232, #46800, #56792, .T. ) ;
#19428=AXIS2_PLACEMENT_3D ( 'NONE', #44906, #18022, #6394 ) ;
#19429=EDGE_LOOP ( 'NONE', ( #15073, #14934, #45698, #48379 ) ) ;
#19435=DIRECTION ( 'NONE',  ( 0.8660254037844482555, 0.000000000000000000, 0.4999999999999831801 ) ) ;
#19437=PLANE ( 'NONE',  #16907 ) ;
#19439=CARTESIAN_POINT ( 'NONE',  ( 30.00000000000000000, -11.50000000000100009, -15.00000000000084910 ) ) ;
#19440=ORIENTED_EDGE ( 'NONE', *, *, #15449, .T. ) ;
#19441=CARTESIAN_POINT ( 'NONE',  ( -11.00000000000000000, -14.04000000000000092, 17.04524521594300523 ) ) ;
#19448=CARTESIAN_POINT ( 'NONE',  ( 30.00000000000000000, -17.00000000000000000, -15.70499999999969809 ) ) ;
#19449=ORIENTED_EDGE ( 'NONE', *, *, #63032, .F. ) ;
#19451=PLANE ( 'NONE',  #40869 ) ;
#19453=ORIENTED_EDGE ( 'NONE', *, *, #47117, .F. ) ;
#19455=LINE ( 'NONE', #51285, #9857 ) ;
#19458=ORIENTED_EDGE ( 'NONE', *, *, #5937, .F. ) ;
#19472=ORIENTED_EDGE ( 'NONE', *, *, #63154, .F. ) ;
#19474=EDGE_CURVE ( 'NONE', #48682, #51892, #40178, .T. ) ;
#19477=EDGE_CURVE ( 'NONE', #61414, #41558, #61755, .T. ) ;
#19479=ORIENTED_EDGE ( 'NONE', *, *, #55984, .F. ) ;
#19481=DIRECTION ( 'NONE',  ( 1.000000000000000000, 0.000000000000000000, 0.000000000000000000 ) ) ;
#19486=CARTESIAN_POINT ( 'NONE',  ( 25.50000000000000355, 0.000000000000000000, 20.87899999999999778 ) ) ;
#19487=DIRECTION ( 'NONE',  ( 0.000000000000000000, 0.000000000000000000, 1.000000000000000000 ) ) ;
#19490=ORIENTED_EDGE ( 'NONE', *, *, #41195, .T. ) ;
#19492=DIRECTION ( 'NONE',  ( 0.000000000000000000, 1.000000000000000000, 0.000000000000000000 ) ) ;
#19497=EDGE_CURVE ( 'NONE', #278, #36973, #36793, .T. ) ;
#19499=LINE ( 'NONE', #24814, #21204 ) ;
#19500=VECTOR ( 'NONE', #9074, 1000.000000000000000 ) ;
#19501=ORIENTED_EDGE ( 'NONE', *, *, #21079, .F. ) ;
#19505=CARTESIAN_POINT ( 'NONE',  ( 30.00000000000000000, -5.200000000000001066, -26.25000000000000000 ) ) ;
#19507=AXIS2_PLACEMENT_3D ( 'NONE', #36080, #9931, #25129 ) ;
#19508=CARTESIAN_POINT ( 'NONE',  ( -17.24945551514599984, -15.50000000000000000, -25.53140320652400064 ) ) ;
#19514=CARTESIAN_POINT ( 'NONE',  ( 11.00000000000000000, -5.200000000000001066, -9.400000000000005684 ) ) ;
#19537=AXIS2_PLACEMENT_3D ( 'NONE', #38545, #6368, #27931 ) ;
#19538=FACE_OUTER_BOUND ( 'NONE', #35454, .T. ) ;
#19549=CARTESIAN_POINT ( 'NONE',  ( -29.50000000000000355, -12.00000000000000000, -11.00000000000000000 ) ) ;
#19551=CARTESIAN_POINT ( 'NONE',  ( -17.51999999999999957, -17.50000000000000000, -26.00000000000000355 ) ) ;
#19553=CARTESIAN_POINT ( 'NONE',  ( 14.25000000000000000, -0.2038245569916330158, -21.77831216351300014 ) ) ;
#19560=ORIENTED_EDGE ( 'NONE', *, *, #56287, .F. ) ;
#19566=CARTESIAN_POINT ( 'NONE',  ( 29.25000000000000000, -5.000000000000000000, 60.00000000000000000 ) ) ;
#19571=ORIENTED_EDGE ( 'NONE', *, *, #63115, .F. ) ;
#19578=DIRECTION ( 'NONE',  ( 0.000000000000000000, -1.000000000000000000, 0.000000000000000000 ) ) ;
#19579=ORIENTED_EDGE ( 'NONE', *, *, #50977, .T. ) ;
#19591=DIRECTION ( 'NONE',  ( 0.000000000000000000, -0.9938079899998859545, 0.1111111111112941946 ) ) ;
#19593=CARTESIAN_POINT ( 'NONE',  ( 16.75000000000000000, -0.2038245569916320166, 23.22168783648699986 ) ) ;
#19597=ORIENTED_EDGE ( 'NONE', *, *, #63152, .F. ) ;
#19598=CARTESIAN_POINT ( 'NONE',  ( 11.50000000000000000, -11.50000000000100009, 10.50000000000065903 ) ) ;
#19600=VERTEX_POINT ( 'NONE', #42285 ) ;
#19607=CYLINDRICAL_SURFACE ( 'NONE', #8232, 4.000000000000000000 ) ;
#19608=EDGE_LOOP ( 'NONE', ( #32850, #20967, #21119, #52821 ) ) ;
#19614=ORIENTED_EDGE ( 'NONE', *, *, #19868, .T. ) ;
#19615=FACE_OUTER_BOUND ( 'NONE', #15738, .T. ) ;
#19616=ORIENTED_EDGE ( 'NONE', *, *, #39239, .T. ) ;
#19623=CIRCLE ( 'NONE', #32057, 3.499999999999850342 ) ;
#19628=VERTEX_POINT ( 'NONE', #33071 ) ;
#19629=ORIENTED_EDGE ( 'NONE', *, *, #22845, .F. ) ;
#19635=ORIENTED_EDGE ( 'NONE', *, *, #4171, .T. ) ;
#19636=DIRECTION ( 'NONE',  ( -1.000000000000000000, 0.000000000000000000, 0.000000000000000000 ) ) ;
#19638=CARTESIAN_POINT ( 'NONE',  ( 13.00000000000000178, -17.50000000000000000, 15.70499999999969809 ) ) ;
#19646=LINE ( 'NONE', #63848, #42390 ) ;
#19653=EDGE_LOOP ( 'NONE', ( #37744, #61852, #4802, #3575, #54648, #64193, #51632, #46445, #68950, #61640, #43036, #25027, #23109, #21412, #44512, #15875, #4676, #67447, #1438, #11002 ) ) ;
#19661=CARTESIAN_POINT ( 'NONE',  ( -25.50000000000000355, 0.000000000000000000, 22.50000000000000000 ) ) ;
#19671=CARTESIAN_POINT ( 'NONE',  ( -11.50000000000000000, -12.00000000000000000, 11.00000000000000000 ) ) ;
#19673=PLANE ( 'NONE',  #45811 ) ;
#19680=CARTESIAN_POINT ( 'NONE',  ( 14.45313394609757296, -0.2715358723599912150, 23.33896727494797929 ) ) ;
#19685=EDGE_CURVE ( 'NONE', #49539, #12955, #17154, .T. ) ;
#19692=CARTESIAN_POINT ( 'NONE',  ( 11.00000000000000000, -9.199999999999999289, -12.69999999999986073 ) ) ;
#19693=DIRECTION ( 'NONE',  ( 0.000000000000000000, 1.000000000000000000, 0.000000000000000000 ) ) ;
#19696=DIRECTION ( 'NONE',  ( 0.000000000000000000, 0.000000000000000000, -1.000000000000000000 ) ) ;
#19707=DIRECTION ( 'NONE',  ( 0.000000000000000000, 0.000000000000000000, 1.000000000000000000 ) ) ;
#19709=CIRCLE ( 'NONE', #5050, 0.3500000000009988455 ) ;
#19718=ORIENTED_EDGE ( 'NONE', *, *, #59780, .F. ) ;
#19726=DIRECTION ( 'NONE',  ( 0.000000000000000000, 0.000000000000000000, -1.000000000000000000 ) ) ;
#19730=ORIENTED_EDGE ( 'NONE', *, *, #40892, .T. ) ;
#19732=ORIENTED_EDGE ( 'NONE', *, *, #584, .T. ) ;
#19735=EDGE_CURVE ( 'NONE', #1819, #13915, #20975, .T. ) ;
#19736=ORIENTED_EDGE ( 'NONE', *, *, #2611, .F. ) ;
#19739=CARTESIAN_POINT ( 'NONE',  ( 11.00000000000000000, -12.00000000000000000, 11.03137303340310282 ) ) ;
#19740=EDGE_CURVE ( 'NONE', #4484, #8573, #55007, .T. ) ;
#19741=DIRECTION ( 'NONE',  ( -1.000000000000000000, 0.000000000000000000, 0.000000000000000000 ) ) ;
#19742=ORIENTED_EDGE ( 'NONE', *, *, #48799, .F. ) ;
#19750=DIRECTION ( 'NONE',  ( 0.000000000000000000, 0.000000000000000000, 1.000000000000000000 ) ) ;
#19751=LINE ( 'NONE', #47338, #18275 ) ;
#19754=CARTESIAN_POINT ( 'NONE',  ( 23.75054448485400016, -15.50000000000000000, -25.53140320652400064 ) ) ;
#19757=CARTESIAN_POINT ( 'NONE',  ( -18.85410196625000268, -15.50000000000000000, -21.50000000000000000 ) ) ;
#19758=CARTESIAN_POINT ( 'NONE',  ( -25.50000000000000355, 0.000000000000000000, 22.50000000000000000 ) ) ;
#19760=CARTESIAN_POINT ( 'NONE',  ( 24.00000000000000000, -15.50000000000000000, 14.50000000000000000 ) ) ;
#19761=ORIENTED_EDGE ( 'NONE', *, *, #7020, .F. ) ;
#19764=CARTESIAN_POINT ( 'NONE',  ( 30.00000000000000000, -10.85999999999999943, 9.000000000000001776 ) ) ;
#19774=DIRECTION ( 'NONE',  ( -1.000000000000000000, 0.000000000000000000, 0.000000000000000000 ) ) ;
#19775=CIRCLE ( 'NONE', #36709, 4.500000000000191847 ) ;
#19776=DIRECTION ( 'NONE',  ( 0.4998444328988824181, 0.000000000000000000, -0.8661152018640445593 ) ) ;
#19778=EDGE_CURVE ( 'NONE', #56472, #39966, #46117, .T. ) ;
#19779=DIRECTION ( 'NONE',  ( 0.000000000000000000, 0.000000000000000000, -1.000000000000000000 ) ) ;
#19786=AXIS2_PLACEMENT_3D ( 'NONE', #30637, #52199, #3760 ) ;
#19790=LINE ( 'NONE', #40322, #46810 ) ;
#19809=EDGE_CURVE ( 'NONE', #23827, #45446, #32291, .T. ) ;
#19813=EDGE_CURVE ( 'NONE', #20791, #48776, #60968, .T. ) ;
#19820=LINE ( 'NONE', #64037, #43977 ) ;
#19821=EDGE_CURVE ( 'NONE', #52778, #27235, #1783, .T. ) ;
#19825=AXIS2_PLACEMENT_3D ( 'NONE', #69207, #41633, #58256 ) ;
#19831=FACE_OUTER_BOUND ( 'NONE', #9050, .T. ) ;
#19836=EDGE_CURVE ( 'NONE', #27192, #16314, #65104, .T. ) ;
#19839=PLANE ( 'NONE',  #39585 ) ;
#19846=EDGE_CURVE ( 'NONE', #52878, #11057, #27840, .T. ) ;
#19855=FACE_OUTER_BOUND ( 'NONE', #7914, .T. ) ;
#19864=EDGE_CURVE ( 'NONE', #58158, #27192, #29847, .T. ) ;
#19868=EDGE_CURVE ( 'NONE', #69377, #37150, #15176, .T. ) ;
#19874=LINE ( 'NONE', #30486, #23711 ) ;
#19883=LINE ( 'NONE', #13875, #34426 ) ;
#19888=DIRECTION ( 'NONE',  ( 0.000000000000000000, 1.000000000000000000, 0.000000000000000000 ) ) ;
#19894=CIRCLE ( 'NONE', #22178, 3.499999999999040323 ) ;
#19897=CARTESIAN_POINT ( 'NONE',  ( 29.50000000000000355, -11.50000000000100009, 15.00000000000084910 ) ) ;
#19908=CYLINDRICAL_SURFACE ( 'NONE', #10755, 1.621000000000000885 ) ;
#19919=ORIENTED_EDGE ( 'NONE', *, *, #16592, .T. ) ;
#19922=AXIS2_PLACEMENT_3D ( 'NONE', #52375, #3234, #47071 ) ;
#19928=ADVANCED_FACE ( 'NONE', ( #47178 ), #14999, .F. ) ;
#19939=LINE ( 'NONE', #30902, #32890 ) ;
#19944=CARTESIAN_POINT ( 'NONE',  ( 0.000000000000000000, -2.500000000000000000, 0.000000000000000000 ) ) ;
#19959=DIRECTION ( 'NONE',  ( 0.000000000000000000, -1.000000000000000000, 0.000000000000000000 ) ) ;
#19965=ORIENTED_EDGE ( 'NONE', *, *, #15914, .F. ) ;
#19967=DIRECTION ( 'NONE',  ( 0.000000000000000000, 1.000000000000000000, 0.000000000000000000 ) ) ;
#19975=EDGE_CURVE ( 'NONE', #32135, #18841, #59178, .T. ) ;
#19977=EDGE_CURVE ( 'NONE', #53470, #21801, #6482, .T. ) ;
#19978=ORIENTED_EDGE ( 'NONE', *, *, #7728, .F. ) ;
#19982=CIRCLE ( 'NONE', #26750, 4.000000000000000888 ) ;
#19992=VERTEX_POINT ( 'NONE', #65526 ) ;
#19998=DIRECTION ( 'NONE',  ( 0.000000000000000000, 0.000000000000000000, 1.000000000000000000 ) ) ;
#20000=CIRCLE ( 'NONE', #59532, 3.499999999999999556 ) ;
#20003=DIRECTION ( 'NONE',  ( 0.000000000000000000, -0.7096009616570518874, 0.7046037717862339012 ) ) ;
#20004=B_SPLINE_CURVE_WITH_KNOTS ( 'NONE', 3,
 ( #22245, #38505, #2654, #65380, #62396, #56058 ),
 .UNSPECIFIED., .F., .F.,
 ( 4, 2, 4 ),
 ( 0.0002380763768114607659, 0.7291065797294573603, 1.457975083082103218 ),
 .UNSPECIFIED. ) ;
#20014=EDGE_CURVE ( 'NONE', #122, #63027, #33681, .T. ) ;
#20015=DIRECTION ( 'NONE',  ( 0.000000000000000000, 1.000000000000000000, 0.000000000000000000 ) ) ;
#20026=ORIENTED_EDGE ( 'NONE', *, *, #6932, .F. ) ;
#20037=DIRECTION ( 'NONE',  ( -1.000000000000000000, 0.000000000000000000, 0.000000000000000000 ) ) ;
#20040=DIRECTION ( 'NONE',  ( 0.000000000000000000, 1.000000000000000000, 0.000000000000000000 ) ) ;
#20061=ORIENTED_EDGE ( 'NONE', *, *, #34084, .T. ) ;
#20064=PLANE ( 'NONE',  #31194 ) ;
#20065=VECTOR ( 'NONE', #59539, 1000.000000000000000 ) ;
#20066=ORIENTED_EDGE ( 'NONE', *, *, #48999, .F. ) ;
#20072=ORIENTED_EDGE ( 'NONE', *, *, #980, .F. ) ;
#20085=AXIS2_PLACEMENT_3D ( 'NONE', #17082, #43608, #22045 ) ;
#20091=VERTEX_POINT ( 'NONE', #38987 ) ;
#20093=SHAPE_DEFINITION_REPRESENTATION ( #29020, #26379 ) ;
#20103=EDGE_CURVE ( 'NONE', #57937, #42164, #60556, .T. ) ;
#20113=B_SPLINE_CURVE_WITH_KNOTS ( 'NONE', 3,
 ( #58641, #48377, #62893, #46970, #31434, #4554 ),
 .UNSPECIFIED., .F., .F.,
 ( 4, 2, 4 ),
 ( 0.0002380763768115301549, 0.7291065797294569162, 1.457975083082102330 ),
 .UNSPECIFIED. ) ;
#20115=LINE ( 'NONE', #48641, #20183 ) ;
#20121=CARTESIAN_POINT ( 'NONE',  ( -29.50000000000000355, -15.97213595500069871, 14.50000000000000000 ) ) ;
#20128=CARTESIAN_POINT ( 'NONE',  ( 11.00000000000000000, -11.50000000000000000, -11.00000000000000000 ) ) ;
#20131=EDGE_LOOP ( 'NONE', ( #19571, #9105, #41400, #57114, #16517, #25774, #54774, #5851 ) ) ;
#20142=CARTESIAN_POINT ( 'NONE',  ( -25.50000000000000355, -17.50000000000000000, 22.50000000000000000 ) ) ;
#20143=EDGE_CURVE ( 'NONE', #43590, #10241, #28720, .T. ) ;
#20151=ORIENTED_EDGE ( 'NONE', *, *, #39373, .F. ) ;
#20152=EDGE_CURVE ( 'NONE', #59443, #50308, #13857, .T. ) ;
#20158=CYLINDRICAL_SURFACE ( 'NONE', #3926, 2.250000000000001776 ) ;
#20183=VECTOR ( 'NONE', #11489, 1000.000000000000000 ) ;
#20191=VECTOR ( 'NONE', #13860, 1000.000000000000000 ) ;
#20199=CYLINDRICAL_SURFACE ( 'NONE', #27301, 4.000000000000000000 ) ;
#20207=PLANE ( 'NONE',  #31125 ) ;
#20215=DIRECTION ( 'NONE',  ( 0.000000000000000000, 0.000000000000000000, 1.000000000000000000 ) ) ;
#20216=PLANE ( 'NONE',  #20380 ) ;
#20217=ADVANCED_FACE ( 'NONE', ( #34720 ), #45320, .T. ) ;
#20222=CIRCLE ( 'NONE', #56357, 0.2999999999998732569 ) ;
#20225=EDGE_CURVE ( 'NONE', #35907, #38480, #13506, .T. ) ;
#20240=VERTEX_POINT ( 'NONE', #36475 ) ;
#20242=ORIENTED_EDGE ( 'NONE', *, *, #53090, .F. ) ;
#20245=DIRECTION ( 'NONE',  ( 0.7142857142857395036, 0.000000000000000000, 0.6998542122237394469 ) ) ;
#20246=LINE ( 'NONE', #30858, #29772 ) ;
#20265=ORIENTED_EDGE ( 'NONE', *, *, #28835, .T. ) ;
#20278=DIRECTION ( 'NONE',  ( 0.000000000000000000, 0.000000000000000000, 1.000000000000000000 ) ) ;
#20280=DIRECTION ( 'NONE',  ( 0.000000000000000000, 0.000000000000000000, -1.000000000000000000 ) ) ;
#20281=ORIENTED_EDGE ( 'NONE', *, *, #29057, .T. ) ;
#20285=ADVANCED_FACE ( 'NONE', ( #37194 ), #42530, .T. ) ;
#20287=CARTESIAN_POINT ( 'NONE',  ( -17.00000000000000000, -16.28999999999999915, -14.50000000000000000 ) ) ;
#20293=AXIS2_PLACEMENT_3D ( 'NONE', #57441, #20652, #3349 ) ;
#20298=DIRECTION ( 'NONE',  ( 0.000000000000000000, 0.000000000000000000, 1.000000000000000000 ) ) ;
#20303=ADVANCED_FACE ( 'NONE', ( #14206 ), #3959, .F. ) ;
#20313=LINE ( 'NONE', #20654, #47830 ) ;
#20318=DIRECTION ( 'NONE',  ( 0.000000000000000000, -5.800915303574361727E-12, -1.000000000000000000 ) ) ;
#20320=CARTESIAN_POINT ( 'NONE',  ( 11.00000000000000000, -17.14999999999900027, -26.64999999999900027 ) ) ;
#20321=FACE_OUTER_BOUND ( 'NONE', #46691, .T. ) ;
#20332=CARTESIAN_POINT ( 'NONE',  ( 11.50000000000000000, -11.50000000000100009, 10.50000000000065903 ) ) ;
#20338=ORIENTED_EDGE ( 'NONE', *, *, #2151, .T. ) ;
#20342=CARTESIAN_POINT ( 'NONE',  ( 25.50000000000000355, -15.50000000000000000, 22.50000000000000000 ) ) ;
#20344=CARTESIAN_POINT ( 'NONE',  ( -15.50000000000000000, 0.000000000000000000, 18.50000000000000000 ) ) ;
#20348=VERTEX_POINT ( 'NONE', #69718 ) ;
#20350=CIRCLE ( 'NONE', #29364, 0.3499999999998879008 ) ;
#20353=ORIENTED_EDGE ( 'NONE', *, *, #46632, .T. ) ;
#20360=EDGE_CURVE ( 'NONE', #38019, #11471, #59444, .T. ) ;
#20373=VERTEX_POINT ( 'NONE', #1092 ) ;
#20380=AXIS2_PLACEMENT_3D ( 'NONE', #35418, #46044, #52777 ) ;
#20394=AXIS2_PLACEMENT_3D ( 'NONE', #19754, #3864, #24015 ) ;
#20400=CARTESIAN_POINT ( 'NONE',  ( 15.50000000000000000, -0.4000000000000000222, 22.50000000000000000 ) ) ;
#20408=ORIENTED_EDGE ( 'NONE', *, *, #30654, .T. ) ;
#20411=CARTESIAN_POINT ( 'NONE',  ( 29.50000000000000355, -11.50000000000100009, 15.00000000000084910 ) ) ;
#20417=CARTESIAN_POINT ( 'NONE',  ( -11.00000000000000000, -12.00000000000000000, 10.20500000000000007 ) ) ;
#20421=VECTOR ( 'NONE', #9864, 1000.000000000000000 ) ;
#20423=DIRECTION ( 'NONE',  ( 1.000000000000000000, 0.000000000000000000, 0.000000000000000000 ) ) ;
#20427=EDGE_CURVE ( 'NONE', #37433, #25346, #15488, .T. ) ;
#20429=AXIS2_PLACEMENT_3D ( 'NONE', #11681, #18368, #1772 ) ;
#20435=EDGE_LOOP ( 'NONE', ( #53799, #31350, #6923, #52690, #37607, #21877, #22576 ) ) ;
#20456=EDGE_CURVE ( 'NONE', #35831, #20091, #50564, .T. ) ;
#20458=EDGE_CURVE ( 'NONE', #12841, #2217, #17689, .T. ) ;
#20459=VERTEX_POINT ( 'NONE', #33934 ) ;
#20466=ORIENTED_EDGE ( 'NONE', *, *, #55642, .F. ) ;
#20469=LINE ( 'NONE', #46991, #47107 ) ;
#20475=AXIS2_PLACEMENT_3D ( 'NONE', #15694, #21339, #10724 ) ;
#20476=FACE_OUTER_BOUND ( 'NONE', #68532, .T. ) ;
#20477=EDGE_LOOP ( 'NONE', ( #58618, #55124, #11532, #21087, #7879, #59035, #21868 ) ) ;
#20479=FACE_OUTER_BOUND ( 'NONE', #43234, .T. ) ;
#20481=DIRECTION ( 'NONE',  ( -1.000000000000000000, 0.000000000000000000, 0.000000000000000000 ) ) ;
#20484=LINE ( 'NONE', #53031, #1252 ) ;
#20486=LINE ( 'NONE', #58678, #41285 ) ;
#20489=LINE ( 'NONE', #31469, #27700 ) ;
#20494=ORIENTED_EDGE ( 'NONE', *, *, #8576, .F. ) ;
#20501=ADVANCED_FACE ( 'NONE', ( #66808 ), #28293, .T. ) ;
#20502=AXIS2_PLACEMENT_3D ( 'NONE', #66893, #13156, #34722 ) ;
#20503=ADVANCED_FACE ( 'NONE', ( #39926 ), #33604, .F. ) ;
#20505=DIRECTION ( 'NONE',  ( 0.000000000000000000, 0.000000000000000000, 1.000000000000000000 ) ) ;
#20510=VERTEX_POINT ( 'NONE', #23674 ) ;
#20515=ORIENTED_EDGE ( 'NONE', *, *, #19975, .F. ) ;
#20524=CIRCLE ( 'NONE', #13745, 0.3499999999998866795 ) ;
#20528=CARTESIAN_POINT ( 'NONE',  ( 11.00000000000000000, -14.34000000000000163, -14.50000000000000178 ) ) ;
#20535=DIRECTION ( 'NONE',  ( 0.000000000000000000, 0.000000000000000000, -1.000000000000000000 ) ) ;
#20545=EDGE_LOOP ( 'NONE', ( #26924, #10026, #29323, #9216 ) ) ;
#20549=CARTESIAN_POINT ( 'NONE',  ( -11.50000000000000000, -11.50000000000000000, 15.00000000000000000 ) ) ;
#20570=VERTEX_POINT ( 'NONE', #61866 ) ;
#20571=DIRECTION ( 'NONE',  ( 0.000000000000000000, 0.000000000000000000, 1.000000000000000000 ) ) ;
#20576=CARTESIAN_POINT ( 'NONE',  ( 11.00000000000000000, -15.46862696659690073, -14.50000000000000000 ) ) ;
#20581=CARTESIAN_POINT ( 'NONE',  ( -11.00000000000000000, -13.54524521594299991, 17.53999999999999915 ) ) ;
#20591=CARTESIAN_POINT ( 'NONE',  ( 11.00000000000000000, -17.35230188589299871, 15.35019951917099945 ) ) ;
#20593=LINE ( 'NONE', #27641, #10494 ) ;
#20601=VERTEX_POINT ( 'NONE', #19764 ) ;
#20606=ORIENTED_EDGE ( 'NONE', *, *, #24803, .F. ) ;
#20621=LINE ( 'NONE', #64140, #67960 ) ;
#20623=CARTESIAN_POINT ( 'NONE',  ( -11.50000000000000000, -12.00000000000000000, 10.69999999999999929 ) ) ;
#20625=CARTESIAN_POINT ( 'NONE',  ( -24.00000000000000000, -16.28999999999710369, 15.00000000000794920 ) ) ;
#20627=ORIENTED_EDGE ( 'NONE', *, *, #39318, .F. ) ;
#20629=DIRECTION ( 'NONE',  ( 1.000000000000000000, -0.000000000000000000, -0.000000000000000000 ) ) ;
#20644=CARTESIAN_POINT ( 'NONE',  ( 13.00000000000000178, -16.64230188589299786, -14.64519951917100116 ) ) ;
#20646=ADVANCED_FACE ( 'NONE', ( #20479 ), #56895, .F. ) ;
#20650=LINE ( 'NONE', #58510, #29296 ) ;
#20652=DIRECTION ( 'NONE',  ( 0.000000000000000000, 0.000000000000000000, 1.000000000000000000 ) ) ;
#20654=CARTESIAN_POINT ( 'NONE',  ( -17.00000000000000000, -17.35230188589299871, 15.35019951917099945 ) ) ;
#20681=VERTEX_POINT ( 'NONE', #8454 ) ;
#20696=EDGE_CURVE ( 'NONE', #53754, #42236, #65206, .T. ) ;
#20698=ADVANCED_FACE ( 'NONE', ( #63981 ), #37449, .F. ) ;
#20700=ORIENTED_EDGE ( 'NONE', *, *, #17721, .T. ) ;
#20702=FACE_OUTER_BOUND ( 'NONE', #36170, .T. ) ;
#20706=ADVANCED_FACE ( 'NONE', ( #22229 ), #37107, .F. ) ;
#20714=EDGE_CURVE ( 'NONE', #10292, #32087, #20822, .T. ) ;
#20719=ADVANCED_FACE ( 'NONE', ( #48749 ), #307, .T. ) ;
#20724=DIRECTION ( 'NONE',  ( 1.000000000000000000, -0.000000000000000000, -0.000000000000000000 ) ) ;
#20735=AXIS2_PLACEMENT_3D ( 'NONE', #3183, #2466, #7417 ) ;
#20739=CARTESIAN_POINT ( 'NONE',  ( -30.00000000000000000, -16.28999999999999915, -14.50000000000000000 ) ) ;
#20741=DIRECTION ( 'NONE',  ( 1.000000000000000000, -0.000000000000000000, -0.000000000000000000 ) ) ;
#20752=LINE ( 'NONE', #52595, #31707 ) ;
#20766=EDGE_CURVE ( 'NONE', #69773, #55741, #7931, .T. ) ;
#20769=EDGE_LOOP ( 'NONE', ( #3125, #31591, #51268, #60335 ) ) ;
#20771=FACE_OUTER_BOUND ( 'NONE', #63021, .T. ) ;
#20786=ORIENTED_EDGE ( 'NONE', *, *, #45597, .T. ) ;
#20788=VECTOR ( 'NONE', #13429, 1000.000000000000000 ) ;
#20791=VERTEX_POINT ( 'NONE', #23857 ) ;
#20797=DIRECTION ( 'NONE',  ( 1.000000000000000000, 0.000000000000000000, 0.000000000000000000 ) ) ;
#20802=ORIENTED_EDGE ( 'NONE', *, *, #62909, .F. ) ;
#20805=CARTESIAN_POINT ( 'NONE',  ( 11.00000000000000000, -12.00000000000000000, 11.03137303340310282 ) ) ;
#20813=CARTESIAN_POINT ( 'NONE',  ( 30.00000000000000000, -9.200000000000120082, 17.64999999999993108 ) ) ;
#20817=DIRECTION ( 'NONE',  ( -1.000000000000000000, 0.000000000000000000, 0.000000000000000000 ) ) ;
#20822=LINE ( 'NONE', #11249, #13237 ) ;
#20823=MANIFOLD_SOLID_BREP ( 'SAWC-0630-60S_wagen', #44193 ) ;
#20825=AXIS2_PLACEMENT_3D ( 'NONE', #31482, #3903, #37131 ) ;
#20827=DIRECTION ( 'NONE',  ( 0.000000000000000000, 0.000000000000000000, 1.000000000000000000 ) ) ;
#20833=DIRECTION ( 'NONE',  ( 0.000000000000000000, 0.000000000000000000, 1.000000000000000000 ) ) ;
#20841=ORIENTED_EDGE ( 'NONE', *, *, #37129, .F. ) ;
#20852=VECTOR ( 'NONE', #67821, 1000.000000000000000 ) ;
#20861=CARTESIAN_POINT ( 'NONE',  ( -30.00000000000000000, -12.00000000000000000, 10.52786404500095863 ) ) ;
#20862=CARTESIAN_POINT ( 'NONE',  ( 24.00000000000000000, -16.64230188589299786, -14.64519951917100116 ) ) ;
#20867=AXIS2_PLACEMENT_3D ( 'NONE', #12311, #66068, #28588 ) ;
#20873=ORIENTED_EDGE ( 'NONE', *, *, #47268, .T. ) ;
#20874=ORIENTED_EDGE ( 'NONE', *, *, #37830, .F. ) ;
#20885=CARTESIAN_POINT ( 'NONE',  ( -25.50000000000000355, 0.000000000000000000, 22.50000000000000000 ) ) ;
#20889=AXIS2_PLACEMENT_3D ( 'NONE', #21277, #64075, #31538 ) ;
#20900=CARTESIAN_POINT ( 'NONE',  ( -30.00000000000000000, -12.00000000000000000, 12.20000000000000107 ) ) ;
#20911=CARTESIAN_POINT ( 'NONE',  ( 30.00000000000000000, -9.454754784057099570, -17.53999999999999915 ) ) ;
#20921=CARTESIAN_POINT ( 'NONE',  ( -17.00000000000000000, -17.35230188589299871, -15.35019951917099945 ) ) ;
#20925=ORIENTED_EDGE ( 'NONE', *, *, #13303, .F. ) ;
#20927=DIRECTION ( 'NONE',  ( 1.000000000000000000, -0.000000000000000000, 1.224646799147353207E-16 ) ) ;
#20933=EDGE_CURVE ( 'NONE', #13102, #50086, #52134, .T. ) ;
#20934=CARTESIAN_POINT ( 'NONE',  ( -15.50000000000000000, -0.2000000000000000111, 22.50000000000000000 ) ) ;
#20935=ORIENTED_EDGE ( 'NONE', *, *, #14021, .F. ) ;
#20937=CIRCLE ( 'NONE', #62720, 0.5000000000079367624 ) ;
#20940=CARTESIAN_POINT ( 'NONE',  ( 29.50000000000000355, -11.70000000000012008, 10.70000000000011831 ) ) ;
#20942=EDGE_CURVE ( 'NONE', #50555, #1682, #31628, .T. ) ;
#20949=DIRECTION ( 'NONE',  ( 1.000000000000000000, 0.000000000000000000, 0.000000000000000000 ) ) ;
#20953=VERTEX_POINT ( 'NONE', #47871 ) ;
#20955=DIRECTION ( 'NONE',  ( 0.4285714285711678118, 0.000000000000000000, 0.9035079029053749711 ) ) ;
#20959=LINE ( 'NONE', #53500, #69258 ) ;
#20965=VERTEX_POINT ( 'NONE', #10402 ) ;
#20967=ORIENTED_EDGE ( 'NONE', *, *, #6431, .F. ) ;
#20971=ORIENTED_EDGE ( 'NONE', *, *, #48349, .T. ) ;
#20972=ORIENTED_EDGE ( 'NONE', *, *, #48263, .T. ) ;
#20973=DIRECTION ( 'NONE',  ( 1.000000000000000000, 0.000000000000000000, 0.000000000000000000 ) ) ;
#20975=CIRCLE ( 'NONE', #30001, 0.3499999999999285905 ) ;
#20981=DIRECTION ( 'NONE',  ( 0.000000000000000000, -0.1111111111108840643, -0.9938079899999319178 ) ) ;
#20983=DIRECTION ( 'NONE',  ( -1.000000000000000000, 0.000000000000000000, 0.000000000000000000 ) ) ;
#20988=ORIENTED_EDGE ( 'NONE', *, *, #11008, .F. ) ;
#20994=LINE ( 'NONE', #43253, #6164 ) ;
#21006=ORIENTED_EDGE ( 'NONE', *, *, #43195, .T. ) ;
#21009=CARTESIAN_POINT ( 'NONE',  ( -28.00000000000000000, -15.50000000000000000, -20.05051025721700242 ) ) ;
#21011=CARTESIAN_POINT ( 'NONE',  ( -14.25000000000000000, -0.2038245569916330158, 21.77831216351300014 ) ) ;
#21025=CARTESIAN_POINT ( 'NONE',  ( 15.08565937784311117, -0.3156604612129180754, -21.29584399676446793 ) ) ;
#21027=ORIENTED_EDGE ( 'NONE', *, *, #27486, .T. ) ;
#21029=AXIS2_PLACEMENT_3D ( 'NONE', #36557, #25967, #9701 ) ;
#21034=ORIENTED_EDGE ( 'NONE', *, *, #35281, .T. ) ;
#21038=ADVANCED_FACE ( 'NONE', ( #6490 ), #17781, .F. ) ;
#21039=ORIENTED_EDGE ( 'NONE', *, *, #8795, .F. ) ;
#21044=DIRECTION ( 'NONE',  ( 0.000000000000000000, 1.000000000000000000, 0.000000000000000000 ) ) ;
#21048=ORIENTED_EDGE ( 'NONE', *, *, #22019, .F. ) ;
#21052=AXIS2_PLACEMENT_3D ( 'NONE', #42862, #20949, #10350 ) ;
#21076=ORIENTED_EDGE ( 'NONE', *, *, #35500, .T. ) ;
#21079=EDGE_CURVE ( 'NONE', #2931, #11595, #38995, .T. ) ;
#21087=ORIENTED_EDGE ( 'NONE', *, *, #60881, .T. ) ;
#21090=CARTESIAN_POINT ( 'NONE',  ( 30.00000000000000000, -13.54524521594299991, 17.53999999999999915 ) ) ;
#21097=ADVANCED_FACE ( 'NONE', ( #33689 ), #55271, .T. ) ;
#21101=VECTOR ( 'NONE', #22527, 1000.000000000000000 ) ;
#21112=DIRECTION ( 'NONE',  ( 0.000000000000000000, 0.000000000000000000, 1.000000000000000000 ) ) ;
#21114=AXIS2_PLACEMENT_3D ( 'NONE', #59434, #60801, #38226 ) ;
#21117=EDGE_CURVE ( 'NONE', #58645, #29870, #43620, .T. ) ;
#21119=ORIENTED_EDGE ( 'NONE', *, *, #66501, .T. ) ;
#21126=CARTESIAN_POINT ( 'NONE',  ( 30.00000000000000000, -8.959999999999999076, 17.04524521594300523 ) ) ;
#21130=ADVANCED_FACE ( 'NONE', ( #49284 ), #857, .T. ) ;
#21139=FACE_OUTER_BOUND ( 'NONE', #68102, .T. ) ;
#21141=EDGE_CURVE ( 'NONE', #57577, #17297, #60215, .T. ) ;
#21142=ORIENTED_EDGE ( 'NONE', *, *, #43626, .T. ) ;
#21154=LINE ( 'NONE', #48371, #6866 ) ;
#21156=EDGE_LOOP ( 'NONE', ( #27038, #8739, #62168, #23201, #16782, #63576, #18915, #32007 ) ) ;
#21157=EDGE_LOOP ( 'NONE', ( #23524, #51907, #39912, #23212 ) ) ;
#21161=ORIENTED_EDGE ( 'NONE', *, *, #30203, .T. ) ;
#21162=ADVANCED_FACE ( 'NONE', ( #66900 ), #56651, .F. ) ;
#21177=LINE ( 'NONE', #4225, #844 ) ;
#21183=CARTESIAN_POINT ( 'NONE',  ( -29.25000000000000000, -5.000000000000000000, -26.25000000000000000 ) ) ;
#21196=DIRECTION ( 'NONE',  ( 0.3479852726768751237, 0.000000000000000000, 0.9375000000000004441 ) ) ;
#21200=EDGE_CURVE ( 'NONE', #27438, #64069, #24831, .T. ) ;
#21204=VECTOR ( 'NONE', #46371, 999.9999999999998863 ) ;
#21207=EDGE_CURVE ( 'NONE', #28218, #14914, #30213, .T. ) ;
#21214=ORIENTED_EDGE ( 'NONE', *, *, #47720, .T. ) ;
#21223=DIRECTION ( 'NONE',  ( 0.000000000000000000, -0.7071067811865460184, -0.7071067811865489050 ) ) ;
#21229=CARTESIAN_POINT ( 'NONE',  ( 14.25000000000000000, -0.2038245569916330158, -23.22168783648699986 ) ) ;
#21230=DIRECTION ( 'NONE',  ( 1.000000000000000000, -0.000000000000000000, -0.000000000000000000 ) ) ;
#21245=LINE ( 'NONE', #16638, #22158 ) ;
#21249=CARTESIAN_POINT ( 'NONE',  ( 30.00000000000000000, -17.00000000000000000, -15.70499999999969809 ) ) ;
#21264=DIRECTION ( 'NONE',  ( 0.000000000000000000, -0.6857142857147903170, 0.7278708115913530285 ) ) ;
#21265=EDGE_CURVE ( 'NONE', #28244, #14932, #24127, .T. ) ;
#21268=CARTESIAN_POINT ( 'NONE',  ( 11.75000000000000000, -5.000000000000000000, -26.25000000000000000 ) ) ;
#21275=DIRECTION ( 'NONE',  ( -1.000000000000000000, 0.000000000000000000, 0.000000000000000000 ) ) ;
#21277=CARTESIAN_POINT ( 'NONE',  ( -25.50000000000000355, -15.12100000000000044, 22.50000000000000000 ) ) ;
#21283=ORIENTED_EDGE ( 'NONE', *, *, #68265, .T. ) ;
#21287=DIRECTION ( 'NONE',  ( 1.000000000000000000, 0.000000000000000000, 0.000000000000000000 ) ) ;
#21309=CARTESIAN_POINT ( 'NONE',  ( 30.00000000000000000, -11.85423089348099879, 9.852125413066602277 ) ) ;
#21310=ORIENTED_EDGE ( 'NONE', *, *, #32523, .F. ) ;
#21313=ORIENTED_EDGE ( 'NONE', *, *, #25708, .F. ) ;
#21317=AXIS2_PLACEMENT_3D ( 'NONE', #23432, #50643, #38990 ) ;
#21328=FACE_OUTER_BOUND ( 'NONE', #53399, .T. ) ;
#21335=EDGE_LOOP ( 'NONE', ( #43431, #43473, #59507, #61828 ) ) ;
#21339=DIRECTION ( 'NONE',  ( 1.000000000000000000, -0.000000000000000000, -0.000000000000000000 ) ) ;
#21351=CARTESIAN_POINT ( 'NONE',  ( 30.00000000000000000, -10.85999999999999943, -9.000000000000001776 ) ) ;
#21358=EDGE_LOOP ( 'NONE', ( #5775, #11960, #4001, #68377 ) ) ;
#21362=ORIENTED_EDGE ( 'NONE', *, *, #6561, .T. ) ;
#21365=ORIENTED_EDGE ( 'NONE', *, *, #58233, .F. ) ;
#21367=AXIS2_PLACEMENT_3D ( 'NONE', #3245, #51328, #41064 ) ;
#21374=ORIENTED_EDGE ( 'NONE', *, *, #11643, .T. ) ;
#21378=CARTESIAN_POINT ( 'NONE',  ( 16.75000000000000000, -2.500000000000000000, -23.22168783648699986 ) ) ;
#21382=ADVANCED_FACE ( 'NONE', ( #27969 ), #32926, .T. ) ;
#21383=EDGE_CURVE ( 'NONE', #23822, #68865, #10664, .T. ) ;
#21394=DIRECTION ( 'NONE',  ( 0.000000000000000000, -1.000000000000000000, 0.000000000000000000 ) ) ;
#21397=VERTEX_POINT ( 'NONE', #43181 ) ;
#21399=ORIENTED_EDGE ( 'NONE', *, *, #18520, .T. ) ;
#21402=AXIS2_PLACEMENT_3D ( 'NONE', #45477, #18610, #15426 ) ;
#21409=CARTESIAN_POINT ( 'NONE',  ( 25.50000000000000355, -15.50000000000000000, -25.99999999999985434 ) ) ;
#21412=ORIENTED_EDGE ( 'NONE', *, *, #60633, .F. ) ;
#21415=CARTESIAN_POINT ( 'NONE',  ( 30.00000000000000000, -17.00000000000000000, 15.70499999999969809 ) ) ;
#21427=EDGE_CURVE ( 'NONE', #61212, #25535, #44936, .T. ) ;
#21431=EDGE_CURVE ( 'NONE', #52778, #9070, #65454, .T. ) ;
#21433=CARTESIAN_POINT ( 'NONE',  ( -17.00000000000000000, -16.28999999999710369, -14.50000000000000000 ) ) ;
#21434=VECTOR ( 'NONE', #48257, 1000.000000000000000 ) ;
#21449=CIRCLE ( 'NONE', #66610, 3.499999999999999556 ) ;
#21452=CARTESIAN_POINT ( 'NONE',  ( -16.75000000000000000, -2.500000000000000000, -21.77831216351300014 ) ) ;
#21459=CARTESIAN_POINT ( 'NONE',  ( 15.50000000000000000, 0.000000000000000000, -18.50000000000000000 ) ) ;
#21463=VERTEX_POINT ( 'NONE', #13072 ) ;
#21465=FACE_OUTER_BOUND ( 'NONE', #22497, .T. ) ;
#21474=ORIENTED_EDGE ( 'NONE', *, *, #37486, .T. ) ;
#21484=EDGE_CURVE ( 'NONE', #17477, #11057, #18990, .T. ) ;
#21485=DIRECTION ( 'NONE',  ( 0.000000000000000000, 1.000000000000000000, 0.000000000000000000 ) ) ;
#21486=AXIS2_PLACEMENT_3D ( 'NONE', #2872, #8170, #52022 ) ;
#21496=EDGE_CURVE ( 'NONE', #47032, #5159, #7075, .T. ) ;
#21499=DIRECTION ( 'NONE',  ( -1.000000000000000000, 0.000000000000000000, 0.000000000000000000 ) ) ;
#21504=CARTESIAN_POINT ( 'NONE',  ( 11.50000000000000000, -15.46862696659690073, 14.50000000000000000 ) ) ;
#21511=AXIS2_PLACEMENT_3D ( 'NONE', #35115, #13561, #67657 ) ;
#21518=CARTESIAN_POINT ( 'NONE',  ( -25.50000000000000355, -5.200000000000001066, -22.50000000000000000 ) ) ;
#21521=CARTESIAN_POINT ( 'NONE',  ( 30.00000000000000000, -11.70000000000000284, -12.50000000000000000 ) ) ;
#21523=DIRECTION ( 'NONE',  ( 0.000000000000000000, -0.7071067811865455743, 0.7071067811865495711 ) ) ;
#21535=CARTESIAN_POINT ( 'NONE',  ( 11.75000000000000000, -5.000000000000000000, -11.75000000000000000 ) ) ;
#21537=DIRECTION ( 'NONE',  ( -1.000000000000000000, 0.000000000000000000, 0.000000000000000000 ) ) ;
#21547=DIRECTION ( 'NONE',  ( 1.000000000000000000, 0.000000000000000000, 0.000000000000000000 ) ) ;
#21556=ORIENTED_EDGE ( 'NONE', *, *, #45904, .F. ) ;
#21558=EDGE_CURVE ( 'NONE', #56607, #50075, #14002, .T. ) ;
#21560=DIRECTION ( 'NONE',  ( 0.000000000000000000, -0.1249999999999996531, -0.9921567416492215186 ) ) ;
#21561=DIRECTION ( 'NONE',  ( 0.000000000000000000, -0.9938079899998859545, 0.1111111111112941946 ) ) ;
#21564=EDGE_CURVE ( 'NONE', #63213, #54079, #52440, .T. ) ;
#21565=LINE ( 'NONE', #55135, #1862 ) ;
#21571=ADVANCED_FACE ( 'NONE', ( #63278 ), #52687, .F. ) ;
#21575=ADVANCED_FACE ( 'NONE', ( #3188 ), #58680, .F. ) ;
#21587=EDGE_CURVE ( 'NONE', #67901, #42614, #25099, .T. ) ;
#21590=DIRECTION ( 'NONE',  ( 1.000000000000000000, 0.000000000000000000, 0.000000000000000000 ) ) ;
#21591=FACE_OUTER_BOUND ( 'NONE', #16262, .T. ) ;
#21595=EDGE_CURVE ( 'NONE', #62386, #54520, #15193, .T. ) ;
#21606=LINE ( 'NONE', #21942, #48742 ) ;
#21612=LINE ( 'NONE', #11329, #50719 ) ;
#21616=VECTOR ( 'NONE', #38600, 1000.000000000000000 ) ;
#21625=AXIS2_PLACEMENT_3D ( 'NONE', #65528, #58503, #26660 ) ;
#21632=ORIENTED_EDGE ( 'NONE', *, *, #35365, .T. ) ;
#21636=DIRECTION ( 'NONE',  ( -1.000000000000000000, 0.000000000000000000, 0.000000000000000000 ) ) ;
#21639=FACE_OUTER_BOUND ( 'NONE', #33792, .T. ) ;
#21645=ORIENTED_EDGE ( 'NONE', *, *, #65964, .T. ) ;
#21648=CIRCLE ( 'NONE', #38603, 0.3499999999999308664 ) ;
#21651=DIRECTION ( 'NONE',  ( 0.3479852726768748461, 0.000000000000000000, 0.9375000000000006661 ) ) ;
#21662=VECTOR ( 'NONE', #36144, 1000.000000000000000 ) ;
#21665=ADVANCED_FACE ( 'NONE', ( #60385 ), #11598, .F. ) ;
#21673=DIRECTION ( 'NONE',  ( -1.000000000000000000, 0.000000000000000000, 0.000000000000000000 ) ) ;
#21675=CARTESIAN_POINT ( 'NONE',  ( -24.00000000000000000, -15.50000000000000000, 19.33772233983200195 ) ) ;
#21680=DIRECTION ( 'NONE',  ( 0.000000000000000000, 0.000000000000000000, -1.000000000000000000 ) ) ;
#21686=ORIENTED_EDGE ( 'NONE', *, *, #19836, .T. ) ;
#21690=CIRCLE ( 'NONE', #32987, 4.000000000000000888 ) ;
#21699=CARTESIAN_POINT ( 'NONE',  ( -14.25000000000000000, -2.500000000000000000, 23.22168783648699986 ) ) ;
#21700=DIRECTION ( 'NONE',  ( -1.000000000000000000, 0.000000000000000000, 0.000000000000000000 ) ) ;
#21705=VECTOR ( 'NONE', #69899, 1000.000000000000000 ) ;
#21709=VECTOR ( 'NONE', #6332, 1000.000000000000000 ) ;
#21712=PLANE ( 'NONE',  #38417 ) ;
#21713=CARTESIAN_POINT ( 'NONE',  ( -30.00000000000000000, -5.200000000000001066, 9.400000000000000355 ) ) ;
#21720=DIRECTION ( 'NONE',  ( 1.000000000000000000, 0.000000000000000000, 0.000000000000000000 ) ) ;
#21729=VERTEX_POINT ( 'NONE', #37805 ) ;
#21735=EDGE_LOOP ( 'NONE', ( #5487, #49185, #52276, #39558, #57276, #21048, #64340 ) ) ;
#21743=EDGE_CURVE ( 'NONE', #57686, #28197, #12630, .T. ) ;
#21747=VECTOR ( 'NONE', #43904, 1000.000000000000000 ) ;
#21754=CARTESIAN_POINT ( 'NONE',  ( -25.50000000000000355, 0.000000000000000000, -22.50000000000000000 ) ) ;
#21767=DIRECTION ( 'NONE',  ( 0.000000000000000000, 0.000000000000000000, 1.000000000000000000 ) ) ;
#21771=EDGE_CURVE ( 'NONE', #46957, #56934, #19002, .T. ) ;
#21792=DIRECTION ( 'NONE',  ( 0.000000000000000000, -1.000000000000000000, 0.000000000000000000 ) ) ;
#21794=VERTEX_POINT ( 'NONE', #28908 ) ;
#21801=VERTEX_POINT ( 'NONE', #50482 ) ;
#21808=VECTOR ( 'NONE', #56143, 1000.000000000000000 ) ;
#21828=AXIS2_PLACEMENT_3D ( 'NONE', #30491, #14578, #14232 ) ;
#21832=AXIS2_PLACEMENT_3D ( 'NONE', #8417, #57222, #49241 ) ;
#21836=CARTESIAN_POINT ( 'NONE',  ( 29.25000000000000000, -5.000000000000000000, 26.25000000000000000 ) ) ;
#21839=ORIENTED_EDGE ( 'NONE', *, *, #30224, .T. ) ;
#21845=VERTEX_POINT ( 'NONE', #61417 ) ;
#21848=DIRECTION ( 'NONE',  ( 0.000000000000000000, 0.000000000000000000, 1.000000000000000000 ) ) ;
#21857=CARTESIAN_POINT ( 'NONE',  ( -30.00000000000000000, -11.10796162543699950, 9.102987789146602893 ) ) ;
#21858=DIRECTION ( 'NONE',  ( 1.000000000000000000, -0.000000000000000000, -0.000000000000000000 ) ) ;
#21860=VECTOR ( 'NONE', #14009, 1000.000000000000000 ) ;
#21866=CARTESIAN_POINT ( 'NONE',  ( -15.50000000000000000, -5.000000000000000000, 26.00000000000000000 ) ) ;
#21867=CARTESIAN_POINT ( 'NONE',  ( -11.00000000000000000, -11.50000000000100009, 15.00000000000084910 ) ) ;
#21868=ORIENTED_EDGE ( 'NONE', *, *, #28042, .F. ) ;
#21869=DIRECTION ( 'NONE',  ( 0.000000000000000000, 0.7071067811865495711, 0.7071067811865455743 ) ) ;
#21870=CARTESIAN_POINT ( 'NONE',  ( -30.00000000000000000, -11.50000000000000000, 19.00000000000000000 ) ) ;
#21874=VERTEX_POINT ( 'NONE', #29245 ) ;
#21875=DIRECTION ( 'NONE',  ( -1.000000000000000000, 0.000000000000000000, 0.000000000000000000 ) ) ;
#21877=ORIENTED_EDGE ( 'NONE', *, *, #48311, .F. ) ;
#21885=ORIENTED_EDGE ( 'NONE', *, *, #7324, .F. ) ;
#21899=ADVANCED_FACE ( 'NONE', ( #67085 ), #66038, .F. ) ;
#21902=VECTOR ( 'NONE', #49453, 1000.000000000000000 ) ;
#21907=ORIENTED_EDGE ( 'NONE', *, *, #51281, .T. ) ;
#21915=CARTESIAN_POINT ( 'NONE',  ( 11.50000000000000000, -11.70000000000012008, 10.70000000000011831 ) ) ;
#21920=VECTOR ( 'NONE', #14950, 1000.000000000000000 ) ;
#21930=CARTESIAN_POINT ( 'NONE',  ( 11.00000000000000000, -12.00000000000000000, -12.20000000000000107 ) ) ;
#21942=CARTESIAN_POINT ( 'NONE',  ( 24.00000000000000000, -15.50000000000000000, -19.33772233983200195 ) ) ;
#21943=LINE ( 'NONE', #65767, #60624 ) ;
#21949=CARTESIAN_POINT ( 'NONE',  ( -11.00000000000000000, -9.487228132326899654, -12.50000000000000000 ) ) ;
#21951=VERTEX_POINT ( 'NONE', #14755 ) ;
#21954=CIRCLE ( 'NONE', #11788, 0.5000000000001392220 ) ;
#21955=VECTOR ( 'NONE', #38949, 1000.000000000000114 ) ;
#21964=CARTESIAN_POINT ( 'NONE',  ( 11.50000000000000000, -11.50000000000100009, 10.50000000000065903 ) ) ;
#21967=DIRECTION ( 'NONE',  ( 1.000000000000000000, -0.000000000000000000, -0.000000000000000000 ) ) ;
#21970=ORIENTED_EDGE ( 'NONE', *, *, #37172, .F. ) ;
#21988=EDGE_CURVE ( 'NONE', #29287, #43823, #46814, .T. ) ;
#21989=ORIENTED_EDGE ( 'NONE', *, *, #6013, .F. ) ;
#21991=DIRECTION ( 'NONE',  ( 0.000000000000000000, -0.1249999999999996531, -0.9921567416492215186 ) ) ;
#21998=ORIENTED_EDGE ( 'NONE', *, *, #49654, .F. ) ;
#22008=AXIS2_PLACEMENT_3D ( 'NONE', #47092, #35407, #3605 ) ;
#22010=LINE ( 'NONE', #43570, #30901 ) ;
#22011=ORIENTED_EDGE ( 'NONE', *, *, #14012, .F. ) ;
#22019=EDGE_CURVE ( 'NONE', #58904, #48024, #8378, .T. ) ;
#22023=VECTOR ( 'NONE', #68002, 1000.000000000000000 ) ;
#22024=LINE ( 'NONE', #43583, #24361 ) ;
#22029=LINE ( 'NONE', #38299, #45286 ) ;
#22030=VERTEX_POINT ( 'NONE', #37036 ) ;
#22031=CIRCLE ( 'NONE', #19786, 4.500000000000190958 ) ;
#22037=EDGE_CURVE ( 'NONE', #67299, #16582, #64903, .T. ) ;
#22039=ORIENTED_EDGE ( 'NONE', *, *, #26931, .F. ) ;
#22045=DIRECTION ( 'NONE',  ( 0.000000000000000000, -0.7046037717859445770, 0.7096009616573392131 ) ) ;
#22047=CARTESIAN_POINT ( 'NONE',  ( 11.75000000000000000, -5.000000000000000000, 26.25000000000000000 ) ) ;
#22054=EDGE_CURVE ( 'NONE', #13915, #14923, #41162, .T. ) ;
#22061=VERTEX_POINT ( 'NONE', #238 ) ;
#22072=AXIS2_PLACEMENT_3D ( 'NONE', #16349, #65487, #11046 ) ;
#22073=CARTESIAN_POINT ( 'NONE',  ( -11.00000000000000000, -12.00000000000000000, -10.20500000000000007 ) ) ;
#22075=ORIENTED_EDGE ( 'NONE', *, *, #19172, .F. ) ;
#22076=CARTESIAN_POINT ( 'NONE',  ( 15.50000000000000000, -1.037157890325000054, -22.50000000000000000 ) ) ;
#22081=DIRECTION ( 'NONE',  ( 0.4999999999999827360, 0.000000000000000000, -0.8660254037844485886 ) ) ;
#22090=EDGE_CURVE ( 'NONE', #28902, #9955, #15799, .T. ) ;
#22092=FACE_OUTER_BOUND ( 'NONE', #56566, .T. ) ;
#22093=EDGE_CURVE ( 'NONE', #66591, #39463, #43355, .T. ) ;
#22097=CARTESIAN_POINT ( 'NONE',  ( 11.00000000000000000, -15.97213595500069871, 14.50000000000000000 ) ) ;
#22109=CIRCLE ( 'NONE', #6300, 3.499999999999999556 ) ;
#22116=CYLINDRICAL_SURFACE ( 'NONE', #14231, 1.621000000000000885 ) ;
#22132=DIRECTION ( 'NONE',  ( 1.000000000000000000, 0.000000000000000000, 0.000000000000000000 ) ) ;
#22137=DIRECTION ( 'NONE',  ( -1.000000000000000000, 0.000000000000000000, 0.000000000000000000 ) ) ;
#22139=EDGE_CURVE ( 'NONE', #38571, #56028, #15804, .T. ) ;
#22146=ORIENTED_EDGE ( 'NONE', *, *, #61016, .F. ) ;
#22147=CARTESIAN_POINT ( 'NONE',  ( -15.50000000000000000, -15.50000000000000000, -22.50000000000000000 ) ) ;
#22152=AXIS2_PLACEMENT_3D ( 'NONE', #14667, #4073, #25640 ) ;
#22158=VECTOR ( 'NONE', #5340, 1000.000000000000000 ) ;
#22169=DIRECTION ( 'NONE',  ( 0.000000000000000000, 0.000000000000000000, -1.000000000000000000 ) ) ;
#22177=EDGE_CURVE ( 'NONE', #30033, #24504, #60333, .T. ) ;
#22178=AXIS2_PLACEMENT_3D ( 'NONE', #28781, #6869, #50359 ) ;
#22180=ORIENTED_EDGE ( 'NONE', *, *, #13986, .F. ) ;
#22205=ADVANCED_FACE ( 'NONE', ( #58492 ), #35849, .T. ) ;
#22212=DIRECTION ( 'NONE',  ( 0.000000000000000000, 1.000000000000000000, 0.000000000000000000 ) ) ;
#22217=CARTESIAN_POINT ( 'NONE',  ( -15.91242688423473517, -0.3152598339554900653, 21.29473909965994594 ) ) ;
#22224=LINE ( 'NONE', #43423, #17618 ) ;
#22228=AXIS2_PLACEMENT_3D ( 'NONE', #59777, #27264, #17323 ) ;
#22229=FACE_OUTER_BOUND ( 'NONE', #42832, .T. ) ;
#22232=DIRECTION ( 'NONE',  ( 0.4999999999989410693, 0.000000000000000000, -0.8660254037850499964 ) ) ;
#22233=LINE ( 'NONE', #27191, #22831 ) ;
#22239=LINE ( 'NONE', #65372, #9636 ) ;
#22245=CARTESIAN_POINT ( 'NONE',  ( 16.75000000000000000, -0.2038245569916320166, -23.22168783648699986 ) ) ;
#22255=VERTEX_POINT ( 'NONE', #30899 ) ;
#22256=ORIENTED_EDGE ( 'NONE', *, *, #41195, .F. ) ;
#22258=ORIENTED_EDGE ( 'NONE', *, *, #69942, .T. ) ;
#22272=VECTOR ( 'NONE', #37139, 1000.000000000000000 ) ;
#22279=ORIENTED_EDGE ( 'NONE', *, *, #9200, .F. ) ;
#22281=AXIS2_PLACEMENT_3D ( 'NONE', #58642, #63948, #42369 ) ;
#22287=DIRECTION ( 'NONE',  ( 0.000000000000000000, 1.000000000000000000, 0.000000000000000000 ) ) ;
#22291=CARTESIAN_POINT ( 'NONE',  ( 25.49999999999869971, -15.50000000000000000, -22.50000000000000000 ) ) ;
#22302=CARTESIAN_POINT ( 'NONE',  ( -15.50000000000000000, -0.1999999999999999556, 22.50000000000000000 ) ) ;
#22305=CARTESIAN_POINT ( 'NONE',  ( 30.00000000000000000, -16.28999999999999915, 14.50000000000000000 ) ) ;
#22321=CARTESIAN_POINT ( 'NONE',  ( 30.00000000000000000, -11.50000000000000000, -19.00000000000000000 ) ) ;
#22325=ORIENTED_EDGE ( 'NONE', *, *, #1537, .T. ) ;
#22330=DIRECTION ( 'NONE',  ( 0.000000000000000000, -0.9938079899998859545, 0.1111111111112941946 ) ) ;
#22336=AXIS2_PLACEMENT_3D ( 'NONE', #38477, #65001, #43077 ) ;
#22337=DIRECTION ( 'NONE',  ( 0.000000000000000000, 0.000000000000000000, 1.000000000000000000 ) ) ;
#22348=PLANE ( 'NONE',  #33998 ) ;
#22357=CARTESIAN_POINT ( 'NONE',  ( -30.00000000000000000, -9.200000000000120082, 17.64999999999993108 ) ) ;
#22358=ORIENTED_EDGE ( 'NONE', *, *, #38033, .F. ) ;
#22359=LINE ( 'NONE', #37578, #21747 ) ;
#22372=LINE ( 'NONE', #43918, #59118 ) ;
#22390=EDGE_CURVE ( 'NONE', #64346, #1690, #17071, .T. ) ;
#22411=ORIENTED_EDGE ( 'NONE', *, *, #57919, .F. ) ;
#22412=DIRECTION ( 'NONE',  ( 1.000000000000000000, -0.000000000000000000, -0.000000000000000000 ) ) ;
#22415=VECTOR ( 'NONE', #44506, 1000.000000000000000 ) ;
#22427=AXIS2_PLACEMENT_3D ( 'NONE', #28378, #7844, #7148 ) ;
#22429=CARTESIAN_POINT ( 'NONE',  ( -30.00000000000000000, -9.454754784057099570, -17.53999999999999915 ) ) ;
#22432=DIRECTION ( 'NONE',  ( 0.000000000000000000, 1.000000000000000000, 0.000000000000000000 ) ) ;
#22436=EDGE_CURVE ( 'NONE', #11224, #49372, #26995, .T. ) ;
#22437=VERTEX_POINT ( 'NONE', #67240 ) ;
#22438=LINE ( 'NONE', #17818, #56973 ) ;
#22439=CARTESIAN_POINT ( 'NONE',  ( 15.50000000000000000, 0.000000000000000000, -26.50000000000000000 ) ) ;
#22441=CARTESIAN_POINT ( 'NONE',  ( 25.50000000000000355, -15.50000000000000000, 22.50000000000000000 ) ) ;
#22448=ORIENTED_EDGE ( 'NONE', *, *, #50456, .T. ) ;
#22449=EDGE_CURVE ( 'NONE', #56239, #45920, #24459, .T. ) ;
#22454=CYLINDRICAL_SURFACE ( 'NONE', #67773, 4.000000000000000000 ) ;
#22456=EDGE_CURVE ( 'NONE', #32779, #10509, #45307, .T. ) ;
#22457=CARTESIAN_POINT ( 'NONE',  ( 11.00000000000000000, -9.200000000000120082, 17.30000000000000071 ) ) ;
#22466=AXIS2_PLACEMENT_3D ( 'NONE', #36021, #38048, #212 ) ;
#22468=DIRECTION ( 'NONE',  ( -0.000000000000000000, 1.000000000000000000, -0.000000000000000000 ) ) ;
#22472=AXIS2_PLACEMENT_3D ( 'NONE', #19096, #50451, #18972 ) ;
#22479=CARTESIAN_POINT ( 'NONE',  ( -30.00000000000000000, -12.00000000000000000, -11.03137303340310282 ) ) ;
#22481=DIRECTION ( 'NONE',  ( -1.000000000000000000, 0.000000000000000000, 0.000000000000000000 ) ) ;
#22482=CIRCLE ( 'NONE', #21367, 0.3500000000002722600 ) ;
#22483=CARTESIAN_POINT ( 'NONE',  ( -30.00000000000000000, 0.000000000000000000, -27.00000000000000000 ) ) ;
#22485=CARTESIAN_POINT ( 'NONE',  ( 11.00000000000000000, -16.64230188589300141, 14.64519951917099583 ) ) ;
#22497=EDGE_LOOP ( 'NONE', ( #56786, #31418, #50348, #45613 ) ) ;
#22500=LINE ( 'NONE', #7249, #26650 ) ;
#22507=DIRECTION ( 'NONE',  ( 0.000000000000000000, 0.000000000000000000, 1.000000000000000000 ) ) ;
#22510=AXIS2_PLACEMENT_3D ( 'NONE', #35766, #25171, #3247 ) ;
#22516=ORIENTED_EDGE ( 'NONE', *, *, #42974, .T. ) ;
#22519=CARTESIAN_POINT ( 'NONE',  ( -29.50000000000000355, -12.00000000000000000, 11.03137303340310282 ) ) ;
#22527=DIRECTION ( 'NONE',  ( -1.000000000000000000, 0.000000000000000000, 0.000000000000000000 ) ) ;
#22529=CARTESIAN_POINT ( 'NONE',  ( -30.00000000000000000, -8.959999999999999076, -12.95475478405700009 ) ) ;
#22532=ORIENTED_EDGE ( 'NONE', *, *, #26635, .F. ) ;
#22544=LINE ( 'NONE', #33491, #63144 ) ;
#22557=CARTESIAN_POINT ( 'NONE',  ( 30.00000000000000000, -16.64230188589299786, -14.64519951917100116 ) ) ;
#22573=EDGE_LOOP ( 'NONE', ( #61536, #12927, #6706, #63031, #63621 ) ) ;
#22576=ORIENTED_EDGE ( 'NONE', *, *, #9587, .F. ) ;
#22593=VECTOR ( 'NONE', #68421, 1000.000000000000000 ) ;
#22596=ORIENTED_EDGE ( 'NONE', *, *, #45597, .F. ) ;
#22598=DIRECTION ( 'NONE',  ( 0.4999999999989410693, 0.000000000000000000, 0.8660254037850499964 ) ) ;
#22603=AXIS2_PLACEMENT_3D ( 'NONE', #51518, #34881, #51156 ) ;
#22607=VERTEX_POINT ( 'NONE', #50217 ) ;
#22608=CARTESIAN_POINT ( 'NONE',  ( -28.00000000000000000, -16.64230188589299786, -14.64519951917100116 ) ) ;
#22615=EDGE_CURVE ( 'NONE', #30686, #10280, #39262, .T. ) ;
#22630=ORIENTED_EDGE ( 'NONE', *, *, #62587, .T. ) ;
#22634=ORIENTED_EDGE ( 'NONE', *, *, #8576, .T. ) ;
#22641=DIRECTION ( 'NONE',  ( 0.000000000000000000, 0.000000000000000000, -1.000000000000000000 ) ) ;
#22644=ORIENTED_EDGE ( 'NONE', *, *, #48130, .F. ) ;
#22645=CARTESIAN_POINT ( 'NONE',  ( 30.00000000000000000, -10.85999999999999943, 9.000000000000001776 ) ) ;
#22661=EDGE_LOOP ( 'NONE', ( #44011, #28078, #46162, #67333 ) ) ;
#22677=VERTEX_POINT ( 'NONE', #22997 ) ;
#22682=DIRECTION ( 'NONE',  ( 1.000000000000000000, -0.000000000000000000, -0.000000000000000000 ) ) ;
#22683=VECTOR ( 'NONE', #10883, 1000.000000000000000 ) ;
#22690=EDGE_LOOP ( 'NONE', ( #40668, #34411, #17617, #63479 ) ) ;
#22692=ORIENTED_EDGE ( 'NONE', *, *, #54510, .F. ) ;
#22700=ADVANCED_FACE ( 'NONE', ( #3780 ), #25354, .F. ) ;
#22707=VERTEX_POINT ( 'NONE', #9805 ) ;
#22715=DIRECTION ( 'NONE',  ( 0.000000000000000000, 0.000000000000000000, -1.000000000000000000 ) ) ;
#22716=CARTESIAN_POINT ( 'NONE',  ( -11.75000000000000000, -5.200000000000001066, 11.75000000000000000 ) ) ;
#22719=CIRCLE ( 'NONE', #3495, 3.499999999999999556 ) ;
#22725=VERTEX_POINT ( 'NONE', #26403 ) ;
#22728=ORIENTED_EDGE ( 'NONE', *, *, #9017, .T. ) ;
#22739=VECTOR ( 'NONE', #5780, 1000.000000000000000 ) ;
#22746=DIRECTION ( 'NONE',  ( -1.000000000000000000, 0.000000000000000000, 0.000000000000000000 ) ) ;
#22753=CIRCLE ( 'NONE', #30684, 2.000000000000001776 ) ;
#22759=VERTEX_POINT ( 'NONE', #47969 ) ;
#22760=AXIS2_PLACEMENT_3D ( 'NONE', #33290, #43199, #54864 ) ;
#22768=EDGE_LOOP ( 'NONE', ( #39570, #53522, #52750, #11997 ) ) ;
#22775=CARTESIAN_POINT ( 'NONE',  ( 0.000000000000000000, 0.000000000000000000, 0.000000000000000000 ) ) ;
#22784=EDGE_CURVE ( 'NONE', #50247, #14428, #32413, .T. ) ;
#22786=ORIENTED_EDGE ( 'NONE', *, *, #62841, .T. ) ;
#22794=PLANE ( 'NONE',  #69568 ) ;
#22796=CIRCLE ( 'NONE', #66786, 0.2000000000005226763 ) ;
#22804=LINE ( 'NONE', #50366, #32718 ) ;
#22813=VECTOR ( 'NONE', #67259, 1000.000000000000000 ) ;
#22823=ORIENTED_EDGE ( 'NONE', *, *, #36402, .F. ) ;
#22828=ORIENTED_EDGE ( 'NONE', *, *, #14152, .F. ) ;
#22831=VECTOR ( 'NONE', #12275, 1000.000000000000000 ) ;
#22833=DIRECTION ( 'NONE',  ( 0.000000000000000000, 1.000000000000000000, 0.000000000000000000 ) ) ;
#22839=DIRECTION ( 'NONE',  ( 1.000000000000000000, -0.000000000000000000, -0.000000000000000000 ) ) ;
#22844=CARTESIAN_POINT ( 'NONE',  ( -25.50000000000000355, -15.50000000000000000, -25.99999999999985079 ) ) ;
#22845=EDGE_CURVE ( 'NONE', #23822, #11704, #27445, .T. ) ;
#22855=EDGE_CURVE ( 'NONE', #49549, #45382, #49016, .T. ) ;
#22867=VERTEX_POINT ( 'NONE', #54325 ) ;
#22888=ORIENTED_EDGE ( 'NONE', *, *, #55202, .F. ) ;
#22891=FACE_OUTER_BOUND ( 'NONE', #53043, .T. ) ;
#22893=CARTESIAN_POINT ( 'NONE',  ( -11.00000000000000000, -11.50000000000000000, 11.00000000000000000 ) ) ;
#22907=CARTESIAN_POINT ( 'NONE',  ( 15.50000000000000000, -2.500000000000000000, 21.05662432702600029 ) ) ;
#22910=FACE_OUTER_BOUND ( 'NONE', #62851, .T. ) ;
#22912=CARTESIAN_POINT ( 'NONE',  ( -29.25000000000000000, -5.000000000000000000, -26.25000000000000000 ) ) ;
#22931=EDGE_LOOP ( 'NONE', ( #44928, #35972 ) ) ;
#22936=CARTESIAN_POINT ( 'NONE',  ( 11.00000000000000000, -8.959999999999999076, -12.95475478405700009 ) ) ;
#22939=VERTEX_POINT ( 'NONE', #1958 ) ;
#22944=ORIENTED_EDGE ( 'NONE', *, *, #14021, .T. ) ;
#22954=EDGE_LOOP ( 'NONE', ( #51362, #31090, #35915, #66013 ) ) ;
#22955=ORIENTED_EDGE ( 'NONE', *, *, #65636, .F. ) ;
#22956=VECTOR ( 'NONE', #53549, 1000.000000000000000 ) ;
#22962=DIRECTION ( 'NONE',  ( -0.000000000000000000, 1.000000000000000000, -0.000000000000000000 ) ) ;
#22971=DIRECTION ( 'NONE',  ( -0.000000000000000000, 1.000000000000000000, -0.000000000000000000 ) ) ;
#22975=CIRCLE ( 'NONE', #56834, 0.2000000000005261458 ) ;
#22980=VERTEX_POINT ( 'NONE', #41536 ) ;
#22981=CARTESIAN_POINT ( 'NONE',  ( -28.00000000000000000, -17.50000000000000000, -15.70500000000000007 ) ) ;
#22995=ORIENTED_EDGE ( 'NONE', *, *, #28881, .T. ) ;
#22997=CARTESIAN_POINT ( 'NONE',  ( 29.50000000000000355, -11.50000000000000000, 19.00000000000000000 ) ) ;
#22999=EDGE_CURVE ( 'NONE', #22939, #50838, #14335, .T. ) ;
#23005=EDGE_CURVE ( 'NONE', #9490, #39690, #17703, .T. ) ;
#23019=LINE ( 'NONE', #44569, #14896 ) ;
#23021=DIRECTION ( 'NONE',  ( 0.000000000000000000, 0.000000000000000000, 1.000000000000000000 ) ) ;
#23028=ORIENTED_EDGE ( 'NONE', *, *, #63917, .F. ) ;
#23035=ORIENTED_EDGE ( 'NONE', *, *, #67472, .F. ) ;
#23046=CARTESIAN_POINT ( 'NONE',  ( -29.50000000000000355, -12.00000000000000000, 11.00000000000000000 ) ) ;
#23047=ORIENTED_EDGE ( 'NONE', *, *, #63111, .T. ) ;
#23061=DIRECTION ( 'NONE',  ( 0.000000000000000000, 1.000000000000000000, 0.000000000000000000 ) ) ;
#23063=EDGE_LOOP ( 'NONE', ( #52290, #54710 ) ) ;
#23064=DIRECTION ( 'NONE',  ( 1.000000000000000000, -0.000000000000000000, -0.000000000000000000 ) ) ;
#23069=DIRECTION ( 'NONE',  ( 0.000000000000000000, 1.000000000000000000, 0.000000000000000000 ) ) ;
#23071=DIRECTION ( 'NONE',  ( -1.000000000000000000, 0.000000000000000000, 0.000000000000000000 ) ) ;
#23074=CARTESIAN_POINT ( 'NONE',  ( 30.00000000000000000, -5.200000000000001066, -26.59999999999999787 ) ) ;
#23076=VERTEX_POINT ( 'NONE', #35509 ) ;
#23080=EDGE_CURVE ( 'NONE', #36191, #6937, #30823, .T. ) ;
#23082=DIRECTION ( 'NONE',  ( 0.000000000000000000, 0.000000000000000000, 1.000000000000000000 ) ) ;
#23083=EDGE_LOOP ( 'NONE', ( #66860, #46680, #9463, #5128 ) ) ;
#23088=ORIENTED_EDGE ( 'NONE', *, *, #11160, .F. ) ;
#23092=CYLINDRICAL_SURFACE ( 'NONE', #10300, 1.621000000000000885 ) ;
#23095=EDGE_LOOP ( 'NONE', ( #20151, #59295, #60898, #13610 ) ) ;
#23099=CARTESIAN_POINT ( 'NONE',  ( -30.00000000000000000, -16.28999999999999915, 14.50000000000000000 ) ) ;
#23103=DIRECTION ( 'NONE',  ( 1.000000000000000000, -0.000000000000000000, -0.000000000000000000 ) ) ;
#23106=ORIENTED_EDGE ( 'NONE', *, *, #33430, .T. ) ;
#23109=ORIENTED_EDGE ( 'NONE', *, *, #53850, .T. ) ;
#23110=CYLINDRICAL_SURFACE ( 'NONE', #24229, 0.4999999999991868727 ) ;
#23111=CYLINDRICAL_SURFACE ( 'NONE', #45602, 4.000000000000000000 ) ;
#23114=AXIS2_PLACEMENT_3D ( 'NONE', #38814, #45497, #55773 ) ;
#23120=AXIS2_PLACEMENT_3D ( 'NONE', #23286, #39880, #44849 ) ;
#23123=ORIENTED_EDGE ( 'NONE', *, *, #38619, .T. ) ;
#23125=ORIENTED_EDGE ( 'NONE', *, *, #34185, .F. ) ;
#23126=ORIENTED_EDGE ( 'NONE', *, *, #37486, .F. ) ;
#23127=DIRECTION ( 'NONE',  ( 1.000000000000000000, -0.000000000000000000, -0.000000000000000000 ) ) ;
#23128=DIRECTION ( 'NONE',  ( -0.000000000000000000, 1.000000000000000000, -0.000000000000000000 ) ) ;
#23131=CARTESIAN_POINT ( 'NONE',  ( -14.10805890929250062, -5.000000000000000000, -26.25000000000000000 ) ) ;
#23135=EDGE_LOOP ( 'NONE', ( #1350, #64240, #30866, #13727 ) ) ;
#23139=CARTESIAN_POINT ( 'NONE',  ( 11.00000000000000000, -5.599999999999999645, 27.00000000000000000 ) ) ;
#23141=ORIENTED_EDGE ( 'NONE', *, *, #65118, .F. ) ;
#23143=AXIS2_PLACEMENT_3D ( 'NONE', #62545, #57256, #8820 ) ;
#23144=AXIS2_PLACEMENT_3D ( 'NONE', #15925, #64368, #59054 ) ;
#23162=EDGE_CURVE ( 'NONE', #14966, #27877, #66307, .T. ) ;
#23170=FACE_OUTER_BOUND ( 'NONE', #52840, .T. ) ;
#23173=DIRECTION ( 'NONE',  ( 0.000000000000000000, 0.000000000000000000, 1.000000000000000000 ) ) ;
#23189=ORIENTED_EDGE ( 'NONE', *, *, #56944, .T. ) ;
#23199=CIRCLE ( 'NONE', #29961, 1.449999999999996403 ) ;
#23200=VECTOR ( 'NONE', #36901, 1000.000000000000000 ) ;
#23201=ORIENTED_EDGE ( 'NONE', *, *, #56490, .F. ) ;
#23202=VERTEX_POINT ( 'NONE', #15719 ) ;
#23203=DIRECTION ( 'NONE',  ( 0.000000000000000000, -1.000000000000000000, 0.000000000000000000 ) ) ;
#23204=DIRECTION ( 'NONE',  ( 1.000000000000000000, -0.000000000000000000, -0.000000000000000000 ) ) ;
#23207=ORIENTED_EDGE ( 'NONE', *, *, #63154, .T. ) ;
#23209=VECTOR ( 'NONE', #63228, 1000.000000000000000 ) ;
#23211=DIRECTION ( 'NONE',  ( 0.000000000000000000, -1.000000000000000000, 0.000000000000000000 ) ) ;
#23212=ORIENTED_EDGE ( 'NONE', *, *, #55280, .T. ) ;
#23218=EDGE_LOOP ( 'NONE', ( #26373, #49403, #67963, #13357 ) ) ;
#23223=CARTESIAN_POINT ( 'NONE',  ( 29.25000000000000000, -5.200000000000001066, 26.25000000000000000 ) ) ;
#23224=CARTESIAN_POINT ( 'NONE',  ( -11.00000000000000000, -11.70000000000000284, 12.50000000000000000 ) ) ;
#23229=ORIENTED_EDGE ( 'NONE', *, *, #36280, .T. ) ;
#23236=DIRECTION ( 'NONE',  ( 0.000000000000000000, -0.9921567416492215186, 0.1249999999999996531 ) ) ;
#23248=FACE_BOUND ( 'NONE', #58372, .T. ) ;
#23249=CARTESIAN_POINT ( 'NONE',  ( 11.00000000000000000, -15.97213595500069871, 14.50000000000000000 ) ) ;
#23250=VECTOR ( 'NONE', #51063, 1000.000000000000000 ) ;
#23252=AXIS2_PLACEMENT_3D ( 'NONE', #14871, #69672, #62961 ) ;
#23254=EDGE_LOOP ( 'NONE', ( #57560, #61046, #24309, #56370 ) ) ;
#23257=EDGE_LOOP ( 'NONE', ( #53916, #22075, #301, #7667 ) ) ;
#23259=DIRECTION ( 'NONE',  ( -1.000000000000000000, 0.000000000000000000, 0.000000000000000000 ) ) ;
#23260=VECTOR ( 'NONE', #45388, 1000.000000000000000 ) ;
#23279=ORIENTED_EDGE ( 'NONE', *, *, #18068, .F. ) ;
#23281=DIRECTION ( 'NONE',  ( 0.9375000000000006661, 0.000000000000000000, -0.3479852726768744020 ) ) ;
#23284=ORIENTED_EDGE ( 'NONE', *, *, #12368, .T. ) ;
#23286=CARTESIAN_POINT ( 'NONE',  ( 30.00000000000000000, -16.28999999999999915, 14.50000000000000000 ) ) ;
#23293=EDGE_CURVE ( 'NONE', #44220, #28197, #12092, .T. ) ;
#23294=CIRCLE ( 'NONE', #49263, 4.000000000000000888 ) ;
#23295=AXIS2_PLACEMENT_3D ( 'NONE', #53088, #52745, #14187 ) ;
#23298=EDGE_CURVE ( 'NONE', #1375, #65337, #58412, .T. ) ;
#23304=ORIENTED_EDGE ( 'NONE', *, *, #43537, .F. ) ;
#23311=VERTEX_POINT ( 'NONE', #1193 ) ;
#23319=PLANE ( 'NONE',  #52073 ) ;
#23321=CARTESIAN_POINT ( 'NONE',  ( -29.25000000000000000, -5.200000000000001066, 26.25000000000000000 ) ) ;
#23326=CARTESIAN_POINT ( 'NONE',  ( 25.50000000000000355, -15.12100000000000044, -22.50000000000000000 ) ) ;
#23329=EDGE_CURVE ( 'NONE', #30577, #38571, #54248, .T. ) ;
#23330=EDGE_CURVE ( 'NONE', #46437, #10205, #6460, .T. ) ;
#23332=CARTESIAN_POINT ( 'NONE',  ( -13.00000000000000178, -16.28999999999710369, -14.50000000000000000 ) ) ;
#23334=DIRECTION ( 'NONE',  ( 0.000000000000000000, -0.6857142857147903170, -0.7278708115913530285 ) ) ;
#23336=ADVANCED_FACE ( 'NONE', ( #28063 ), #60911, .T. ) ;
#23337=CARTESIAN_POINT ( 'NONE',  ( -17.00000000000000000, -17.35230188589299871, -15.35019951917099945 ) ) ;
#23341=AXIS2_PLACEMENT_3D ( 'NONE', #56216, #34274, #55861 ) ;
#23345=ORIENTED_EDGE ( 'NONE', *, *, #9509, .F. ) ;
#23361=ORIENTED_EDGE ( 'NONE', *, *, #35701, .F. ) ;
#23368=CARTESIAN_POINT ( 'NONE',  ( -11.00000000000000000, -10.85999999999999943, 9.000000000000001776 ) ) ;
#23371=CARTESIAN_POINT ( 'NONE',  ( 29.50000000000000355, -12.00000000000000000, -11.00000000000000000 ) ) ;
#23398=ORIENTED_EDGE ( 'NONE', *, *, #40087, .T. ) ;
#23399=ORIENTED_EDGE ( 'NONE', *, *, #55194, .F. ) ;
#23403=CARTESIAN_POINT ( 'NONE',  ( -11.50000000000000000, -11.70000000000012008, 10.70000000000011831 ) ) ;
#23412=ORIENTED_EDGE ( 'NONE', *, *, #50464, .F. ) ;
#23426=EDGE_LOOP ( 'NONE', ( #24603, #18041, #45133, #973 ) ) ;
#23428=CARTESIAN_POINT ( 'NONE',  ( -11.50000000000000000, -11.50000000000100009, 10.50000000000065903 ) ) ;
#23431=DIRECTION ( 'NONE',  ( -1.000000000000000000, 0.000000000000000000, 0.000000000000000000 ) ) ;
#23432=CARTESIAN_POINT ( 'NONE',  ( 15.50000000000000000, -0.4000000000005274892, -22.50000000000000000 ) ) ;
#23437=ADVANCED_FACE ( 'NONE', ( #35080 ), #35430, .T. ) ;
#23443=EDGE_CURVE ( 'NONE', #11065, #8763, #8563, .T. ) ;
#23447=VERTEX_POINT ( 'NONE', #61598 ) ;
#23453=LINE ( 'NONE', #66582, #19279 ) ;
#23462=VECTOR ( 'NONE', #61580, 1000.000000000000000 ) ;
#23463=AXIS2_PLACEMENT_3D ( 'NONE', #28162, #16523, #61015 ) ;
#23476=ORIENTED_EDGE ( 'NONE', *, *, #28835, .F. ) ;
#23490=DIRECTION ( 'NONE',  ( 0.000000000000000000, 1.000000000000000000, 0.000000000000000000 ) ) ;
#23491=EDGE_CURVE ( 'NONE', #37646, #25470, #7860, .T. ) ;
#23494=CARTESIAN_POINT ( 'NONE',  ( -11.00000000000000000, -9.454754784057099570, 17.53999999999999915 ) ) ;
#23496=ORIENTED_EDGE ( 'NONE', *, *, #68175, .T. ) ;
#23502=AXIS2_PLACEMENT_3D ( 'NONE', #48771, #32852, #10585 ) ;
#23507=CARTESIAN_POINT ( 'NONE',  ( 11.00000000000000000, -17.14999999999900027, 27.00000000000000000 ) ) ;
#23510=CARTESIAN_POINT ( 'NONE',  ( 30.00000000000000000, -9.199999999999999289, -12.69999999999986073 ) ) ;
#23516=DIRECTION ( 'NONE',  ( 0.000000000000000000, 0.000000000000000000, 1.000000000000000000 ) ) ;
#23517=PLANE ( 'NONE',  #38789 ) ;
#23519=EDGE_CURVE ( 'NONE', #4367, #46404, #29103, .T. ) ;
#23524=ORIENTED_EDGE ( 'NONE', *, *, #30536, .F. ) ;
#23525=CARTESIAN_POINT ( 'NONE',  ( -14.45366306705349224, -0.2717122460102528447, -21.66072723692568402 ) ) ;
#23528=EDGE_CURVE ( 'NONE', #15458, #22255, #14577, .T. ) ;
#23533=ORIENTED_EDGE ( 'NONE', *, *, #56636, .T. ) ;
#23534=CARTESIAN_POINT ( 'NONE',  ( -11.75000000000000000, -5.000000000000000000, 11.75000000000000000 ) ) ;
#23542=DIRECTION ( 'NONE',  ( 0.000000000000000000, 0.000000000000000000, 1.000000000000000000 ) ) ;
#23554=ORIENTED_EDGE ( 'NONE', *, *, #50061, .F. ) ;
#23556=DIRECTION ( 'NONE',  ( -1.000000000000000000, 0.000000000000000000, 0.000000000000000000 ) ) ;
#23562=DIRECTION ( 'NONE',  ( 0.000000000000000000, 0.000000000000000000, 1.000000000000000000 ) ) ;
#23565=ORIENTED_EDGE ( 'NONE', *, *, #14774, .T. ) ;
#23573=DIRECTION ( 'NONE',  ( 0.000000000000000000, 0.000000000000000000, -1.000000000000000000 ) ) ;
#23574=CARTESIAN_POINT ( 'NONE',  ( 11.00000000000000000, -11.50000000000100009, 10.50000000000065903 ) ) ;
#23590=DIRECTION ( 'NONE',  ( 1.000000000000000000, 0.000000000000000000, 0.000000000000000000 ) ) ;
#23594=ORIENTED_EDGE ( 'NONE', *, *, #47761, .F. ) ;
#23603=VECTOR ( 'NONE', #3090, 1000.000000000000000 ) ;
#23606=ORIENTED_EDGE ( 'NONE', *, *, #27971, .T. ) ;
#23609=DIRECTION ( 'NONE',  ( 1.000000000000000000, -0.000000000000000000, 1.224646799147353207E-16 ) ) ;
#23618=ORIENTED_EDGE ( 'NONE', *, *, #19975, .T. ) ;
#23619=ORIENTED_EDGE ( 'NONE', *, *, #48647, .F. ) ;
#23622=CARTESIAN_POINT ( 'NONE',  ( 11.50000000000000000, -11.50000000000100009, 15.00000000000084910 ) ) ;
#23627=CARTESIAN_POINT ( 'NONE',  ( -24.00000000000000000, -15.50000000000000000, 2.000000000000000000 ) ) ;
#23631=ORIENTED_EDGE ( 'NONE', *, *, #37882, .T. ) ;
#23637=AXIS2_PLACEMENT_3D ( 'NONE', #27909, #12306, #21560 ) ;
#23641=EDGE_CURVE ( 'NONE', #52042, #68236, #4304, .T. ) ;
#23652=EDGE_CURVE ( 'NONE', #57801, #47666, #52418, .T. ) ;
#23656=AXIS2_PLACEMENT_3D ( 'NONE', #66310, #24217, #56736 ) ;
#23657=DIRECTION ( 'NONE',  ( -1.000000000000000000, 0.000000000000000000, 0.000000000000000000 ) ) ;
#23662=CARTESIAN_POINT ( 'NONE',  ( -23.75054448485400016, -17.50000000000000000, 25.53140320652400064 ) ) ;
#23663=AXIS2_PLACEMENT_3D ( 'NONE', #12864, #11831, #61306 ) ;
#23670=CARTESIAN_POINT ( 'NONE',  ( -30.00000000000000000, -12.00000000000000000, -10.20500000000000007 ) ) ;
#23671=DIRECTION ( 'NONE',  ( 0.4999999999989410693, 0.000000000000000000, -0.8660254037850499964 ) ) ;
#23674=CARTESIAN_POINT ( 'NONE',  ( 23.75054448485400016, -17.50000000000000000, -25.53140320652400064 ) ) ;
#23676=ADVANCED_FACE ( 'NONE', ( #66143, #48507 ), #416, .T. ) ;
#23688=VECTOR ( 'NONE', #14337, 1000.000000000000000 ) ;
#23701=AXIS2_PLACEMENT_3D ( 'NONE', #66041, #49460, #43439 ) ;
#23702=CYLINDRICAL_SURFACE ( 'NONE', #12891, 1.621000000000000885 ) ;
#23707=ORIENTED_EDGE ( 'NONE', *, *, #65636, .T. ) ;
#23709=CYLINDRICAL_SURFACE ( 'NONE', #5856, 0.3499999999998886224 ) ;
#23710=ORIENTED_EDGE ( 'NONE', *, *, #6932, .T. ) ;
#23711=VECTOR ( 'NONE', #3265, 1000.000000000000000 ) ;
#23716=EDGE_CURVE ( 'NONE', #57835, #29890, #64120, .T. ) ;
#23730=DIRECTION ( 'NONE',  ( 0.000000000000000000, 0.000000000000000000, 1.000000000000000000 ) ) ;
#23731=EDGE_CURVE ( 'NONE', #32488, #48332, #47188, .T. ) ;
#23735=ORIENTED_EDGE ( 'NONE', *, *, #53243, .T. ) ;
#23738=CARTESIAN_POINT ( 'NONE',  ( 15.50000000000000000, -2.500000000000000000, 23.94337567297399971 ) ) ;
#23746=VERTEX_POINT ( 'NONE', #56235 ) ;
#23747=EDGE_CURVE ( 'NONE', #67807, #20681, #2832, .T. ) ;
#23748=VECTOR ( 'NONE', #53987, 1000.000000000000000 ) ;
#23750=DIRECTION ( 'NONE',  ( -1.000000000000000000, 0.000000000000000000, 0.000000000000000000 ) ) ;
#23757=PLANE ( 'NONE',  #5799 ) ;
#23770=CARTESIAN_POINT ( 'NONE',  ( -24.00000000000000000, -17.35230188589299871, 15.35019951917099945 ) ) ;
#23772=CIRCLE ( 'NONE', #53185, 3.499999999999999556 ) ;
#23774=CARTESIAN_POINT ( 'NONE',  ( 30.00000000000000000, -5.200000000000001066, -9.400000000000000355 ) ) ;
#23779=EDGE_CURVE ( 'NONE', #49938, #32123, #66488, .T. ) ;
#23781=EDGE_LOOP ( 'NONE', ( #4088, #28730, #47134, #42071 ) ) ;
#23784=ORIENTED_EDGE ( 'NONE', *, *, #28044, .F. ) ;
#23786=ORIENTED_EDGE ( 'NONE', *, *, #13063, .T. ) ;
#23796=ORIENTED_EDGE ( 'NONE', *, *, #32161, .F. ) ;
#23806=CARTESIAN_POINT ( 'NONE',  ( 11.00000000000000000, -17.50000000000000000, -26.64999999999900027 ) ) ;
#23814=CARTESIAN_POINT ( 'NONE',  ( -17.00000000000000000, -17.35230188589299516, -15.35019951917100478 ) ) ;
#23822=VERTEX_POINT ( 'NONE', #7779 ) ;
#23827=VERTEX_POINT ( 'NONE', #14140 ) ;
#23828=FACE_OUTER_BOUND ( 'NONE', #13207, .T. ) ;
#23830=DIRECTION ( 'NONE',  ( -1.000000000000000000, 0.000000000000000000, 0.000000000000000000 ) ) ;
#23833=EDGE_CURVE ( 'NONE', #64699, #3316, #6515, .T. ) ;
#23834=LINE ( 'NONE', #8259, #34061 ) ;
#23838=ORIENTED_EDGE ( 'NONE', *, *, #52038, .T. ) ;
#23848=DIRECTION ( 'NONE',  ( -0.3479852726768751237, 0.000000000000000000, 0.9375000000000004441 ) ) ;
#23849=ORIENTED_EDGE ( 'NONE', *, *, #66895, .T. ) ;
#23855=CIRCLE ( 'NONE', #35103, 2.000000000000001776 ) ;
#23857=CARTESIAN_POINT ( 'NONE',  ( -11.75000000000000000, -5.200000000000001066, -11.75000000000000000 ) ) ;
#23866=EDGE_CURVE ( 'NONE', #28596, #12012, #50231, .T. ) ;
#23870=ORIENTED_EDGE ( 'NONE', *, *, #60447, .T. ) ;
#23872=CARTESIAN_POINT ( 'NONE',  ( 11.50000000000000000, -11.50000000000100009, 19.50000000000103739 ) ) ;
#23874=EDGE_CURVE ( 'NONE', #54299, #11406, #45973, .T. ) ;
#23875=FACE_OUTER_BOUND ( 'NONE', #66332, .T. ) ;
#23879=EDGE_CURVE ( 'NONE', #68528, #41558, #8124, .T. ) ;
#23887=EDGE_LOOP ( 'NONE', ( #6151, #15962, #48857, #43313 ) ) ;
#23901=DIRECTION ( 'NONE',  ( 0.8660254037844482555, 0.000000000000000000, 0.4999999999999831801 ) ) ;
#23906=AXIS2_PLACEMENT_3D ( 'NONE', #52331, #57279, #67546 ) ;
#23926=AXIS2_PLACEMENT_3D ( 'NONE', #52466, #63067, #63775 ) ;
#23930=DIRECTION ( 'NONE',  ( -0.4999999999999832356, 0.000000000000000000, -0.8660254037844483666 ) ) ;
#23932=DIRECTION ( 'NONE',  ( -1.000000000000000000, 0.000000000000000000, 0.000000000000000000 ) ) ;
#23940=DIRECTION ( 'NONE',  ( 0.000000000000000000, 0.000000000000000000, 1.000000000000000000 ) ) ;
#23944=CARTESIAN_POINT ( 'NONE',  ( 11.00000000000000000, -15.46862696659690073, -14.50000000000000000 ) ) ;
#23946=DIRECTION ( 'NONE',  ( -1.000000000000000000, 0.000000000000000000, 0.000000000000000000 ) ) ;
#23961=DIRECTION ( 'NONE',  ( 0.000000000000000000, 0.000000000000000000, 1.000000000000000000 ) ) ;
#23969=ORIENTED_EDGE ( 'NONE', *, *, #66697, .F. ) ;
#23976=CARTESIAN_POINT ( 'NONE',  ( 30.00000000000000000, -15.46862696659690073, -14.50000000000000000 ) ) ;
#23978=DIRECTION ( 'NONE',  ( 0.000000000000000000, -1.000000000000000000, 0.000000000000000000 ) ) ;
#23985=VERTEX_POINT ( 'NONE', #25107 ) ;
#23988=ORIENTED_EDGE ( 'NONE', *, *, #57919, .T. ) ;
#23991=ORIENTED_EDGE ( 'NONE', *, *, #4204, .F. ) ;
#23992=ORIENTED_EDGE ( 'NONE', *, *, #52477, .T. ) ;
#23993=CONICAL_SURFACE ( 'NONE', #19507, 1732.050807568789651, 1.047197551196575871 ) ;
#23994=EDGE_CURVE ( 'NONE', #5636, #16184, #35926, .T. ) ;
#24001=LINE ( 'NONE', #9150, #11387 ) ;
#24003=VECTOR ( 'NONE', #1890, 1000.000000000000114 ) ;
#24005=DIRECTION ( 'NONE',  ( 0.000000000000000000, 0.7071067811865450192, 0.7071067811865500152 ) ) ;
#24009=ORIENTED_EDGE ( 'NONE', *, *, #30540, .T. ) ;
#24014=LINE ( 'NONE', #14107, #13223 ) ;
#24015=DIRECTION ( 'NONE',  ( 0.4999999999989371835, 0.000000000000000000, 0.8660254037850523279 ) ) ;
#24020=DIRECTION ( 'NONE',  ( 0.000000000000000000, -0.7096009616570518874, -0.7046037717862339012 ) ) ;
#24037=EDGE_CURVE ( 'NONE', #12650, #9391, #26167, .T. ) ;
#24041=DIRECTION ( 'NONE',  ( 0.000000000000000000, 0.000000000000000000, 1.000000000000000000 ) ) ;
#24047=EDGE_CURVE ( 'NONE', #13228, #9204, #32560, .T. ) ;
#24055=DIRECTION ( 'NONE',  ( -1.000000000000000000, 0.000000000000000000, 0.000000000000000000 ) ) ;
#24057=ORIENTED_EDGE ( 'NONE', *, *, #39611, .T. ) ;
#24071=VERTEX_POINT ( 'NONE', #53391 ) ;
#24074=VECTOR ( 'NONE', #30015, 1000.000000000000000 ) ;
#24076=CARTESIAN_POINT ( 'NONE',  ( -25.50000000000000355, -15.12100000000000044, -24.12099999999999511 ) ) ;
#24077=CARTESIAN_POINT ( 'NONE',  ( 29.50000000000000355, -11.50000000000100009, 15.00000000000084910 ) ) ;
#24078=ADVANCED_FACE ( 'NONE', ( #49466 ), #44478, .T. ) ;
#24079=EDGE_LOOP ( 'NONE', ( #64091, #25694, #42011, #42607 ) ) ;
#24084=ORIENTED_EDGE ( 'NONE', *, *, #30756, .T. ) ;
#24086=VERTEX_POINT ( 'NONE', #5642 ) ;
#24087=FACE_BOUND ( 'NONE', #29510, .T. ) ;
#24088=CIRCLE ( 'NONE', #31890, 3.499999999999849454 ) ;
#24091=CARTESIAN_POINT ( 'NONE',  ( -23.75054448485400016, -17.50000000000000000, -25.53140320652400064 ) ) ;
#24092=FACE_OUTER_BOUND ( 'NONE', #40821, .T. ) ;
#24095=EDGE_LOOP ( 'NONE', ( #4256, #25792, #35543, #22728 ) ) ;
#24098=CARTESIAN_POINT ( 'NONE',  ( 24.00000000000000000, -15.50000000000000000, -2.000000000000000000 ) ) ;
#24106=DIRECTION ( 'NONE',  ( 0.000000000000000000, 1.000000000000000000, 0.000000000000000000 ) ) ;
#24112=EDGE_CURVE ( 'NONE', #32193, #5395, #47241, .T. ) ;
#24113=LINE ( 'NONE', #51704, #23462 ) ;
#24125=ORIENTED_EDGE ( 'NONE', *, *, #58978, .T. ) ;
#24127=LINE ( 'NONE', #45681, #60728 ) ;
#24130=EDGE_CURVE ( 'NONE', #4729, #1941, #53737, .T. ) ;
#24132=EDGE_LOOP ( 'NONE', ( #66483, #12456, #18305, #64983, #56257, #36001 ) ) ;
#24133=EDGE_CURVE ( 'NONE', #38291, #65451, #1033, .T. ) ;
#24143=LINE ( 'NONE', #18837, #52085 ) ;
#24152=LINE ( 'NONE', #40414, #46736 ) ;
#24168=VERTEX_POINT ( 'NONE', #65384 ) ;
#24171=DIRECTION ( 'NONE',  ( 1.000000000000000000, -0.000000000000000000, -0.000000000000000000 ) ) ;
#24173=VECTOR ( 'NONE', #4221, 1000.000000000000000 ) ;
#24182=VERTEX_POINT ( 'NONE', #38509 ) ;
#24183=EDGE_CURVE ( 'NONE', #51332, #17638, #54766, .T. ) ;
#24191=AXIS2_PLACEMENT_3D ( 'NONE', #52437, #63041, #58792 ) ;
#24197=EDGE_CURVE ( 'NONE', #42854, #16184, #2048, .T. ) ;
#24204=PLANE ( 'NONE',  #34705 ) ;
#24207=CARTESIAN_POINT ( 'NONE',  ( -15.50000000000000000, -2.500000000000000000, -21.05662432702600029 ) ) ;
#24212=DIRECTION ( 'NONE',  ( 1.060575238724892987E-16, 0.5000000000000199840, -0.8660254037844271613 ) ) ;
#24217=DIRECTION ( 'NONE',  ( 1.000000000000000000, 0.000000000000000000, 0.000000000000000000 ) ) ;
#24221=CARTESIAN_POINT ( 'NONE',  ( 15.50000000000000000, -15.50000000000000000, -22.50000000000000000 ) ) ;
#24226=CARTESIAN_POINT ( 'NONE',  ( -14.66434062215826017, -0.3156604612126701626, -21.53909249377373669 ) ) ;
#24229=AXIS2_PLACEMENT_3D ( 'NONE', #11802, #66255, #53320 ) ;
#24231=DIRECTION ( 'NONE',  ( 0.000000000000000000, 0.000000000000000000, -1.000000000000000000 ) ) ;
#24236=EDGE_CURVE ( 'NONE', #24071, #4441, #34565, .T. ) ;
#24238=CARTESIAN_POINT ( 'NONE',  ( -30.00000000000000000, -16.28999999999710369, 15.00000000000794920 ) ) ;
#24241=ORIENTED_EDGE ( 'NONE', *, *, #54384, .F. ) ;
#24243=VERTEX_POINT ( 'NONE', #66408 ) ;
#24257=ORIENTED_EDGE ( 'NONE', *, *, #66509, .T. ) ;
#24270=ADVANCED_FACE ( 'NONE', ( #18652 ), #13358, .F. ) ;
#24274=AXIS2_PLACEMENT_3D ( 'NONE', #5047, #58800, #31237 ) ;
#24275=EDGE_CURVE ( 'NONE', #65451, #57577, #50493, .T. ) ;
#24282=ORIENTED_EDGE ( 'NONE', *, *, #36367, .T. ) ;
#24283=ORIENTED_EDGE ( 'NONE', *, *, #33929, .F. ) ;
#24286=CARTESIAN_POINT ( 'NONE',  ( 13.00000000000000178, -17.00000000000000000, -15.70499999999969809 ) ) ;
#24287=CARTESIAN_POINT ( 'NONE',  ( -25.50000000000000355, -5.578999999999999737, 22.50000000000000000 ) ) ;
#24289=FACE_OUTER_BOUND ( 'NONE', #34817, .T. ) ;
#24292=DIRECTION ( 'NONE',  ( 1.000000000000000000, -0.000000000000000000, -0.000000000000000000 ) ) ;
#24294=DIRECTION ( 'NONE',  ( 0.000000000000000000, 1.000000000000000000, 0.000000000000000000 ) ) ;
#24297=DIRECTION ( 'NONE',  ( 0.000000000000000000, 0.000000000000000000, 1.000000000000000000 ) ) ;
#24298=ORIENTED_EDGE ( 'NONE', *, *, #11632, .T. ) ;
#24304=DIRECTION ( 'NONE',  ( -1.000000000000000000, 0.000000000000000000, 0.000000000000000000 ) ) ;
#24306=CIRCLE ( 'NONE', #69492, 0.5000000000079367624 ) ;
#24308=FACE_OUTER_BOUND ( 'NONE', #16087, .T. ) ;
#24309=ORIENTED_EDGE ( 'NONE', *, *, #11632, .F. ) ;
#24317=CARTESIAN_POINT ( 'NONE',  ( 29.50000000000000355, -11.50000000000000000, -15.00000000000000000 ) ) ;
#24320=DIRECTION ( 'NONE',  ( 0.000000000000000000, 0.000000000000000000, 1.000000000000000000 ) ) ;
#24325=DIRECTION ( 'NONE',  ( 1.000000000000000000, -0.000000000000000000, -0.000000000000000000 ) ) ;
#24328=DIRECTION ( 'NONE',  ( -1.000000000000000000, 0.000000000000000000, 0.000000000000000000 ) ) ;
#24331=CARTESIAN_POINT ( 'NONE',  ( -11.50000000000000000, -15.97213595500069871, 14.50000000000000000 ) ) ;
#24333=VECTOR ( 'NONE', #24212, 999.9999999999998863 ) ;
#24339=DIRECTION ( 'NONE',  ( 0.000000000000000000, -0.7046037717859411353, -0.7096009616573427659 ) ) ;
#24351=DIRECTION ( 'NONE',  ( -1.000000000000000000, 0.000000000000000000, 0.000000000000000000 ) ) ;
#24353=AXIS2_PLACEMENT_3D ( 'NONE', #9279, #30846, #3979 ) ;
#24355=PLANE ( 'NONE',  #50018 ) ;
#24357=EDGE_CURVE ( 'NONE', #7353, #12401, #9460, .T. ) ;
#24361=VECTOR ( 'NONE', #32975, 1000.000000000000000 ) ;
#24368=CARTESIAN_POINT ( 'NONE',  ( 30.00000000000000000, -5.000000000000000000, -27.00000000000000000 ) ) ;
#24371=AXIS2_PLACEMENT_3D ( 'NONE', #32036, #32386, #63153 ) ;
#24374=DIRECTION ( 'NONE',  ( 0.000000000000000000, -0.1249999999999996531, -0.9921567416492215186 ) ) ;
#24376=DIRECTION ( 'NONE',  ( 0.000000000000000000, -0.1111111111108840643, -0.9938079899999319178 ) ) ;
#24378=CARTESIAN_POINT ( 'NONE',  ( -15.50000000000000000, -0.4000000000000000222, -19.00000000000000355 ) ) ;
#24380=LINE ( 'NONE', #62199, #69657 ) ;
#24383=LINE ( 'NONE', #18721, #51417 ) ;
#24387=VECTOR ( 'NONE', #2031, 1000.000000000000114 ) ;
#24393=VERTEX_POINT ( 'NONE', #30677 ) ;
#24399=FACE_OUTER_BOUND ( 'NONE', #48688, .T. ) ;
#24408=EDGE_CURVE ( 'NONE', #60221, #52778, #2098, .T. ) ;
#24416=ORIENTED_EDGE ( 'NONE', *, *, #38445, .T. ) ;
#24425=DIRECTION ( 'NONE',  ( -1.000000000000000000, 0.000000000000000000, 0.000000000000000000 ) ) ;
#24440=VERTEX_POINT ( 'NONE', #52242 ) ;
#24441=VERTEX_POINT ( 'NONE', #19356 ) ;
#24447=FACE_OUTER_BOUND ( 'NONE', #46702, .T. ) ;
#24449=EDGE_CURVE ( 'NONE', #42297, #30976, #63907, .T. ) ;
#24452=DIRECTION ( 'NONE',  ( 0.000000000000000000, -1.000000000000000000, 0.000000000000000000 ) ) ;
#24453=EDGE_CURVE ( 'NONE', #62784, #6004, #37104, .T. ) ;
#24457=ORIENTED_EDGE ( 'NONE', *, *, #17801, .F. ) ;
#24459=LINE ( 'NONE', #13136, #5257 ) ;
#24460=ADVANCED_FACE ( 'NONE', ( #30326 ), #52957, .T. ) ;
#24462=DIRECTION ( 'NONE',  ( 0.000000000000000000, 1.000000000000000000, 0.000000000000000000 ) ) ;
#24464=CARTESIAN_POINT ( 'NONE',  ( 15.50000000000000000, -0.1999999999999999556, -23.94999999999999574 ) ) ;
#24465=LINE ( 'NONE', #46029, #1224 ) ;
#24467=ADVANCED_FACE ( 'NONE', ( #69202 ), #25025, .T. ) ;
#24468=DIRECTION ( 'NONE',  ( 0.000000000000000000, -1.000000000000000000, 6.036837696397648868E-13 ) ) ;
#24476=VECTOR ( 'NONE', #49496, 1000.000000000000000 ) ;
#24477=DIRECTION ( 'NONE',  ( 0.000000000000000000, 0.000000000000000000, 1.000000000000000000 ) ) ;
#24483=CARTESIAN_POINT ( 'NONE',  ( 30.00000000000000000, -9.199999999999999289, -12.69999999999986073 ) ) ;
#24484=ORIENTED_EDGE ( 'NONE', *, *, #44100, .F. ) ;
#24487=VECTOR ( 'NONE', #37853, 1000.000000000000000 ) ;
#24489=CIRCLE ( 'NONE', #9817, 0.5000000000079362072 ) ;
#24492=PLANE ( 'NONE',  #32757 ) ;
#24501=ORIENTED_EDGE ( 'NONE', *, *, #26218, .T. ) ;
#24504=VERTEX_POINT ( 'NONE', #64596 ) ;
#24508=DIRECTION ( 'NONE',  ( 0.000000000000000000, 1.000000000000000000, 0.000000000000000000 ) ) ;
#24512=LINE ( 'NONE', #46416, #33226 ) ;
#24513=EDGE_LOOP ( 'NONE', ( #20494, #59402, #35020, #51683 ) ) ;
#24514=VERTEX_POINT ( 'NONE', #12143 ) ;
#24517=AXIS2_PLACEMENT_3D ( 'NONE', #42026, #63606, #63249 ) ;
#24526=VERTEX_POINT ( 'NONE', #60584 ) ;
#24530=CARTESIAN_POINT ( 'NONE',  ( 25.50000000000000355, 0.000000000000000000, -20.87899999999999778 ) ) ;
#24531=VECTOR ( 'NONE', #33076, 1000.000000000000000 ) ;
#24535=DIRECTION ( 'NONE',  ( 0.000000000000000000, 0.7071067811865495711, -0.7071067811865455743 ) ) ;
#24537=VERTEX_POINT ( 'NONE', #12821 ) ;
#24539=CARTESIAN_POINT ( 'NONE',  ( -15.50000000000000000, -0.2038245569916614930, -23.94337567297399971 ) ) ;
#24551=PLANE ( 'NONE',  #9705 ) ;
#24559=AXIS2_PLACEMENT_3D ( 'NONE', #15544, #21869, #21523 ) ;
#24561=DIRECTION ( 'NONE',  ( -1.000000000000000000, 0.000000000000000000, 0.000000000000000000 ) ) ;
#24576=CARTESIAN_POINT ( 'NONE',  ( 11.75000000000000000, -5.200000000000001066, -11.75000000000000000 ) ) ;
#24577=AXIS2_PLACEMENT_3D ( 'NONE', #60557, #1502, #66214 ) ;
#24578=CARTESIAN_POINT ( 'NONE',  ( -30.00000000000000000, -17.00000000000000000, -15.70499999999969809 ) ) ;
#24584=CARTESIAN_POINT ( 'NONE',  ( -30.00000000000000000, -17.35230188589299871, 15.35019951917099945 ) ) ;
#24587=CARTESIAN_POINT ( 'NONE',  ( 25.50000000000000355, -5.578999999999999737, 24.12099999999999866 ) ) ;
#24593=CARTESIAN_POINT ( 'NONE',  ( 30.00000000000000000, -11.10796162543699950, -9.102987789146602893 ) ) ;
#24598=DIRECTION ( 'NONE',  ( 0.000000000000000000, -0.1249999999999996531, -0.9921567416492215186 ) ) ;
#24602=EDGE_CURVE ( 'NONE', #49081, #42236, #34386, .T. ) ;
#24603=ORIENTED_EDGE ( 'NONE', *, *, #15083, .T. ) ;
#24609=VERTEX_POINT ( 'NONE', #21459 ) ;
#24616=ADVANCED_FACE ( 'NONE', ( #10499 ), #5211, .F. ) ;
#24655=EDGE_LOOP ( 'NONE', ( #61893, #1716, #20841, #35562, #52620, #60942 ) ) ;
#24662=CARTESIAN_POINT ( 'NONE',  ( -11.00000000000000000, -8.959999999999999076, -12.95475478405700009 ) ) ;
#24663=DIRECTION ( 'NONE',  ( 1.000000000000000000, 0.000000000000000000, 0.000000000000000000 ) ) ;
#24666=EDGE_CURVE ( 'NONE', #8384, #24071, #42739, .T. ) ;
#24677=DIRECTION ( 'NONE',  ( 1.000000000000000000, -0.000000000000000000, -0.000000000000000000 ) ) ;
#24683=ORIENTED_EDGE ( 'NONE', *, *, #62949, .F. ) ;
#24701=DIRECTION ( 'NONE',  ( -1.000000000000000000, 0.000000000000000000, 0.000000000000000000 ) ) ;
#24710=DIRECTION ( 'NONE',  ( 0.000000000000000000, 1.000000000000000000, 0.000000000000000000 ) ) ;
#24712=ORIENTED_EDGE ( 'NONE', *, *, #27239, .F. ) ;
#24723=AXIS2_PLACEMENT_3D ( 'NONE', #34351, #17769, #60884 ) ;
#24725=FACE_OUTER_BOUND ( 'NONE', #11557, .T. ) ;
#24729=ORIENTED_EDGE ( 'NONE', *, *, #1530, .T. ) ;
#24735=FACE_OUTER_BOUND ( 'NONE', #39251, .T. ) ;
#24739=VECTOR ( 'NONE', #57685, 1000.000000000000114 ) ;
#24741=ORIENTED_EDGE ( 'NONE', *, *, #35118, .T. ) ;
#24743=CARTESIAN_POINT ( 'NONE',  ( -30.00000000000000000, -5.000000000000000000, 27.00000000000000000 ) ) ;
#24745=CARTESIAN_POINT ( 'NONE',  ( 30.00000000000000000, -9.200000000000120082, 17.64999999999993108 ) ) ;
#24749=CARTESIAN_POINT ( 'NONE',  ( 24.00000000000000000, -16.28999999999999915, -14.50000000000000000 ) ) ;
#24751=DIRECTION ( 'NONE',  ( 0.000000000000000000, -0.9921567416492215186, 0.1249999999999996531 ) ) ;
#24752=ORIENTED_EDGE ( 'NONE', *, *, #13359, .F. ) ;
#24772=FACE_OUTER_BOUND ( 'NONE', #38407, .T. ) ;
#24780=VERTEX_POINT ( 'NONE', #52430 ) ;
#24785=TOROIDAL_SURFACE ( 'NONE', #21402, 3.299999999999470024, 0.2000000000005275058 ) ;
#24790=ORIENTED_EDGE ( 'NONE', *, *, #23879, .T. ) ;
#24796=DIRECTION ( 'NONE',  ( 0.000000000000000000, -1.000000000000000000, 0.000000000000000000 ) ) ;
#24799=FACE_OUTER_BOUND ( 'NONE', #56091, .T. ) ;
#24803=EDGE_CURVE ( 'NONE', #25888, #20510, #54109, .T. ) ;
#24804=ORIENTED_EDGE ( 'NONE', *, *, #19778, .T. ) ;
#24806=EDGE_CURVE ( 'NONE', #14976, #41912, #4356, .T. ) ;
#24812=ADVANCED_FACE ( 'NONE', ( #14948 ), #19107, .F. ) ;
#24814=CARTESIAN_POINT ( 'NONE',  ( -23.75054448485400016, -15.50000000000000000, 25.53140320652400064 ) ) ;
#24818=DIRECTION ( 'NONE',  ( 1.000000000000000000, 0.000000000000000000, 0.000000000000000000 ) ) ;
#24821=DIRECTION ( 'NONE',  ( 0.000000000000000000, 1.000000000000000000, 0.000000000000000000 ) ) ;
#24823=DIRECTION ( 'NONE',  ( 0.000000000000000000, -1.000000000000000000, 0.000000000000000000 ) ) ;
#24829=EDGE_LOOP ( 'NONE', ( #5530, #47834, #49944, #17546, #19200, #27391 ) ) ;
#24830=AXIS2_PLACEMENT_3D ( 'NONE', #3888, #7772, #2823 ) ;
#24831=LINE ( 'NONE', #19514, #60686 ) ;
#24833=AXIS2_PLACEMENT_3D ( 'NONE', #48585, #16407, #862 ) ;
#24836=LINE ( 'NONE', #41793, #36131 ) ;
#24852=CARTESIAN_POINT ( 'NONE',  ( 11.50000000000000000, -11.50000000000100009, 15.00000000000084910 ) ) ;
#24854=CARTESIAN_POINT ( 'NONE',  ( 15.50000000000000000, -0.1999999999999999556, 21.05000000000000426 ) ) ;
#24858=DIRECTION ( 'NONE',  ( 0.000000000000000000, 0.7057491738665938596, 0.7084617869628679898 ) ) ;
#24861=ORIENTED_EDGE ( 'NONE', *, *, #25843, .F. ) ;
#24869=VERTEX_POINT ( 'NONE', #69034 ) ;
#24876=LINE ( 'NONE', #41132, #31099 ) ;
#24878=VECTOR ( 'NONE', #5291, 1000.000000000000000 ) ;
#24879=VERTEX_POINT ( 'NONE', #20591 ) ;
#24880=PLANE ( 'NONE',  #24881 ) ;
#24881=AXIS2_PLACEMENT_3D ( 'NONE', #19566, #41135, #2606 ) ;
#24889=ORIENTED_EDGE ( 'NONE', *, *, #68744, .F. ) ;
#24895=DIRECTION ( 'NONE',  ( -1.000000000000000000, 0.000000000000000000, 0.000000000000000000 ) ) ;
#24905=DIRECTION ( 'NONE',  ( 0.000000000000000000, 0.000000000000000000, -1.000000000000000000 ) ) ;
#24906=EDGE_CURVE ( 'NONE', #55585, #57937, #20222, .T. ) ;
#24919=VECTOR ( 'NONE', #52405, 1000.000000000000000 ) ;
#24923=CARTESIAN_POINT ( 'NONE',  ( 30.00000000000000000, -12.00000000000000000, 10.69999999999999929 ) ) ;
#24924=DIRECTION ( 'NONE',  ( 0.000000000000000000, 0.000000000000000000, -1.000000000000000000 ) ) ;
#24925=CYLINDRICAL_SURFACE ( 'NONE', #41313, 0.5000000000001374456 ) ;
#24934=CARTESIAN_POINT ( 'NONE',  ( -24.00000000000000000, -15.50000000000000000, -14.50000000000000000 ) ) ;
#24951=CIRCLE ( 'NONE', #47520, 0.2999999999998732569 ) ;
#24952=ORIENTED_EDGE ( 'NONE', *, *, #17318, .F. ) ;
#24954=CARTESIAN_POINT ( 'NONE',  ( 30.00000000000000000, -5.599999999999999645, -9.000000000000001776 ) ) ;
#24956=ORIENTED_EDGE ( 'NONE', *, *, #13202, .T. ) ;
#24965=AXIS2_PLACEMENT_3D ( 'NONE', #16563, #1659, #28198 ) ;
#24970=CIRCLE ( 'NONE', #26096, 0.3499999999998875677 ) ;
#24979=VECTOR ( 'NONE', #13046, 1000.000000000000000 ) ;
#24986=FACE_OUTER_BOUND ( 'NONE', #37947, .T. ) ;
#24988=CARTESIAN_POINT ( 'NONE',  ( 11.75000000000000000, -5.000000000000000000, -23.89194109070750116 ) ) ;
#24989=CARTESIAN_POINT ( 'NONE',  ( 15.50000000000000000, -1.037157890325000054, 22.50000000000000000 ) ) ;
#24993=DIRECTION ( 'NONE',  ( 1.000000000000000000, -0.000000000000000000, -0.000000000000000000 ) ) ;
#24997=VECTOR ( 'NONE', #31346, 1000.000000000000000 ) ;
#25008=DIRECTION ( 'NONE',  ( 0.000000000000000000, 0.000000000000000000, 1.000000000000000000 ) ) ;
#25010=ADVANCED_FACE ( 'NONE', ( #28322 ), #49893, .T. ) ;
#25014=DIRECTION ( 'NONE',  ( -1.000000000000000000, 0.000000000000000000, 0.000000000000000000 ) ) ;
#25020=EDGE_LOOP ( 'NONE', ( #58086, #36545, #21310, #41644 ) ) ;
#25021=DIRECTION ( 'NONE',  ( -1.000000000000000000, 0.000000000000000000, 0.000000000000000000 ) ) ;
#25025=PLANE ( 'NONE',  #50647 ) ;
#25027=ORIENTED_EDGE ( 'NONE', *, *, #47941, .T. ) ;
#25035=ORIENTED_EDGE ( 'NONE', *, *, #14788, .F. ) ;
#25038=LINE ( 'NONE', #31746, #38397 ) ;
#25039=CARTESIAN_POINT ( 'NONE',  ( -11.00000000000000000, -5.200000000000001066, 9.400000000000000355 ) ) ;
#25052=DIRECTION ( 'NONE',  ( 0.000000000000000000, 1.000000000000000000, 0.000000000000000000 ) ) ;
#25053=EDGE_LOOP ( 'NONE', ( #35489, #11567, #26586, #46231, #5805, #65088, #4478, #42700, #4290, #68693, #32911 ) ) ;
#25054=CARTESIAN_POINT ( 'NONE',  ( -15.50000000000000000, -1.037157890325000054, 19.00000000000000000 ) ) ;
#25060=EDGE_LOOP ( 'NONE', ( #68497, #56759, #41100, #42916 ) ) ;
#25061=ADVANCED_FACE ( 'NONE', ( #3556 ), #45269, .F. ) ;
#25062=DIRECTION ( 'NONE',  ( 0.000000000000000000, 0.000000000000000000, -1.000000000000000000 ) ) ;
#25063=CARTESIAN_POINT ( 'NONE',  ( 14.25000000000000000, -2.500000000000000000, 21.77831216351300014 ) ) ;
#25066=EDGE_LOOP ( 'NONE', ( #18308, #14427, #66262, #26785 ) ) ;
#25067=ADVANCED_FACE ( 'NONE', ( #51647 ), #39620, .F. ) ;
#25071=ORIENTED_EDGE ( 'NONE', *, *, #49866, .T. ) ;
#25075=LINE ( 'NONE', #68205, #43054 ) ;
#25077=EDGE_CURVE ( 'NONE', #10205, #22677, #40604, .T. ) ;
#25088=CARTESIAN_POINT ( 'NONE',  ( -15.50000000000000000, -5.000000000000000000, -22.50000000000000000 ) ) ;
#25099=LINE ( 'NONE', #9899, #10634 ) ;
#25104=ORIENTED_EDGE ( 'NONE', *, *, #32697, .F. ) ;
#25107=CARTESIAN_POINT ( 'NONE',  ( -25.50000000000000355, -15.50000000000000000, -20.49999999999999645 ) ) ;
#25108=AXIS2_PLACEMENT_3D ( 'NONE', #59273, #64582, #32414 ) ;
#25122=DIRECTION ( 'NONE',  ( 0.000000000000000000, 0.000000000000000000, 1.000000000000000000 ) ) ;
#25125=PLANE ( 'NONE',  #18711 ) ;
#25129=DIRECTION ( 'NONE',  ( 0.000000000000000000, 0.000000000000000000, 1.000000000000000000 ) ) ;
#25136=AXIS2_PLACEMENT_3D ( 'NONE', #38344, #59899, #10425 ) ;
#25143=CARTESIAN_POINT ( 'NONE',  ( -24.00000000000000000, -15.50000000000000000, 14.50000000000000000 ) ) ;
#25144=ORIENTED_EDGE ( 'NONE', *, *, #51177, .F. ) ;
#25146=PLANE ( 'NONE',  #40935 ) ;
#25171=DIRECTION ( 'NONE',  ( 1.000000000000000000, -0.000000000000000000, -0.000000000000000000 ) ) ;
#25179=CARTESIAN_POINT ( 'NONE',  ( 11.50000000000000000, -11.50000000000000000, -19.00000000000000000 ) ) ;
#25182=LINE ( 'NONE', #25539, #52651 ) ;
#25189=CIRCLE ( 'NONE', #6014, 4.500000000000191847 ) ;
#25198=ORIENTED_EDGE ( 'NONE', *, *, #13830, .F. ) ;
#25199=DIRECTION ( 'NONE',  ( 0.000000000000000000, 1.000000000000000000, 0.000000000000000000 ) ) ;
#25201=ORIENTED_EDGE ( 'NONE', *, *, #28502, .F. ) ;
#25219=CIRCLE ( 'NONE', #2592, 0.3499999999999285905 ) ;
#25232=CARTESIAN_POINT ( 'NONE',  ( -11.75000000000000000, -5.000000000000000000, -11.75000000000000000 ) ) ;
#25239=AXIS2_PLACEMENT_3D ( 'NONE', #6248, #69907, #16521 ) ;
#25241=DIRECTION ( 'NONE',  ( 0.000000000000000000, -0.1249999999999996531, -0.9921567416492215186 ) ) ;
#25256=FACE_OUTER_BOUND ( 'NONE', #11075, .T. ) ;
#25264=DIRECTION ( 'NONE',  ( 0.000000000000000000, 0.000000000000000000, -1.000000000000000000 ) ) ;
#25265=PLANE ( 'NONE',  #40109 ) ;
#25267=ORIENTED_EDGE ( 'NONE', *, *, #42725, .T. ) ;
#25268=DIRECTION ( 'NONE',  ( 0.000000000000000000, 0.000000000000000000, 1.000000000000000000 ) ) ;
#25270=DIRECTION ( 'NONE',  ( 1.000000000000000000, 0.000000000000000000, 0.000000000000000000 ) ) ;
#25274=DIRECTION ( 'NONE',  ( -1.000000000000000000, 0.000000000000000000, 0.000000000000000000 ) ) ;
#25275=CYLINDRICAL_SURFACE ( 'NONE', #2348, 4.000000000000000000 ) ;
#25282=CIRCLE ( 'NONE', #464, 2.000000000000001776 ) ;
#25287=EDGE_LOOP ( 'NONE', ( #61080, #65151, #16585, #60482 ) ) ;
#25295=ORIENTED_EDGE ( 'NONE', *, *, #63492, .F. ) ;
#25297=EDGE_CURVE ( 'NONE', #53470, #30033, #47732, .T. ) ;
#25298=VECTOR ( 'NONE', #68909, 1000.000000000000000 ) ;
#25304=CARTESIAN_POINT ( 'NONE',  ( 14.25000000000000000, -0.2038245569916330158, 23.22168783648699986 ) ) ;
#25309=DIRECTION ( 'NONE',  ( -1.000000000000000000, 0.000000000000000000, 0.000000000000000000 ) ) ;
#25314=EDGE_CURVE ( 'NONE', #12401, #38480, #63509, .T. ) ;
#25316=UNCERTAINTY_MEASURE_WITH_UNIT (LENGTH_MEASURE( 1.000000000000000082E-05 ), #43659, 'distance_accuracy_value', 'NONE');
#25317=CARTESIAN_POINT ( 'NONE',  ( 11.50000000000000000, -12.00000000000000000, -11.03137303340310282 ) ) ;
#25321=ORIENTED_EDGE ( 'NONE', *, *, #58933, .T. ) ;
#25340=EDGE_CURVE ( 'NONE', #8160, #9204, #43465, .T. ) ;
#25341=DIRECTION ( 'NONE',  ( 0.000000000000000000, -1.000000000000000000, 0.000000000000000000 ) ) ;
#25346=VERTEX_POINT ( 'NONE', #43117 ) ;
#25354=CYLINDRICAL_SURFACE ( 'NONE', #51575, 1.621000000000000885 ) ;
#25364=FACE_OUTER_BOUND ( 'NONE', #56621, .T. ) ;
#25366=ORIENTED_EDGE ( 'NONE', *, *, #9446, .F. ) ;
#25370=AXIS2_PLACEMENT_3D ( 'NONE', #19448, #39954, #7783 ) ;
#25379=ORIENTED_EDGE ( 'NONE', *, *, #45066, .F. ) ;
#25390=CIRCLE ( 'NONE', #49112, 4.000000000000000888 ) ;
#25394=ORIENTED_EDGE ( 'NONE', *, *, #64453, .T. ) ;
#25397=EDGE_CURVE ( 'NONE', #18780, #28902, #47382, .T. ) ;
#25401=CARTESIAN_POINT ( 'NONE',  ( -11.50000000000000000, -11.50000000000000000, 11.00000000000000000 ) ) ;
#25403=DIRECTION ( 'NONE',  ( -1.000000000000000000, 0.000000000000000000, 0.000000000000000000 ) ) ;
#25405=EDGE_CURVE ( 'NONE', #62633, #38291, #16951, .T. ) ;
#25414=ORIENTED_EDGE ( 'NONE', *, *, #31878, .F. ) ;
#25415=CIRCLE ( 'NONE', #64943, 0.3500000000009988455 ) ;
#25418=DIRECTION ( 'NONE',  ( 0.000000000000000000, 0.000000000000000000, 1.000000000000000000 ) ) ;
#25431=FACE_OUTER_BOUND ( 'NONE', #32351, .T. ) ;
#25436=AXIS2_PLACEMENT_3D ( 'NONE', #44340, #23830, #45038 ) ;
#25438=CARTESIAN_POINT ( 'NONE',  ( 30.00000000000000000, -14.04000000000000092, -14.80000000000000071 ) ) ;
#25467=LINE ( 'NONE', #47031, #28445 ) ;
#25470=VERTEX_POINT ( 'NONE', #22936 ) ;
#25473=CARTESIAN_POINT ( 'NONE',  ( -15.70366306705059323, -0.2717122460101009662, -21.17420925361163953 ) ) ;
#25474=VECTOR ( 'NONE', #23573, 1000.000000000000000 ) ;
#25483=EDGE_LOOP ( 'NONE', ( #30363, #22630, #67647, #39992 ) ) ;
#25507=VECTOR ( 'NONE', #35554, 1000.000000000000000 ) ;
#25513=DIRECTION ( 'NONE',  ( 0.000000000000000000, 0.000000000000000000, 1.000000000000000000 ) ) ;
#25521=CARTESIAN_POINT ( 'NONE',  ( 30.00000000000000000, -4.000000000000000000, 26.25000000000000000 ) ) ;
#25524=EDGE_CURVE ( 'NONE', #65032, #60221, #56403, .T. ) ;
#25525=VERTEX_POINT ( 'NONE', #35263 ) ;
#25534=AXIS2_PLACEMENT_3D ( 'NONE', #16850, #22839, #26773 ) ;
#25535=VERTEX_POINT ( 'NONE', #24331 ) ;
#25539=CARTESIAN_POINT ( 'NONE',  ( 29.50000000000000355, -12.00000000000000000, -10.69999999999999929 ) ) ;
#25546=DIRECTION ( 'NONE',  ( 0.000000000000000000, -1.000000000000000000, 0.000000000000000000 ) ) ;
#25549=CARTESIAN_POINT ( 'NONE',  ( -29.50000000000000355, -11.50000000000000000, 19.00000000000000000 ) ) ;
#25552=CIRCLE ( 'NONE', #57022, 0.3500000000002722600 ) ;
#25554=CARTESIAN_POINT ( 'NONE',  ( 30.00000000000000000, -8.959999999999999076, -12.95475478405700009 ) ) ;
#25557=DIRECTION ( 'NONE',  ( 0.000000000000000000, 0.000000000000000000, -1.000000000000000000 ) ) ;
#25566=LINE ( 'NONE', #57374, #21920 ) ;
#25570=CARTESIAN_POINT ( 'NONE',  ( -17.00000000000000000, -17.00000000000000000, 15.70499999999969809 ) ) ;
#25578=CARTESIAN_POINT ( 'NONE',  ( 30.00000000000000000, -5.599999999999999645, 27.00000000000000000 ) ) ;
#25583=ORIENTED_EDGE ( 'NONE', *, *, #40087, .F. ) ;
#25596=CARTESIAN_POINT ( 'NONE',  ( -28.00000000000000000, -17.35230188589299871, -15.35019951917099945 ) ) ;
#25599=VECTOR ( 'NONE', #60540, 1000.000000000000114 ) ;
#25616=EDGE_CURVE ( 'NONE', #55345, #15054, #61816, .T. ) ;
#25620=VERTEX_POINT ( 'NONE', #14431 ) ;
#25630=FACE_OUTER_BOUND ( 'NONE', #6244, .T. ) ;
#25631=CARTESIAN_POINT ( 'NONE',  ( 25.50000000000000355, 0.000000000000000000, 24.75000000000000000 ) ) ;
#25635=CARTESIAN_POINT ( 'NONE',  ( -14.25000000000000178, -0.2714405302574902090, 22.01253933645463690 ) ) ;
#25638=LINE ( 'NONE', #3012, #56959 ) ;
#25640=DIRECTION ( 'NONE',  ( 0.000000000000000000, 0.000000000000000000, -1.000000000000000000 ) ) ;
#25667=ADVANCED_FACE ( 'NONE', ( #8769 ), #58261, .F. ) ;
#25673=EDGE_CURVE ( 'NONE', #18841, #6609, #25038, .T. ) ;
#25675=ORIENTED_EDGE ( 'NONE', *, *, #43985, .F. ) ;
#25677=FACE_OUTER_BOUND ( 'NONE', #60321, .T. ) ;
#25689=ORIENTED_EDGE ( 'NONE', *, *, #14252, .F. ) ;
#25691=AXIS2_PLACEMENT_3D ( 'NONE', #56873, #25062, #57234 ) ;
#25694=ORIENTED_EDGE ( 'NONE', *, *, #43697, .T. ) ;
#25708=EDGE_CURVE ( 'NONE', #55302, #57112, #3470, .T. ) ;
#25720=ORIENTED_EDGE ( 'NONE', *, *, #21484, .T. ) ;
#25723=FACE_OUTER_BOUND ( 'NONE', #7165, .T. ) ;
#25726=CARTESIAN_POINT ( 'NONE',  ( -29.25000000000000000, -5.000000000000000000, -26.25000000000000000 ) ) ;
#25730=FACE_OUTER_BOUND ( 'NONE', #26992, .T. ) ;
#25731=DIRECTION ( 'NONE',  ( 0.000000000000000000, 1.000000000000000000, 0.000000000000000000 ) ) ;
#25733=ORIENTED_EDGE ( 'NONE', *, *, #6199, .F. ) ;
#25740=CARTESIAN_POINT ( 'NONE',  ( 11.75000000000000000, -5.200000000000001066, -26.25000000000000000 ) ) ;
#25746=DIRECTION ( 'NONE',  ( -1.000000000000000000, 0.000000000000000000, 0.000000000000000000 ) ) ;
#25766=PLANE ( 'NONE',  #54812 ) ;
#25768=CARTESIAN_POINT ( 'NONE',  ( 16.75000000000000000, -0.2038245569916320166, -23.22168783648699986 ) ) ;
#25773=ORIENTED_EDGE ( 'NONE', *, *, #7251, .F. ) ;
#25774=ORIENTED_EDGE ( 'NONE', *, *, #29151, .F. ) ;
#25777=DIRECTION ( 'NONE',  ( 0.000000000000000000, -1.000000000000000000, 0.000000000000000000 ) ) ;
#25778=LINE ( 'NONE', #58291, #50465 ) ;
#25783=ORIENTED_EDGE ( 'NONE', *, *, #57075, .F. ) ;
#25785=ORIENTED_EDGE ( 'NONE', *, *, #10964, .F. ) ;
#25791=DIRECTION ( 'NONE',  ( 0.000000000000000000, 1.000000000000000000, 0.000000000000000000 ) ) ;
#25792=ORIENTED_EDGE ( 'NONE', *, *, #34732, .F. ) ;
#25798=ORIENTED_EDGE ( 'NONE', *, *, #45142, .T. ) ;
#25805=DIRECTION ( 'NONE',  ( 0.000000000000000000, -1.000000000000000000, 0.000000000000000000 ) ) ;
#25807=ORIENTED_EDGE ( 'NONE', *, *, #62749, .F. ) ;
#25810=CARTESIAN_POINT ( 'NONE',  ( 30.00000000000000000, -14.33999999999999986, 14.50000000000000000 ) ) ;
#25843=EDGE_CURVE ( 'NONE', #55741, #41566, #27472, .T. ) ;
#25854=ADVANCED_FACE ( 'NONE', ( #604 ), #48694, .F. ) ;
#25856=ORIENTED_EDGE ( 'NONE', *, *, #53090, .T. ) ;
#25858=LINE ( 'NONE', #14894, #45176 ) ;
#25885=ORIENTED_EDGE ( 'NONE', *, *, #17714, .F. ) ;
#25888=VERTEX_POINT ( 'NONE', #1623 ) ;
#25897=ORIENTED_EDGE ( 'NONE', *, *, #18138, .T. ) ;
#25902=DIRECTION ( 'NONE',  ( 0.000000000000000000, -0.9921567416492215186, -0.1249999999999996531 ) ) ;
#25903=DIRECTION ( 'NONE',  ( 0.4999999999989417354, 0.000000000000000000, 0.8660254037850495523 ) ) ;
#25913=DIRECTION ( 'NONE',  ( 0.000000000000000000, 0.000000000000000000, -1.000000000000000000 ) ) ;
#25917=CIRCLE ( 'NONE', #23656, 4.000000000000000888 ) ;
#25919=LINE ( 'NONE', #41809, #68193 ) ;
#25923=DIRECTION ( 'NONE',  ( 0.000000000000000000, 0.000000000000000000, 1.000000000000000000 ) ) ;
#25930=DIRECTION ( 'NONE',  ( 0.000000000000000000, 0.000000000000000000, 1.000000000000000000 ) ) ;
#25942=EDGE_CURVE ( 'NONE', #903, #29890, #3042, .T. ) ;
#25945=CARTESIAN_POINT ( 'NONE',  ( -13.00000000000000178, -15.50000000000000000, -2.000000000000000000 ) ) ;
#25948=AXIS2_PLACEMENT_3D ( 'NONE', #48679, #28147, #5548 ) ;
#25950=AXIS2_PLACEMENT_3D ( 'NONE', #46241, #19028, #23281 ) ;
#25967=DIRECTION ( 'NONE',  ( -0.4999999999999832356, 0.000000000000000000, 0.8660254037844483666 ) ) ;
#25971=VECTOR ( 'NONE', #18673, 1000.000000000000000 ) ;
#25973=ADVANCED_FACE ( 'NONE', ( #50760 ), #17894, .F. ) ;
#25976=CARTESIAN_POINT ( 'NONE',  ( -17.00000000000000000, -16.28999999999710369, -14.50000000000000000 ) ) ;
#25980=LINE ( 'NONE', #47537, #29302 ) ;
#25982=CARTESIAN_POINT ( 'NONE',  ( 13.00000000000000178, -17.35230188589299871, 15.35019951917099945 ) ) ;
#25984=CARTESIAN_POINT ( 'NONE',  ( 25.49999999999869971, -15.50000000000000000, 22.50000000000000000 ) ) ;
#25990=DIRECTION ( 'NONE',  ( -1.000000000000000000, 0.000000000000000000, 0.000000000000000000 ) ) ;
#25994=VECTOR ( 'NONE', #30590, 1000.000000000000000 ) ;
#25999=CARTESIAN_POINT ( 'NONE',  ( -28.00000000000000000, -15.50000000000000000, -14.50000000000000000 ) ) ;
#26005=LINE ( 'NONE', #26341, #56664 ) ;
#26007=ORIENTED_EDGE ( 'NONE', *, *, #34229, .T. ) ;
#26009=VERTEX_POINT ( 'NONE', #20344 ) ;
#26011=DIRECTION ( 'NONE',  ( 0.000000000000000000, 0.000000000000000000, 1.000000000000000000 ) ) ;
#26015=EDGE_CURVE ( 'NONE', #52878, #37597, #49545, .T. ) ;
#26019=CARTESIAN_POINT ( 'NONE',  ( -11.00000000000000000, -9.199999999999999289, 12.69999999999986073 ) ) ;
#26038=EDGE_CURVE ( 'NONE', #22255, #58992, #37151, .T. ) ;
#26048=CARTESIAN_POINT ( 'NONE',  ( -25.50000000000000355, 0.000000000000000000, 24.75000000000000000 ) ) ;
#26055=DIRECTION ( 'NONE',  ( 0.000000000000000000, 0.000000000000000000, -1.000000000000000000 ) ) ;
#26061=ORIENTED_EDGE ( 'NONE', *, *, #46348, .F. ) ;
#26063=DIRECTION ( 'NONE',  ( 0.000000000000000000, -0.6857142857147903170, 0.7278708115913530285 ) ) ;
#26066=CIRCLE ( 'NONE', #54280, 0.5000000000079367624 ) ;
#26067=CARTESIAN_POINT ( 'NONE',  ( -29.50000000000000355, -11.50000000000000000, -15.00000000000000000 ) ) ;
#26068=ORIENTED_EDGE ( 'NONE', *, *, #21117, .T. ) ;
#26076=DIRECTION ( 'NONE',  ( 0.000000000000000000, 0.000000000000000000, 1.000000000000000000 ) ) ;
#26080=DIRECTION ( 'NONE',  ( 0.000000000000000000, 1.000000000000000000, 0.000000000000000000 ) ) ;
#26081=DIRECTION ( 'NONE',  ( -1.000000000000000000, 0.000000000000000000, 0.000000000000000000 ) ) ;
#26083=LINE ( 'NONE', #41985, #10799 ) ;
#26092=AXIS2_PLACEMENT_3D ( 'NONE', #10290, #4984, #25513 ) ;
#26096=AXIS2_PLACEMENT_3D ( 'NONE', #59450, #11014, #32588 ) ;
#26101=VERTEX_POINT ( 'NONE', #25304 ) ;
#26106=VECTOR ( 'NONE', #17539, 1000.000000000000114 ) ;
#26117=AXIS2_PLACEMENT_3D ( 'NONE', #2997, #55766, #24905 ) ;
#26118=DIRECTION ( 'NONE',  ( 0.000000000000000000, 0.000000000000000000, 1.000000000000000000 ) ) ;
#26120=CARTESIAN_POINT ( 'NONE',  ( 11.75000000000000000, -5.000000000000000000, 21.10805890929250239 ) ) ;
#26122=CARTESIAN_POINT ( 'NONE',  ( 24.00000000000000000, -16.28999999999710369, -14.50000000000000000 ) ) ;
#26136=CARTESIAN_POINT ( 'NONE',  ( -25.50000000000000355, -5.578999999999999737, 22.50000000000000000 ) ) ;
#26138=CARTESIAN_POINT ( 'NONE',  ( 11.50000000000000000, -11.50000000000100009, 15.00000000000084910 ) ) ;
#26141=VECTOR ( 'NONE', #7485, 1000.000000000000000 ) ;
#26155=VECTOR ( 'NONE', #43541, 1000.000000000000000 ) ;
#26159=CYLINDRICAL_SURFACE ( 'NONE', #50753, 0.3499999999998886224 ) ;
#26163=EDGE_LOOP ( 'NONE', ( #57131, #46174, #52510, #69143, #47990 ) ) ;
#26165=ORIENTED_EDGE ( 'NONE', *, *, #29151, .T. ) ;
#26166=ORIENTED_EDGE ( 'NONE', *, *, #58486, .F. ) ;
#26167=LINE ( 'NONE', #41359, #50606 ) ;
#26174=ORIENTED_EDGE ( 'NONE', *, *, #21988, .T. ) ;
#26178=DIRECTION ( 'NONE',  ( 0.000000000000000000, 0.000000000000000000, 1.000000000000000000 ) ) ;
#26179=VECTOR ( 'NONE', #65919, 1000.000000000000000 ) ;
#26188=ORIENTED_EDGE ( 'NONE', *, *, #51413, .T. ) ;
#26195=DIRECTION ( 'NONE',  ( 1.000000000000000000, -0.000000000000000000, -0.000000000000000000 ) ) ;
#26198=VERTEX_POINT ( 'NONE', #183 ) ;
#26211=DIRECTION ( 'NONE',  ( 0.000000000000000000, 0.000000000000000000, 1.000000000000000000 ) ) ;
#26218=EDGE_CURVE ( 'NONE', #4367, #57233, #897, .T. ) ;
#26226=ADVANCED_FACE ( 'NONE', ( #64538 ), #37661, .F. ) ;
#26227=ORIENTED_EDGE ( 'NONE', *, *, #5823, .T. ) ;
#26233=CARTESIAN_POINT ( 'NONE',  ( -11.00000000000000000, -16.28999999999999915, -14.50000000000000000 ) ) ;
#26236=ADVANCED_FACE ( 'NONE', ( #22092 ), #38356, .F. ) ;
#26237=CIRCLE ( 'NONE', #69130, 4.000000000000000888 ) ;
#26241=DIRECTION ( 'NONE',  ( -1.000000000000000000, 0.000000000000000000, 0.000000000000000000 ) ) ;
#26248=DIRECTION ( 'NONE',  ( 1.000000000000000000, -0.000000000000000000, -0.000000000000000000 ) ) ;
#26249=DIRECTION ( 'NONE',  ( -0.000000000000000000, 1.000000000000000000, -0.000000000000000000 ) ) ;
#26252=FACE_OUTER_BOUND ( 'NONE', #1316, .T. ) ;
#26259=DIRECTION ( 'NONE',  ( 0.000000000000000000, 1.000000000000000000, 0.000000000000000000 ) ) ;
#26261=CARTESIAN_POINT ( 'NONE',  ( -11.50000000000000000, -11.70000000000000284, 11.00000000000000000 ) ) ;
#26266=ORIENTED_EDGE ( 'NONE', *, *, #21141, .T. ) ;
#26269=CYLINDRICAL_SURFACE ( 'NONE', #46772, 0.5000000000001357803 ) ;
#26271=ORIENTED_EDGE ( 'NONE', *, *, #45537, .F. ) ;
#26276=LINE ( 'NONE', #36530, #67213 ) ;
#26280=CARTESIAN_POINT ( 'NONE',  ( -28.00000000000000000, -15.50000000000000000, 20.05051025721700242 ) ) ;
#26286=CARTESIAN_POINT ( 'NONE',  ( 16.75000000000000000, -2.500000000000000000, -21.77831216351300014 ) ) ;
#26302=DIRECTION ( 'NONE',  ( -1.000000000000000000, 0.000000000000000000, 0.000000000000000000 ) ) ;
#26303=AXIS2_PLACEMENT_3D ( 'NONE', #19282, #3723, #30250 ) ;
#26305=CARTESIAN_POINT ( 'NONE',  ( -11.00000000000000000, -11.50000000000000000, -19.00000000000000000 ) ) ;
#26306=CIRCLE ( 'NONE', #47748, 4.000000000000000888 ) ;
#26312=CONICAL_SURFACE ( 'NONE', #28512, 1.621000000000000885, 0.7853981633974518317 ) ;
#26323=DIRECTION ( 'NONE',  ( 0.000000000000000000, -1.000000000000000000, 0.000000000000000000 ) ) ;
#26326=DIRECTION ( 'NONE',  ( 0.000000000000000000, 0.000000000000000000, 1.000000000000000000 ) ) ;
#26328=DIRECTION ( 'NONE',  ( -1.000000000000000000, 0.000000000000000000, 0.000000000000000000 ) ) ;
#26332=ORIENTED_EDGE ( 'NONE', *, *, #50487, .F. ) ;
#26336=CARTESIAN_POINT ( 'NONE',  ( 24.00000000000000000, -16.64230188589299786, 14.64519951917100116 ) ) ;
#26337=DIRECTION ( 'NONE',  ( -1.000000000000000000, 0.000000000000000000, 0.000000000000000000 ) ) ;
#26339=CIRCLE ( 'NONE', #68113, 0.2999999999998732569 ) ;
#26341=CARTESIAN_POINT ( 'NONE',  ( 29.25000000000000000, -5.200000000000001066, -26.25000000000000000 ) ) ;
#26354=AXIS2_PLACEMENT_3D ( 'NONE', #39936, #13075, #12719 ) ;
#26355=DIRECTION ( 'NONE',  ( 0.000000000000000000, 0.000000000000000000, 1.000000000000000000 ) ) ;
#26363=DIRECTION ( 'NONE',  ( -1.000000000000000000, 0.000000000000000000, 0.000000000000000000 ) ) ;
#26372=EDGE_CURVE ( 'NONE', #65633, #40754, #6847, .T. ) ;
#26373=ORIENTED_EDGE ( 'NONE', *, *, #36551, .T. ) ;
#26379=SHAPE_REPRESENTATION ( 'SAWC-0630-60S_wagen', ( #45918 ), #34756 ) ;
#26381=VERTEX_POINT ( 'NONE', #12158 ) ;
#26398=CIRCLE ( 'NONE', #35408, 0.3499999999999597877 ) ;
#26403=CARTESIAN_POINT ( 'NONE',  ( -22.14589803375000088, -17.50000000000000000, 21.50000000000000000 ) ) ;
#26404=CARTESIAN_POINT ( 'NONE',  ( -15.50000000000000000, -0.2038245569916614930, 23.94337567297399971 ) ) ;
#26414=VECTOR ( 'NONE', #68273, 1000.000000000000000 ) ;
#26450=PLANE ( 'NONE',  #8507 ) ;
#26453=LINE ( 'NONE', #43053, #23209 ) ;
#26455=CARTESIAN_POINT ( 'NONE',  ( -17.00000000000000000, -15.50000000000000000, -14.50000000000000000 ) ) ;
#26460=AXIS2_PLACEMENT_3D ( 'NONE', #60889, #7500, #50288 ) ;
#26468=CONICAL_SURFACE ( 'NONE', #65965, 1732.050807568785558, 1.047197551196574761 ) ;
#26470=AXIS2_PLACEMENT_3D ( 'NONE', #39994, #18430, #61566 ) ;
#26491=CARTESIAN_POINT ( 'NONE',  ( 23.48000000000000043, -15.50000000000000000, 26.00000000000000355 ) ) ;
#26503=ORIENTED_EDGE ( 'NONE', *, *, #25843, .T. ) ;
#26513=VERTEX_POINT ( 'NONE', #42835 ) ;
#26514=ORIENTED_EDGE ( 'NONE', *, *, #36551, .F. ) ;
#26519=CARTESIAN_POINT ( 'NONE',  ( 15.08757311576526128, -0.3152598339554911200, -23.70526090034004341 ) ) ;
#26521=VECTOR ( 'NONE', #60370, 1000.000000000000000 ) ;
#26522=CARTESIAN_POINT ( 'NONE',  ( -11.00000000000000000, -16.64230188589299786, -14.64519951917100116 ) ) ;
#26546=DIRECTION ( 'NONE',  ( 0.000000000000000000, 0.000000000000000000, 1.000000000000000000 ) ) ;
#26549=AXIS2_PLACEMENT_3D ( 'NONE', #7409, #12354, #27957 ) ;
#26552=DIRECTION ( 'NONE',  ( 0.000000000000000000, 0.000000000000000000, 1.000000000000000000 ) ) ;
#26580=EDGE_CURVE ( 'NONE', #2518, #47170, #18960, .T. ) ;
#26582=CARTESIAN_POINT ( 'NONE',  ( -23.48000000000000043, -17.50000000000000000, 26.00000000000000355 ) ) ;
#26586=ORIENTED_EDGE ( 'NONE', *, *, #25077, .F. ) ;
#26590=VECTOR ( 'NONE', #9104, 1000.000000000000000 ) ;
#26606=CIRCLE ( 'NONE', #39008, 0.4000000000000609179 ) ;
#26609=CARTESIAN_POINT ( 'NONE',  ( -11.00000000000000000, -11.50000000000000000, 19.00000000000000000 ) ) ;
#26615=DIRECTION ( 'NONE',  ( 0.000000000000000000, 1.000000000000000000, 0.000000000000000000 ) ) ;
#26620=DIRECTION ( 'NONE',  ( 8.659560562354963673E-17, 0.7071067811865450192, -0.7071067811865500152 ) ) ;
#26628=ORIENTED_EDGE ( 'NONE', *, *, #52256, .F. ) ;
#26632=ORIENTED_EDGE ( 'NONE', *, *, #12602, .T. ) ;
#26635=EDGE_CURVE ( 'NONE', #21397, #46652, #20937, .T. ) ;
#26641=LINE ( 'NONE', #48212, #38550 ) ;
#26650=VECTOR ( 'NONE', #33097, 1000.000000000000000 ) ;
#26654=AXIS2_PLACEMENT_3D ( 'NONE', #46790, #62702, #14279 ) ;
#26660=DIRECTION ( 'NONE',  ( 0.000000000000000000, 0.000000000000000000, 1.000000000000000000 ) ) ;
#26666=VECTOR ( 'NONE', #64899, 1000.000000000000000 ) ;
#26684=FACE_BOUND ( 'NONE', #16706, .T. ) ;
#26699=CARTESIAN_POINT ( 'NONE',  ( 29.50000000000000355, -12.00000000000000000, -10.52786404500095863 ) ) ;
#26707=VERTEX_POINT ( 'NONE', #25317 ) ;
#26709=AXIS2_PLACEMENT_3D ( 'NONE', #46111, #40455, #62013 ) ;
#26712=ORIENTED_EDGE ( 'NONE', *, *, #23747, .F. ) ;
#26720=VERTEX_POINT ( 'NONE', #35924 ) ;
#26728=EDGE_CURVE ( 'NONE', #10205, #18896, #4801, .T. ) ;
#26731=ORIENTED_EDGE ( 'NONE', *, *, #55202, .T. ) ;
#26740=LINE ( 'NONE', #38057, #4324 ) ;
#26750=AXIS2_PLACEMENT_3D ( 'NONE', #58723, #22287, #43837 ) ;
#26757=AXIS2_PLACEMENT_3D ( 'NONE', #41914, #19636, #15048 ) ;
#26761=ADVANCED_FACE ( 'NONE', ( #36618 ), #69495, .F. ) ;
#26765=DIRECTION ( 'NONE',  ( 1.000000000000000000, -0.000000000000000000, -0.000000000000000000 ) ) ;
#26770=CIRCLE ( 'NONE', #66281, 0.5000000000079362072 ) ;
#26773=DIRECTION ( 'NONE',  ( 0.000000000000000000, -0.7084617869615144059, 0.7057491738679528837 ) ) ;
#26775=ORIENTED_EDGE ( 'NONE', *, *, #10328, .T. ) ;
#26780=ORIENTED_EDGE ( 'NONE', *, *, #25524, .T. ) ;
#26784=ORIENTED_EDGE ( 'NONE', *, *, #24666, .F. ) ;
#26785=ORIENTED_EDGE ( 'NONE', *, *, #21427, .F. ) ;
#26791=LINE ( 'NONE', #69215, #16673 ) ;
#26793=AXIS2_PLACEMENT_3D ( 'NONE', #4234, #15184, #65014 ) ;
#26799=ORIENTED_EDGE ( 'NONE', *, *, #45142, .F. ) ;
#26804=CIRCLE ( 'NONE', #68539, 0.5000000000079367624 ) ;
#26809=EDGE_CURVE ( 'NONE', #36688, #56607, #19646, .T. ) ;
#26810=VECTOR ( 'NONE', #30144, 1000.000000000000000 ) ;
#26821=LINE ( 'NONE', #36361, #1994 ) ;
#26823=ORIENTED_EDGE ( 'NONE', *, *, #22436, .F. ) ;
#26824=AXIS2_PLACEMENT_3D ( 'NONE', #5268, #49767, #16905 ) ;
#26834=CARTESIAN_POINT ( 'NONE',  ( 15.50000000000000000, -0.4000000000005274892, 22.50000000000000000 ) ) ;
#26836=ORIENTED_EDGE ( 'NONE', *, *, #48259, .T. ) ;
#26840=EDGE_CURVE ( 'NONE', #47971, #48505, #29960, .T. ) ;
#26859=CARTESIAN_POINT ( 'NONE',  ( -30.00000000000000000, 0.000000000000000000, 27.00000000000000000 ) ) ;
#26862=ORIENTED_EDGE ( 'NONE', *, *, #38573, .T. ) ;
#26869=VECTOR ( 'NONE', #43256, 1000.000000000000000 ) ;
#26875=VERTEX_POINT ( 'NONE', #49661 ) ;
#26885=CARTESIAN_POINT ( 'NONE',  ( 11.50000000000000000, -11.50000000000100009, 15.00000000000084910 ) ) ;
#26889=DIRECTION ( 'NONE',  ( 0.000000000000000000, 0.000000000000000000, 1.000000000000000000 ) ) ;
#26904=DIRECTION ( 'NONE',  ( 0.000000000000000000, -1.000000000000000000, 0.000000000000000000 ) ) ;
#26910=DIRECTION ( 'NONE',  ( 0.000000000000000000, -0.7278708115916149302, -0.6857142857145122061 ) ) ;
#26916=DIRECTION ( 'NONE',  ( 0.000000000000000000, 0.000000000000000000, -1.000000000000000000 ) ) ;
#26919=DIRECTION ( 'NONE',  ( 0.000000000000000000, 0.000000000000000000, -1.000000000000000000 ) ) ;
#26924=ORIENTED_EDGE ( 'NONE', *, *, #44387, .F. ) ;
#26931=EDGE_CURVE ( 'NONE', #5431, #46013, #16456, .T. ) ;
#26940=EDGE_CURVE ( 'NONE', #68528, #3061, #33407, .T. ) ;
#26951=ORIENTED_EDGE ( 'NONE', *, *, #58486, .T. ) ;
#26952=ORIENTED_EDGE ( 'NONE', *, *, #4596, .T. ) ;
#26956=VECTOR ( 'NONE', #50323, 1000.000000000000000 ) ;
#26959=CARTESIAN_POINT ( 'NONE',  ( 15.50000000000000000, 998.9628421096749662, 22.50000000000000000 ) ) ;
#26965=LINE ( 'NONE', #38272, #57823 ) ;
#26968=ORIENTED_EDGE ( 'NONE', *, *, #52734, .F. ) ;
#26981=DIRECTION ( 'NONE',  ( 0.000000000000000000, 0.000000000000000000, 1.000000000000000000 ) ) ;
#26983=CARTESIAN_POINT ( 'NONE',  ( 11.00000000000000000, -12.00000000000000000, -10.20500000000000007 ) ) ;
#26991=DIRECTION ( 'NONE',  ( 0.000000000000000000, 0.000000000000000000, 1.000000000000000000 ) ) ;
#26992=EDGE_LOOP ( 'NONE', ( #18224, #458 ) ) ;
#26995=LINE ( 'NONE', #48557, #6356 ) ;
#27001=DIRECTION ( 'NONE',  ( 0.000000000000000000, 0.000000000000000000, 1.000000000000000000 ) ) ;
#27006=DIRECTION ( 'NONE',  ( 0.000000000000000000, 1.000000000000000000, 0.000000000000000000 ) ) ;
#27012=DIRECTION ( 'NONE',  ( 1.000000000000000000, 0.000000000000000000, 0.000000000000000000 ) ) ;
#27013=EDGE_CURVE ( 'NONE', #64069, #17432, #53710, .T. ) ;
#27016=AXIS2_PLACEMENT_3D ( 'NONE', #40875, #34517, #29565 ) ;
#27024=CARTESIAN_POINT ( 'NONE',  ( 29.50000000000000355, -15.97213595500069871, 14.50000000000000000 ) ) ;
#27029=CARTESIAN_POINT ( 'NONE',  ( 29.50000000000000355, -11.70000000000000284, -11.00000000000000000 ) ) ;
#27035=FACE_OUTER_BOUND ( 'NONE', #56760, .T. ) ;
#27038=ORIENTED_EDGE ( 'NONE', *, *, #67099, .T. ) ;
#27059=CARTESIAN_POINT ( 'NONE',  ( -11.00000000000000000, -5.599999999999999645, 27.00000000000000000 ) ) ;
#27063=LINE ( 'NONE', #33409, #26666 ) ;
#27069=FACE_OUTER_BOUND ( 'NONE', #28028, .T. ) ;
#27070=EDGE_CURVE ( 'NONE', #41911, #2041, #33410, .T. ) ;
#27080=FACE_OUTER_BOUND ( 'NONE', #58106, .T. ) ;
#27082=CARTESIAN_POINT ( 'NONE',  ( 15.50000000000000000, -1.037157890325000054, 22.50000000000000000 ) ) ;
#27087=CYLINDRICAL_SURFACE ( 'NONE', #655, 0.3499999999998886224 ) ;
#27089=VECTOR ( 'NONE', #56819, 1000.000000000000000 ) ;
#27109=AXIS2_PLACEMENT_3D ( 'NONE', #49659, #23127, #18511 ) ;
#27111=ADVANCED_FACE ( 'NONE', ( #28430 ), #12511, .T. ) ;
#27112=AXIS2_PLACEMENT_3D ( 'NONE', #7518, #51348, #23082 ) ;
#27116=ORIENTED_EDGE ( 'NONE', *, *, #23874, .T. ) ;
#27122=FACE_OUTER_BOUND ( 'NONE', #3031, .T. ) ;
#27124=ORIENTED_EDGE ( 'NONE', *, *, #5944, .F. ) ;
#27127=CARTESIAN_POINT ( 'NONE',  ( -30.00000000000000000, -13.54524521594299991, 17.53999999999999915 ) ) ;
#27132=VERTEX_POINT ( 'NONE', #51759 ) ;
#27134=LINE ( 'NONE', #43383, #7505 ) ;
#27136=DIRECTION ( 'NONE',  ( 0.000000000000000000, -5.800915303574361727E-12, 1.000000000000000000 ) ) ;
#27137=ORIENTED_EDGE ( 'NONE', *, *, #12602, .F. ) ;
#27142=CARTESIAN_POINT ( 'NONE',  ( 14.25000000000000000, -2.500000000000000000, -21.77831216351300014 ) ) ;
#27156=CARTESIAN_POINT ( 'NONE',  ( 13.00000000000000178, -15.50000000000000000, -20.05051025721700242 ) ) ;
#27162=CARTESIAN_POINT ( 'NONE',  ( -15.50000000000000000, -0.2000000000000000111, -22.50000000000000000 ) ) ;
#27168=CARTESIAN_POINT ( 'NONE',  ( -15.50000000000000000, -1.037157890325000054, 26.50000000000000000 ) ) ;
#27171=CARTESIAN_POINT ( 'NONE',  ( 15.50000000000000000, 0.000000000000000000, 22.50000000000000000 ) ) ;
#27173=DIRECTION ( 'NONE',  ( 0.000000000000000000, 1.000000000000000000, 0.000000000000000000 ) ) ;
#27184=ORIENTED_EDGE ( 'NONE', *, *, #17109, .T. ) ;
#27186=AXIS2_PLACEMENT_3D ( 'NONE', #109, #21673, #64807 ) ;
#27190=ADVANCED_FACE ( 'NONE', ( #41137 ), #69063, .T. ) ;
#27191=CARTESIAN_POINT ( 'NONE',  ( -30.00000000000000000, -11.70000000000000284, -12.50000000000000000 ) ) ;
#27192=VERTEX_POINT ( 'NONE', #57403 ) ;
#27193=DIRECTION ( 'NONE',  ( 0.000000000000000000, -0.1249999999999996531, -0.9921567416492215186 ) ) ;
#27195=ORIENTED_EDGE ( 'NONE', *, *, #53145, .T. ) ;
#27204=AXIS2_PLACEMENT_3D ( 'NONE', #9591, #64391, #26552 ) ;
#27205=ORIENTED_EDGE ( 'NONE', *, *, #10823, .T. ) ;
#27206=ORIENTED_EDGE ( 'NONE', *, *, #21265, .F. ) ;
#27207=CARTESIAN_POINT ( 'NONE',  ( 13.00000000000000178, -17.50000000000000000, -20.05051025721700242 ) ) ;
#27215=VECTOR ( 'NONE', #2747, 1000.000000000000000 ) ;
#27219=VERTEX_POINT ( 'NONE', #25596 ) ;
#27221=ORIENTED_EDGE ( 'NONE', *, *, #63028, .T. ) ;
#27222=VECTOR ( 'NONE', #35089, 1000.000000000000000 ) ;
#27235=VERTEX_POINT ( 'NONE', #63418 ) ;
#27239=EDGE_CURVE ( 'NONE', #8233, #20681, #9336, .T. ) ;
#27248=DIRECTION ( 'NONE',  ( -1.000000000000000000, 0.000000000000000000, 0.000000000000000000 ) ) ;
#27251=AXIS2_PLACEMENT_3D ( 'NONE', #55589, #61215, #17763 ) ;
#27259=ORIENTED_EDGE ( 'NONE', *, *, #55265, .T. ) ;
#27261=EDGE_CURVE ( 'NONE', #54344, #68712, #53177, .T. ) ;
#27262=CARTESIAN_POINT ( 'NONE',  ( 11.00000000000000000, -17.50000000000000000, 60.00000000000000000 ) ) ;
#27264=DIRECTION ( 'NONE',  ( 1.000000000000000000, -0.000000000000000000, -0.000000000000000000 ) ) ;
#27265=CARTESIAN_POINT ( 'NONE',  ( 25.50000000000000355, -5.200000000000001066, -24.50000000000000000 ) ) ;
#27272=LINE ( 'NONE', #16298, #8970 ) ;
#27275=CARTESIAN_POINT ( 'NONE',  ( -22.14589803375000088, -15.50000000000000000, 21.50000000000000000 ) ) ;
#27279=DIRECTION ( 'NONE',  ( 1.000000000000000000, -0.000000000000000000, -0.000000000000000000 ) ) ;
#27291=ORIENTED_EDGE ( 'NONE', *, *, #49144, .T. ) ;
#27296=CARTESIAN_POINT ( 'NONE',  ( -30.00000000000000000, -9.199999999999999289, 12.69999999999986073 ) ) ;
#27301=AXIS2_PLACEMENT_3D ( 'NONE', #9599, #63342, #42113 ) ;
#27304=ORIENTED_EDGE ( 'NONE', *, *, #39736, .T. ) ;
#27306=CARTESIAN_POINT ( 'NONE',  ( 30.00000000000000000, -16.28999999999710369, -15.00000000000794920 ) ) ;
#27314=ORIENTED_EDGE ( 'NONE', *, *, #50777, .F. ) ;
#27320=EDGE_CURVE ( 'NONE', #69663, #32597, #11405, .T. ) ;
#27322=VERTEX_POINT ( 'NONE', #48903 ) ;
#27323=ORIENTED_EDGE ( 'NONE', *, *, #49866, .F. ) ;
#27329=EDGE_CURVE ( 'NONE', #40687, #27463, #22024, .T. ) ;
#27338=DIRECTION ( 'NONE',  ( 0.000000000000000000, 0.000000000000000000, -1.000000000000000000 ) ) ;
#27340=ADVANCED_FACE ( 'NONE', ( #121 ), #16367, .T. ) ;
#27349=CARTESIAN_POINT ( 'NONE',  ( 15.50000000000000000, -5.000000000000000000, -22.50000000000000000 ) ) ;
#27354=ORIENTED_EDGE ( 'NONE', *, *, #34068, .T. ) ;
#27367=DIRECTION ( 'NONE',  ( 0.000000000000000000, 0.000000000000000000, 1.000000000000000000 ) ) ;
#27371=CONICAL_SURFACE ( 'NONE', #13825, 1732.050807568785558, 1.047197551196574761 ) ;
#27372=DIRECTION ( 'NONE',  ( 0.000000000000000000, 1.000000000000000000, 0.000000000000000000 ) ) ;
#27380=EDGE_LOOP ( 'NONE', ( #55537, #36597, #17530, #33871 ) ) ;
#27391=ORIENTED_EDGE ( 'NONE', *, *, #19308, .F. ) ;
#27404=VERTEX_POINT ( 'NONE', #1148 ) ;
#27422=LINE ( 'NONE', #31073, #39351 ) ;
#27427=ORIENTED_EDGE ( 'NONE', *, *, #16809, .T. ) ;
#27430=CARTESIAN_POINT ( 'NONE',  ( 30.00000000000000000, -17.50000000000000000, -15.70500000000000007 ) ) ;
#27432=CYLINDRICAL_SURFACE ( 'NONE', #65868, 4.500000000000189182 ) ;
#27434=CARTESIAN_POINT ( 'NONE',  ( 30.00000000000000000, -16.64230188589299786, -14.64519951917100116 ) ) ;
#27437=DIRECTION ( 'NONE',  ( 0.000000000000000000, 1.000000000000000000, 0.000000000000000000 ) ) ;
#27438=VERTEX_POINT ( 'NONE', #2179 ) ;
#27441=CIRCLE ( 'NONE', #42081, 4.000000000000000888 ) ;
#27445=LINE ( 'NONE', #17171, #15446 ) ;
#27447=ORIENTED_EDGE ( 'NONE', *, *, #38108, .T. ) ;
#27455=VERTEX_POINT ( 'NONE', #1478 ) ;
#27456=AXIS2_PLACEMENT_3D ( 'NONE', #39622, #39961, #17036 ) ;
#27461=VECTOR ( 'NONE', #22337, 1000.000000000000000 ) ;
#27463=VERTEX_POINT ( 'NONE', #23046 ) ;
#27466=EDGE_LOOP ( 'NONE', ( #8815, #55228, #27354, #20353 ) ) ;
#27472=LINE ( 'NONE', #49043, #32736 ) ;
#27481=VERTEX_POINT ( 'NONE', #12419 ) ;
#27484=LINE ( 'NONE', #38118, #44274 ) ;
#27486=EDGE_CURVE ( 'NONE', #42614, #24441, #64455, .T. ) ;
#27491=EDGE_CURVE ( 'NONE', #26513, #22437, #33928, .T. ) ;
#27498=ADVANCED_FACE ( 'NONE', ( #47068 ), #35039, .T. ) ;
#27499=EDGE_CURVE ( 'NONE', #38679, #62810, #35386, .T. ) ;
#27501=ADVANCED_FACE ( 'NONE', ( #24447 ), #56957, .F. ) ;
#27508=VERTEX_POINT ( 'NONE', #41403 ) ;
#27512=VECTOR ( 'NONE', #26620, 1000.000000000000000 ) ;
#27513=PLANE ( 'NONE',  #26824 ) ;
#27525=DIRECTION ( 'NONE',  ( 0.000000000000000000, 0.000000000000000000, 1.000000000000000000 ) ) ;
#27532=DIRECTION ( 'NONE',  ( 0.000000000000000000, 0.000000000000000000, -1.000000000000000000 ) ) ;
#27538=DIRECTION ( 'NONE',  ( 0.000000000000000000, 0.000000000000000000, 1.000000000000000000 ) ) ;
#27541=VECTOR ( 'NONE', #66311, 1000.000000000000000 ) ;
#27543=EDGE_CURVE ( 'NONE', #51391, #22759, #25858, .T. ) ;
#27544=CARTESIAN_POINT ( 'NONE',  ( 11.00000000000000000, -9.487228132326899654, -12.50000000000000000 ) ) ;
#27554=AXIS2_PLACEMENT_3D ( 'NONE', #3880, #41345, #53030 ) ;
#27555=AXIS2_PLACEMENT_3D ( 'NONE', #39376, #34058, #55994 ) ;
#27567=ORIENTED_EDGE ( 'NONE', *, *, #1277, .T. ) ;
#27570=AXIS2_PLACEMENT_3D ( 'NONE', #35351, #3558, #9213 ) ;
#27571=CARTESIAN_POINT ( 'NONE',  ( 25.50000000000000355, -15.50000000000000000, 22.50000000000000000 ) ) ;
#27582=EDGE_CURVE ( 'NONE', #2319, #64180, #67931, .T. ) ;
#27584=VERTEX_POINT ( 'NONE', #9237 ) ;
#27586=DIRECTION ( 'NONE',  ( -0.000000000000000000, 1.000000000000000000, -0.000000000000000000 ) ) ;
#27593=CARTESIAN_POINT ( 'NONE',  ( 30.00000000000000000, -16.64230188589299786, -14.64519951917100116 ) ) ;
#27594=EDGE_CURVE ( 'NONE', #59384, #26720, #44087, .T. ) ;
#27596=PLANE ( 'NONE',  #42565 ) ;
#27620=DIRECTION ( 'NONE',  ( 1.000000000000000000, 0.000000000000000000, 0.000000000000000000 ) ) ;
#27622=ORIENTED_EDGE ( 'NONE', *, *, #61633, .F. ) ;
#27627=VECTOR ( 'NONE', #18767, 1000.000000000000000 ) ;
#27629=DIRECTION ( 'NONE',  ( 0.000000000000000000, 0.000000000000000000, -1.000000000000000000 ) ) ;
#27634=ORIENTED_EDGE ( 'NONE', *, *, #20152, .F. ) ;
#27636=CARTESIAN_POINT ( 'NONE',  ( 30.00000000000000000, -11.70000000000000284, -11.00000000000000000 ) ) ;
#27640=DIRECTION ( 'NONE',  ( 0.000000000000000000, 1.000000000000000000, 0.000000000000000000 ) ) ;
#27641=CARTESIAN_POINT ( 'NONE',  ( -25.50000000000000355, -15.50000000000000000, 20.49999999999999645 ) ) ;
#27655=EDGE_CURVE ( 'NONE', #18488, #27508, #19253, .T. ) ;
#27659=AXIS2_PLACEMENT_3D ( 'NONE', #4970, #43478, #64707 ) ;
#27669=CARTESIAN_POINT ( 'NONE',  ( 28.00000000000000000, -15.50000000000000000, 14.50000000000000000 ) ) ;
#27672=DIRECTION ( 'NONE',  ( 0.000000000000000000, 0.000000000000000000, 1.000000000000000000 ) ) ;
#27673=ORIENTED_EDGE ( 'NONE', *, *, #38285, .F. ) ;
#27679=VERTEX_POINT ( 'NONE', #59068 ) ;
#27681=ORIENTED_EDGE ( 'NONE', *, *, #63650, .T. ) ;
#27682=DIRECTION ( 'NONE',  ( 0.000000000000000000, -0.1249999999999996531, -0.9921567416492215186 ) ) ;
#27690=ORIENTED_EDGE ( 'NONE', *, *, #31980, .F. ) ;
#27691=DIRECTION ( 'NONE',  ( 1.000000000000000000, -0.000000000000000000, -0.000000000000000000 ) ) ;
#27697=CIRCLE ( 'NONE', #67206, 3.499999999999041655 ) ;
#27699=ORIENTED_EDGE ( 'NONE', *, *, #11643, .F. ) ;
#27700=VECTOR ( 'NONE', #16226, 1000.000000000000000 ) ;
#27701=CARTESIAN_POINT ( 'NONE',  ( -13.00000000000000178, -16.64230188589300141, 14.64519951917099583 ) ) ;
#27703=CIRCLE ( 'NONE', #6252, 3.499999999999999556 ) ;
#27712=VECTOR ( 'NONE', #265, 1000.000000000000000 ) ;
#27719=CARTESIAN_POINT ( 'NONE',  ( -11.75000000000000000, -5.200000000000001066, -26.25000000000000000 ) ) ;
#27725=AXIS2_PLACEMENT_3D ( 'NONE', #53544, #147, #42918 ) ;
#27727=CARTESIAN_POINT ( 'NONE',  ( -25.50000000000000355, -15.50000000000000000, -22.50000000000000000 ) ) ;
#27730=AXIS2_PLACEMENT_3D ( 'NONE', #58410, #4322, #14913 ) ;
#27740=ORIENTED_EDGE ( 'NONE', *, *, #52482, .F. ) ;
#27742=ORIENTED_EDGE ( 'NONE', *, *, #11180, .F. ) ;
#27752=DIRECTION ( 'NONE',  ( 0.000000000000000000, 0.000000000000000000, -1.000000000000000000 ) ) ;
#27763=VECTOR ( 'NONE', #68104, 1000.000000000000000 ) ;
#27770=DIRECTION ( 'NONE',  ( -1.000000000000000000, 0.000000000000000000, 0.000000000000000000 ) ) ;
#27774=DIRECTION ( 'NONE',  ( -1.000000000000000000, 0.000000000000000000, 0.000000000000000000 ) ) ;
#27796=EDGE_CURVE ( 'NONE', #47032, #30962, #1201, .T. ) ;
#27798=CIRCLE ( 'NONE', #69603, 0.3500000000002722600 ) ;
#27800=EDGE_CURVE ( 'NONE', #25525, #68528, #49501, .T. ) ;
#27805=CIRCLE ( 'NONE', #8615, 3.499999999999040323 ) ;
#27806=VECTOR ( 'NONE', #2436, 1000.000000000000000 ) ;
#27814=AXIS2_PLACEMENT_3D ( 'NONE', #17287, #32539, #53751 ) ;
#27816=ORIENTED_EDGE ( 'NONE', *, *, #8840, .T. ) ;
#27829=CARTESIAN_POINT ( 'NONE',  ( 11.50000000000000000, -11.50000000000100009, -10.50000000000065903 ) ) ;
#27832=ORIENTED_EDGE ( 'NONE', *, *, #48521, .F. ) ;
#27834=PLANE ( 'NONE',  #40093 ) ;
#27835=DIRECTION ( 'NONE',  ( 0.000000000000000000, 0.000000000000000000, 1.000000000000000000 ) ) ;
#27840=CIRCLE ( 'NONE', #62808, 0.2000000000005261458 ) ;
#27842=EDGE_CURVE ( 'NONE', #52180, #42854, #11996, .T. ) ;
#27847=CARTESIAN_POINT ( 'NONE',  ( -15.50000000000000000, -1.037157890325000054, -22.50000000000000000 ) ) ;
#27850=VECTOR ( 'NONE', #5348, 1000.000000000000000 ) ;
#27854=CARTESIAN_POINT ( 'NONE',  ( 30.00000000000000000, -11.70000000000012008, -10.70000000000011831 ) ) ;
#27855=DIRECTION ( 'NONE',  ( 0.000000000000000000, 0.000000000000000000, 1.000000000000000000 ) ) ;
#27865=VECTOR ( 'NONE', #41312, 1000.000000000000000 ) ;
#27871=CARTESIAN_POINT ( 'NONE',  ( -30.00000000000000000, -12.00000000000000000, -12.20000000000000107 ) ) ;
#27873=DIRECTION ( 'NONE',  ( 1.000000000000000000, 0.000000000000000000, 0.000000000000000000 ) ) ;
#27877=VERTEX_POINT ( 'NONE', #7040 ) ;
#27888=CARTESIAN_POINT ( 'NONE',  ( -30.00000000000000000, -14.04000000000000092, -14.80000000000000071 ) ) ;
#27889=ORIENTED_EDGE ( 'NONE', *, *, #26372, .F. ) ;
#27896=CIRCLE ( 'NONE', #44772, 2.250000000000001776 ) ;
#27898=DIRECTION ( 'NONE',  ( 0.000000000000000000, -1.000000000000000000, 0.000000000000000000 ) ) ;
#27900=CARTESIAN_POINT ( 'NONE',  ( -15.50000000000000000, -5.000000000000000000, 19.00000000000000000 ) ) ;
#27903=ORIENTED_EDGE ( 'NONE', *, *, #584, .F. ) ;
#27905=EDGE_CURVE ( 'NONE', #19992, #60323, #24001, .T. ) ;
#27907=EDGE_LOOP ( 'NONE', ( #14103, #58623, #29007, #69811 ) ) ;
#27909=CARTESIAN_POINT ( 'NONE',  ( 11.50000000000000000, -11.50000000000000000, 15.00000000000000000 ) ) ;
#27919=PLANE ( 'NONE',  #44374 ) ;
#27921=EDGE_LOOP ( 'NONE', ( #39614, #1656, #62533, #18242 ) ) ;
#27925=VERTEX_POINT ( 'NONE', #51228 ) ;
#27931=DIRECTION ( 'NONE',  ( 0.000000000000000000, 0.000000000000000000, -1.000000000000000000 ) ) ;
#27934=ORIENTED_EDGE ( 'NONE', *, *, #16869, .T. ) ;
#27936=CARTESIAN_POINT ( 'NONE',  ( 29.50000000000000355, -12.00000000000000000, 11.00000000000000000 ) ) ;
#27939=VERTEX_POINT ( 'NONE', #35293 ) ;
#27953=DIRECTION ( 'NONE',  ( -0.8660254037844482555, 0.000000000000000000, -0.4999999999999831801 ) ) ;
#27955=VECTOR ( 'NONE', #12727, 1000.000000000000114 ) ;
#27957=DIRECTION ( 'NONE',  ( 0.000000000000000000, 0.000000000000000000, 1.000000000000000000 ) ) ;
#27963=LINE ( 'NONE', #48493, #42191 ) ;
#27969=FACE_OUTER_BOUND ( 'NONE', #15133, .T. ) ;
#27971=EDGE_CURVE ( 'NONE', #37432, #16302, #61027, .T. ) ;
#27972=AXIS2_PLACEMENT_3D ( 'NONE', #48735, #59342, #28201 ) ;
#27975=EDGE_CURVE ( 'NONE', #29308, #6488, #8431, .T. ) ;
#27988=DIRECTION ( 'NONE',  ( -1.000000000000000000, 0.000000000000000000, 0.000000000000000000 ) ) ;
#27989=VERTEX_POINT ( 'NONE', #57931 ) ;
#27990=EDGE_CURVE ( 'NONE', #18063, #37646, #3847, .T. ) ;
#28000=CARTESIAN_POINT ( 'NONE',  ( 23.48000000000000043, -17.50000000000000000, -26.00000000000000355 ) ) ;
#28004=EDGE_LOOP ( 'NONE', ( #49156, #7720, #48883, #44748, #42774, #44913 ) ) ;
#28006=CARTESIAN_POINT ( 'NONE',  ( 15.50000000000000000, -2.500000000000000000, 21.05662432702600029 ) ) ;
#28011=ORIENTED_EDGE ( 'NONE', *, *, #23641, .F. ) ;
#28012=ORIENTED_EDGE ( 'NONE', *, *, #19477, .T. ) ;
#28015=DIRECTION ( 'NONE',  ( 0.000000000000000000, 0.000000000000000000, -1.000000000000000000 ) ) ;
#28019=EDGE_LOOP ( 'NONE', ( #52469, #6334, #17374, #34587, #49647, #61573, #29094, #18491, #2852, #20873, #667, #48547, #54200, #40208, #21686, #63283, #328, #44968 ) ) ;
#28020=DIRECTION ( 'NONE',  ( 0.000000000000000000, 3.989863994748342081E-13, 1.000000000000000000 ) ) ;
#28025=LINE ( 'NONE', #59157, #60702 ) ;
#28028=EDGE_LOOP ( 'NONE', ( #64192, #16163, #22256, #55641 ) ) ;
#28039=ORIENTED_EDGE ( 'NONE', *, *, #37741, .F. ) ;
#28040=CARTESIAN_POINT ( 'NONE',  ( -30.00000000000000000, -5.000000000000000000, 27.00000000000000000 ) ) ;
#28042=EDGE_CURVE ( 'NONE', #31900, #12490, #31780, .T. ) ;
#28044=EDGE_CURVE ( 'NONE', #15054, #14428, #4556, .T. ) ;
#28051=EDGE_LOOP ( 'NONE', ( #16362, #23284, #34690, #53078 ) ) ;
#28052=DIRECTION ( 'NONE',  ( 0.000000000000000000, -1.000000000000000000, 0.000000000000000000 ) ) ;
#28055=VECTOR ( 'NONE', #14418, 1000.000000000000114 ) ;
#28063=FACE_OUTER_BOUND ( 'NONE', #69778, .T. ) ;
#28064=DIRECTION ( 'NONE',  ( -1.000000000000000000, 0.000000000000000000, 0.000000000000000000 ) ) ;
#28067=DIRECTION ( 'NONE',  ( 0.000000000000000000, -0.9921567416492215186, 0.1249999999999996531 ) ) ;
#28069=EDGE_CURVE ( 'NONE', #67816, #16876, #63600, .T. ) ;
#28073=EDGE_CURVE ( 'NONE', #7006, #10852, #67866, .T. ) ;
#28078=ORIENTED_EDGE ( 'NONE', *, *, #49984, .T. ) ;
#28087=DIRECTION ( 'NONE',  ( 0.000000000000000000, 0.000000000000000000, 1.000000000000000000 ) ) ;
#28092=ORIENTED_EDGE ( 'NONE', *, *, #44525, .F. ) ;
#28106=EDGE_CURVE ( 'NONE', #50851, #24869, #66287, .T. ) ;
#28112=CARTESIAN_POINT ( 'NONE',  ( 30.00000000000000000, -9.199999999999999289, 12.69999999999986073 ) ) ;
#28122=CIRCLE ( 'NONE', #30396, 0.3499999999999285905 ) ;
#28124=DIRECTION ( 'NONE',  ( 1.000000000000000000, -0.000000000000000000, -0.000000000000000000 ) ) ;
#28128=DIRECTION ( 'NONE',  ( -1.000000000000000000, 0.000000000000000000, 0.000000000000000000 ) ) ;
#28131=VERTEX_POINT ( 'NONE', #7917 ) ;
#28134=DIRECTION ( 'NONE',  ( 0.000000000000000000, 0.7057491738665943037, 0.7084617869628675457 ) ) ;
#28142=CARTESIAN_POINT ( 'NONE',  ( 11.75000000000000000, -5.200000000000001066, -11.75000000000000000 ) ) ;
#28147=DIRECTION ( 'NONE',  ( 1.000000000000000000, -0.000000000000000000, -0.000000000000000000 ) ) ;
#28148=LINE ( 'NONE', #44388, #66145 ) ;
#28153=AXIS2_PLACEMENT_3D ( 'NONE', #34865, #66005, #45126 ) ;
#28156=ORIENTED_EDGE ( 'NONE', *, *, #18490, .T. ) ;
#28162=CARTESIAN_POINT ( 'NONE',  ( -25.50000000000000355, -15.50000000000000000, -22.50000000000000000 ) ) ;
#28164=ORIENTED_EDGE ( 'NONE', *, *, #69097, .F. ) ;
#28170=ORIENTED_EDGE ( 'NONE', *, *, #64966, .F. ) ;
#28182=ORIENTED_EDGE ( 'NONE', *, *, #5113, .F. ) ;
#28195=CARTESIAN_POINT ( 'NONE',  ( 25.50000000000000355, -15.50000000000000000, -22.50000000000000000 ) ) ;
#28197=VERTEX_POINT ( 'NONE', #34427 ) ;
#28198=DIRECTION ( 'NONE',  ( 0.000000000000000000, 0.000000000000000000, -1.000000000000000000 ) ) ;
#28201=DIRECTION ( 'NONE',  ( 0.000000000000000000, -0.1249999999999996531, -0.9921567416492215186 ) ) ;
#28206=CARTESIAN_POINT ( 'NONE',  ( 30.00000000000000000, -10.85999999999999943, -9.350000000000269651 ) ) ;
#28211=CARTESIAN_POINT ( 'NONE',  ( -29.50000000000000355, -11.70000000000012008, 10.70000000000011831 ) ) ;
#28216=CARTESIAN_POINT ( 'NONE',  ( 30.00000000000000000, -11.70000000000000284, -12.50000000000000000 ) ) ;
#28218=VERTEX_POINT ( 'NONE', #50707 ) ;
#28229=EDGE_CURVE ( 'NONE', #48332, #4626, #46457, .T. ) ;
#28230=CARTESIAN_POINT ( 'NONE',  ( -16.75000000000000000, -2.500000000000000000, 21.77831216351300014 ) ) ;
#28234=ORIENTED_EDGE ( 'NONE', *, *, #20458, .F. ) ;
#28244=VERTEX_POINT ( 'NONE', #69431 ) ;
#28263=VECTOR ( 'NONE', #58547, 1000.000000000000000 ) ;
#28273=PLANE ( 'NONE',  #14372 ) ;
#28289=DIRECTION ( 'NONE',  ( -1.000000000000000000, 0.000000000000000000, 0.000000000000000000 ) ) ;
#28293=PLANE ( 'NONE',  #53857 ) ;
#28295=AXIS2_PLACEMENT_3D ( 'NONE', #48847, #15969, #69361 ) ;
#28308=CARTESIAN_POINT ( 'NONE',  ( 30.00000000000000000, -8.959999999999999076, 17.04524521594300523 ) ) ;
#28311=EDGE_CURVE ( 'NONE', #26875, #34775, #51770, .T. ) ;
#28313=AXIS2_PLACEMENT_3D ( 'NONE', #4912, #68568, #4570 ) ;
#28316=CARTESIAN_POINT ( 'NONE',  ( 30.00000000000000000, -17.00000000000000000, 15.70499999999969809 ) ) ;
#28319=ORIENTED_EDGE ( 'NONE', *, *, #35341, .F. ) ;
#28320=LINE ( 'NONE', #23371, #17106 ) ;
#28322=FACE_OUTER_BOUND ( 'NONE', #894, .T. ) ;
#28332=ORIENTED_EDGE ( 'NONE', *, *, #56284, .T. ) ;
#28335=VECTOR ( 'NONE', #36725, 1000.000000000000000 ) ;
#28340=VERTEX_POINT ( 'NONE', #8972 ) ;
#28343=DIRECTION ( 'NONE',  ( 0.4999999999999827360, 0.000000000000000000, 0.8660254037844485886 ) ) ;
#28344=CARTESIAN_POINT ( 'NONE',  ( 16.54633693294649888, -0.2717122460102533998, -21.66072723692568402 ) ) ;
#28346=CIRCLE ( 'NONE', #5811, 4.500000000000190958 ) ;
#28363=ADVANCED_FACE ( 'NONE', ( #10038 ), #30551, .F. ) ;
#28364=DIRECTION ( 'NONE',  ( 1.000000000000000000, -0.000000000000000000, -0.000000000000000000 ) ) ;
#28368=EDGE_CURVE ( 'NONE', #5395, #32193, #63382, .T. ) ;
#28369=ORIENTED_EDGE ( 'NONE', *, *, #54669, .F. ) ;
#28371=EDGE_CURVE ( 'NONE', #35366, #64273, #19939, .T. ) ;
#28376=CARTESIAN_POINT ( 'NONE',  ( -18.85410196625000268, -17.50000000000000000, -21.50000000000000000 ) ) ;
#28377=CARTESIAN_POINT ( 'NONE',  ( 30.00000000000000000, -9.199999999999999289, -12.34999999999989839 ) ) ;
#28378=CARTESIAN_POINT ( 'NONE',  ( -15.50000000000000000, -5.000000000000000000, -22.50000000000000000 ) ) ;
#28380=EDGE_LOOP ( 'NONE', ( #21970, #8470, #44946, #8065 ) ) ;
#28385=ORIENTED_EDGE ( 'NONE', *, *, #52482, .T. ) ;
#28388=ORIENTED_EDGE ( 'NONE', *, *, #36622, .T. ) ;
#28393=FACE_OUTER_BOUND ( 'NONE', #64956, .T. ) ;
#28402=CARTESIAN_POINT ( 'NONE',  ( -25.50000000000000355, -15.50000000000000000, -22.50000000000000000 ) ) ;
#28403=ORIENTED_EDGE ( 'NONE', *, *, #63608, .F. ) ;
#28424=ORIENTED_EDGE ( 'NONE', *, *, #9200, .T. ) ;
#28430=FACE_OUTER_BOUND ( 'NONE', #36624, .T. ) ;
#28431=ORIENTED_EDGE ( 'NONE', *, *, #3055, .T. ) ;
#28445=VECTOR ( 'NONE', #21223, 1000.000000000000114 ) ;
#28449=DIRECTION ( 'NONE',  ( 0.000000000000000000, 0.000000000000000000, -1.000000000000000000 ) ) ;
#28451=LINE ( 'NONE', #60284, #66316 ) ;
#28452=VECTOR ( 'NONE', #24823, 1000.000000000000000 ) ;
#28455=EDGE_CURVE ( 'NONE', #34056, #60969, #49591, .T. ) ;
#28456=ORIENTED_EDGE ( 'NONE', *, *, #21207, .F. ) ;
#28468=CARTESIAN_POINT ( 'NONE',  ( -14.25000000000000000, -0.2038245569916330158, -21.77831216351300014 ) ) ;
#28485=EDGE_CURVE ( 'NONE', #4816, #32597, #473, .T. ) ;
#28486=ORIENTED_EDGE ( 'NONE', *, *, #6927, .F. ) ;
#28488=DIRECTION ( 'NONE',  ( 0.000000000000000000, 0.000000000000000000, -1.000000000000000000 ) ) ;
#28502=EDGE_CURVE ( 'NONE', #21801, #1690, #50948, .T. ) ;
#28507=ORIENTED_EDGE ( 'NONE', *, *, #33302, .F. ) ;
#28512=AXIS2_PLACEMENT_3D ( 'NONE', #26136, #25791, #57250 ) ;
#28528=LINE ( 'NONE', #23224, #35756 ) ;
#28530=CARTESIAN_POINT ( 'NONE',  ( -27.50000000000000000, -5.200000000000001066, -22.50000000000000000 ) ) ;
#28539=ORIENTED_EDGE ( 'NONE', *, *, #51281, .F. ) ;
#28542=FACE_OUTER_BOUND ( 'NONE', #9932, .T. ) ;
#28547=CARTESIAN_POINT ( 'NONE',  ( 28.00000000000000000, -17.00000000000000000, -15.70499999999969809 ) ) ;
#28554=LINE ( 'NONE', #19000, #13061 ) ;
#28557=CARTESIAN_POINT ( 'NONE',  ( 16.75000000000000000, -0.2038245569916320166, -21.77831216351300014 ) ) ;
#28562=DIRECTION ( 'NONE',  ( 0.000000000000000000, -0.7071067811865496822, 0.7071067811865454633 ) ) ;
#28571=EDGE_CURVE ( 'NONE', #44549, #68445, #146, .T. ) ;
#28577=EDGE_CURVE ( 'NONE', #27584, #60914, #12777, .T. ) ;
#28579=DIRECTION ( 'NONE',  ( -1.000000000000000000, 0.000000000000000000, 0.000000000000000000 ) ) ;
#28588=DIRECTION ( 'NONE',  ( 0.000000000000000000, 0.7096009616570518874, 0.7046037717862339012 ) ) ;
#28591=CARTESIAN_POINT ( 'NONE',  ( -30.00000000000000000, -12.00000000000000000, -12.20000000000000107 ) ) ;
#28596=VERTEX_POINT ( 'NONE', #29062 ) ;
#28608=EDGE_LOOP ( 'NONE', ( #32466, #35041, #10271, #26968 ) ) ;
#28615=ADVANCED_FACE ( 'NONE', ( #29748 ), #51322, .F. ) ;
#28616=FACE_OUTER_BOUND ( 'NONE', #16610, .T. ) ;
#28621=FACE_OUTER_BOUND ( 'NONE', #42905, .T. ) ;
#28626=FACE_OUTER_BOUND ( 'NONE', #25053, .T. ) ;
#28628=ORIENTED_EDGE ( 'NONE', *, *, #25314, .F. ) ;
#28630=LINE ( 'NONE', #1417, #31610 ) ;
#28633=ORIENTED_EDGE ( 'NONE', *, *, #49984, .F. ) ;
#28635=CARTESIAN_POINT ( 'NONE',  ( -15.50000000000000000, -0.4000000000000000222, 22.50000000000000000 ) ) ;
#28639=ORIENTED_EDGE ( 'NONE', *, *, #40166, .T. ) ;
#28640=DIRECTION ( 'NONE',  ( -0.000000000000000000, 1.000000000000000000, -0.000000000000000000 ) ) ;
#28645=EDGE_CURVE ( 'NONE', #39887, #15366, #57717, .T. ) ;
#28650=ORIENTED_EDGE ( 'NONE', *, *, #41942, .T. ) ;
#28653=LINE ( 'NONE', #30323, #51870 ) ;
#28654=ADVANCED_FACE ( 'NONE', ( #6790 ), #23757, .F. ) ;
#28656=CIRCLE ( 'NONE', #47853, 0.3499999999999285905 ) ;
#28664=VERTEX_POINT ( 'NONE', #49929 ) ;
#28673=LINE ( 'NONE', #34670, #2612 ) ;
#28676=DIRECTION ( 'NONE',  ( 0.000000000000000000, 0.000000000000000000, -1.000000000000000000 ) ) ;
#28680=EDGE_LOOP ( 'NONE', ( #16962, #65572, #38556, #43548 ) ) ;
#28685=LINE ( 'NONE', #12409, #62435 ) ;
#28689=CARTESIAN_POINT ( 'NONE',  ( 16.75000000000000000, -0.2038245569916320166, -21.77831216351300014 ) ) ;
#28691=ORIENTED_EDGE ( 'NONE', *, *, #39420, .T. ) ;
#28692=ORIENTED_EDGE ( 'NONE', *, *, #48130, .T. ) ;
#28694=DIRECTION ( 'NONE',  ( 1.000000000000000000, -0.000000000000000000, -0.000000000000000000 ) ) ;
#28710=CARTESIAN_POINT ( 'NONE',  ( 16.75000000000000000, -2.500000000000000000, 23.22168783648699986 ) ) ;
#28716=CARTESIAN_POINT ( 'NONE',  ( -24.00000000000000000, -17.00000000000000000, -15.70499999999969809 ) ) ;
#28718=VERTEX_POINT ( 'NONE', #62626 ) ;
#28720=LINE ( 'NONE', #35410, #6393 ) ;
#28730=ORIENTED_EDGE ( 'NONE', *, *, #41838, .F. ) ;
#28733=CONICAL_SURFACE ( 'NONE', #44520, 1.621000000000000885, 0.7853981633974518317 ) ;
#28736=CARTESIAN_POINT ( 'NONE',  ( 0.000000000000000000, 0.000000000000000000, 0.000000000000000000 ) ) ;
#28745=ADVANCED_FACE ( 'NONE', ( #52382 ), #20199, .T. ) ;
#28746=VECTOR ( 'NONE', #7247, 1000.000000000000000 ) ;
#28747=CARTESIAN_POINT ( 'NONE',  ( 30.00000000000000000, -5.599999999999999645, 9.000000000000001776 ) ) ;
#28753=FACE_OUTER_BOUND ( 'NONE', #68649, .T. ) ;
#28758=ORIENTED_EDGE ( 'NONE', *, *, #4204, .T. ) ;
#28760=ORIENTED_EDGE ( 'NONE', *, *, #34480, .F. ) ;
#28763=LINE ( 'NONE', #50334, #33205 ) ;
#28770=DIRECTION ( 'NONE',  ( 0.000000000000000000, -0.7096009616570518874, -0.7046037717862339012 ) ) ;
#28781=CARTESIAN_POINT ( 'NONE',  ( 15.50000000000129852, -17.50000000000000000, 22.50000000000000000 ) ) ;
#28784=CARTESIAN_POINT ( 'NONE',  ( -30.00000000000000000, -14.04000000000000092, 14.80000000000000071 ) ) ;
#28786=EDGE_CURVE ( 'NONE', #16582, #21729, #53097, .T. ) ;
#28792=LINE ( 'NONE', #34797, #49020 ) ;
#28796=CIRCLE ( 'NONE', #15303, 0.5000000000079367624 ) ;
#28809=DIRECTION ( 'NONE',  ( 0.000000000000000000, 0.6857142857142843884, 0.7278708115918295363 ) ) ;
#28810=DIRECTION ( 'NONE',  ( -1.000000000000000000, 0.000000000000000000, 0.000000000000000000 ) ) ;
#28820=ORIENTED_EDGE ( 'NONE', *, *, #58057, .T. ) ;
#28824=EDGE_CURVE ( 'NONE', #69842, #24526, #21606, .T. ) ;
#28830=AXIS2_PLACEMENT_3D ( 'NONE', #47974, #10834, #36669 ) ;
#28835=EDGE_CURVE ( 'NONE', #58770, #52725, #20524, .T. ) ;
#28837=EDGE_CURVE ( 'NONE', #23447, #11691, #19398, .T. ) ;
#28842=VECTOR ( 'NONE', #36445, 1000.000000000000000 ) ;
#28848=VECTOR ( 'NONE', #55465, 1000.000000000000000 ) ;
#28853=AXIS2_PLACEMENT_3D ( 'NONE', #4886, #48370, #37416 ) ;
#28854=CARTESIAN_POINT ( 'NONE',  ( -11.00000000000000000, -11.50000000000000000, -15.00000000000000000 ) ) ;
#28857=CARTESIAN_POINT ( 'NONE',  ( -11.00000000000000000, -16.28999999999999915, -14.50000000000000000 ) ) ;
#28863=ORIENTED_EDGE ( 'NONE', *, *, #37555, .F. ) ;
#28864=EDGE_CURVE ( 'NONE', #60150, #47415, #63434, .T. ) ;
#28881=EDGE_CURVE ( 'NONE', #28664, #67299, #11324, .T. ) ;
#28888=VECTOR ( 'NONE', #16131, 1000.000000000000000 ) ;
#28891=EDGE_CURVE ( 'NONE', #41558, #41898, #16654, .T. ) ;
#28896=VECTOR ( 'NONE', #62153, 1000.000000000000000 ) ;
#28897=CARTESIAN_POINT ( 'NONE',  ( -15.50000000000000000, -5.000000000000000000, -26.50000000000000000 ) ) ;
#28902=VERTEX_POINT ( 'NONE', #10633 ) ;
#28908=CARTESIAN_POINT ( 'NONE',  ( -23.75054448485400016, -15.50000000000000000, 25.53140320652400064 ) ) ;
#28911=ORIENTED_EDGE ( 'NONE', *, *, #8896, .T. ) ;
#28917=CARTESIAN_POINT ( 'NONE',  ( 29.50000000000000355, -11.50000000000000000, 19.00000000000000000 ) ) ;
#28922=CARTESIAN_POINT ( 'NONE',  ( 30.00000000000000000, -13.79999999999979998, 17.30000000000000071 ) ) ;
#28933=FACE_OUTER_BOUND ( 'NONE', #15808, .T. ) ;
#28942=AXIS2_PLACEMENT_3D ( 'NONE', #35444, #52077, #57375 ) ;
#28950=CIRCLE ( 'NONE', #10895, 4.000000000000000888 ) ;
#28953=DIRECTION ( 'NONE',  ( 0.000000000000000000, 1.000000000000000000, 0.000000000000000000 ) ) ;
#28955=ORIENTED_EDGE ( 'NONE', *, *, #20152, .T. ) ;
#28956=VECTOR ( 'NONE', #18435, 1000.000000000000000 ) ;
#28964=EDGE_LOOP ( 'NONE', ( #35678, #2868, #8695, #28424, #21374, #54783 ) ) ;
#28981=LINE ( 'NONE', #51606, #6402 ) ;
#28988=CARTESIAN_POINT ( 'NONE',  ( -15.50000000000000000, -2.500000000000000000, -21.05662432702600029 ) ) ;
#28990=VERTEX_POINT ( 'NONE', #17320 ) ;
#29007=ORIENTED_EDGE ( 'NONE', *, *, #11189, .F. ) ;
#29008=CARTESIAN_POINT ( 'NONE',  ( -15.50000000000000000, -2.500000000000000000, 21.05662432702600029 ) ) ;
#29017=CYLINDRICAL_SURFACE ( 'NONE', #32963, 0.5000000000079367624 ) ;
#29020=PRODUCT_DEFINITION_SHAPE ( 'NONE', 'NONE',  #29636 ) ;
#29030=EDGE_LOOP ( 'NONE', ( #58085, #22180, #35574, #61289, #11391, #28388, #16562, #27832, #50432 ) ) ;
#29033=ORIENTED_EDGE ( 'NONE', *, *, #5937, .T. ) ;
#29049=VERTEX_POINT ( 'NONE', #65766 ) ;
#29051=EDGE_CURVE ( 'NONE', #68865, #12955, #6709, .T. ) ;
#29057=EDGE_CURVE ( 'NONE', #9204, #8160, #46503, .T. ) ;
#29061=AXIS2_PLACEMENT_3D ( 'NONE', #64610, #43032, #32444 ) ;
#29062=CARTESIAN_POINT ( 'NONE',  ( 30.00000000000000000, -5.599999999999999645, -9.000000000000001776 ) ) ;
#29072=DIRECTION ( 'NONE',  ( 0.000000000000000000, -0.7096009616570518874, 0.7046037717862339012 ) ) ;
#29077=DIRECTION ( 'NONE',  ( 0.000000000000000000, 0.000000000000000000, -1.000000000000000000 ) ) ;
#29080=LINE ( 'NONE', #60893, #18209 ) ;
#29081=DIRECTION ( 'NONE',  ( 0.000000000000000000, 0.000000000000000000, 1.000000000000000000 ) ) ;
#29086=FACE_OUTER_BOUND ( 'NONE', #37752, .T. ) ;
#29094=ORIENTED_EDGE ( 'NONE', *, *, #54552, .T. ) ;
#29103=CIRCLE ( 'NONE', #30227, 4.000000000000000888 ) ;
#29118=EDGE_CURVE ( 'NONE', #32857, #18730, #36027, .T. ) ;
#29149=LINE ( 'NONE', #60634, #64826 ) ;
#29151=EDGE_CURVE ( 'NONE', #66059, #46437, #19751, .T. ) ;
#29154=AXIS2_PLACEMENT_3D ( 'NONE', #51578, #24701, #62507 ) ;
#29158=DIRECTION ( 'NONE',  ( 0.000000000000000000, 1.000000000000000000, 0.000000000000000000 ) ) ;
#29165=DIRECTION ( 'NONE',  ( 0.000000000000000000, 1.000000000000000000, 0.000000000000000000 ) ) ;
#29167=CYLINDRICAL_SURFACE ( 'NONE', #51091, 3.499999999999850342 ) ;
#29177=CARTESIAN_POINT ( 'NONE',  ( -17.00000000000000000, -16.64230188589299786, 14.64519951917100116 ) ) ;
#29186=CARTESIAN_POINT ( 'NONE',  ( 25.50000000000000355, -5.578999999999999737, -22.50000000000000000 ) ) ;
#29189=CARTESIAN_POINT ( 'NONE',  ( 30.00000000000000000, -17.14999999999999858, 27.00000000000000000 ) ) ;
#29191=EDGE_LOOP ( 'NONE', ( #37995, #45875, #69264, #62869, #15812, #9518, #61596, #2964, #49857, #61521, #33732, #2336, #3739, #21076, #15416, #7661 ) ) ;
#29193=CARTESIAN_POINT ( 'NONE',  ( 15.50000000000129852, -15.50000000000000000, 22.50000000000000000 ) ) ;
#29197=ORIENTED_EDGE ( 'NONE', *, *, #27990, .T. ) ;
#29198=ORIENTED_EDGE ( 'NONE', *, *, #36367, .F. ) ;
#29199=ORIENTED_EDGE ( 'NONE', *, *, #48811, .T. ) ;
#29205=CARTESIAN_POINT ( 'NONE',  ( 30.00000000000000000, -8.959999999999999076, -12.95475478405700009 ) ) ;
#29207=ORIENTED_EDGE ( 'NONE', *, *, #42420, .T. ) ;
#29209=DIRECTION ( 'NONE',  ( 0.000000000000000000, 0.000000000000000000, 1.000000000000000000 ) ) ;
#29211=FACE_OUTER_BOUND ( 'NONE', #5835, .T. ) ;
#29214=CARTESIAN_POINT ( 'NONE',  ( -11.00000000000000000, -9.487228132326899654, -12.50000000000000000 ) ) ;
#29217=DIRECTION ( 'NONE',  ( 0.000000000000000000, 1.000000000000000000, 0.000000000000000000 ) ) ;
#29223=FACE_OUTER_BOUND ( 'NONE', #25060, .T. ) ;
#29225=CYLINDRICAL_SURFACE ( 'NONE', #50014, 4.000000000000000000 ) ;
#29226=EDGE_CURVE ( 'NONE', #46315, #9955, #26237, .T. ) ;
#29230=DIRECTION ( 'NONE',  ( 0.000000000000000000, 0.000000000000000000, 1.000000000000000000 ) ) ;
#29245=CARTESIAN_POINT ( 'NONE',  ( -15.50000000000000000, -0.4000000000000000222, 19.00000000000000355 ) ) ;
#29249=VECTOR ( 'NONE', #2008, 1000.000000000000000 ) ;
#29252=CARTESIAN_POINT ( 'NONE',  ( -30.00000000000000000, -5.200000000000001066, -26.59999999999999787 ) ) ;
#29255=CARTESIAN_POINT ( 'NONE',  ( 15.50000000000000000, -0.4000000000005274892, -25.79999999999946780 ) ) ;
#29256=VECTOR ( 'NONE', #12011, 1000.000000000000000 ) ;
#29267=DIRECTION ( 'NONE',  ( -0.9583148474998867128, 0.000000000000000000, 0.2857142857143631365 ) ) ;
#29287=VERTEX_POINT ( 'NONE', #53356 ) ;
#29290=CARTESIAN_POINT ( 'NONE',  ( 16.75000000000000000, -2.500000000000000000, 23.22168783648699986 ) ) ;
#29292=EDGE_CURVE ( 'NONE', #51111, #54102, #44278, .T. ) ;
#29296=VECTOR ( 'NONE', #10060, 1000.000000000000000 ) ;
#29302=VECTOR ( 'NONE', #69103, 1000.000000000000000 ) ;
#29308=VERTEX_POINT ( 'NONE', #32126 ) ;
#29318=CARTESIAN_POINT ( 'NONE',  ( -28.00000000000000000, -17.35230188589299871, 15.35019951917099945 ) ) ;
#29319=CARTESIAN_POINT ( 'NONE',  ( 11.00000000000000000, -11.50000000000082068, -10.20500000000000007 ) ) ;
#29323=ORIENTED_EDGE ( 'NONE', *, *, #16480, .T. ) ;
#29325=AXIS2_PLACEMENT_3D ( 'NONE', #10786, #65252, #63847 ) ;
#29327=ORIENTED_EDGE ( 'NONE', *, *, #41287, .T. ) ;
#29328=CARTESIAN_POINT ( 'NONE',  ( 11.50000000000000000, -12.00000000000000000, -10.52786404500095863 ) ) ;
#29330=EDGE_CURVE ( 'NONE', #20601, #49081, #69949, .T. ) ;
#29331=ORIENTED_EDGE ( 'NONE', *, *, #62930, .F. ) ;
#29340=ORIENTED_EDGE ( 'NONE', *, *, #25397, .T. ) ;
#29343=ORIENTED_EDGE ( 'NONE', *, *, #13749, .F. ) ;
#29364=AXIS2_PLACEMENT_3D ( 'NONE', #3951, #41063, #52040 ) ;
#29365=VECTOR ( 'NONE', #58180, 1000.000000000000000 ) ;
#29377=ORIENTED_EDGE ( 'NONE', *, *, #60779, .F. ) ;
#29380=ADVANCED_FACE ( 'NONE', ( #12609 ), #11571, .F. ) ;
#29390=AXIS2_PLACEMENT_3D ( 'NONE', #7384, #7735, #38547 ) ;
#29411=DIRECTION ( 'NONE',  ( -1.000000000000000000, 0.000000000000000000, 0.000000000000000000 ) ) ;
#29412=CARTESIAN_POINT ( 'NONE',  ( 25.50000000000000355, -5.200000000000001066, 22.50000000000000000 ) ) ;
#29424=ORIENTED_EDGE ( 'NONE', *, *, #67643, .T. ) ;
#29431=ORIENTED_EDGE ( 'NONE', *, *, #56752, .F. ) ;
#29438=ORIENTED_EDGE ( 'NONE', *, *, #16355, .T. ) ;
#29443=ORIENTED_EDGE ( 'NONE', *, *, #63492, .T. ) ;
#29451=FACE_OUTER_BOUND ( 'NONE', #69612, .T. ) ;
#29455=DIRECTION ( 'NONE',  ( -1.000000000000000000, 0.000000000000000000, 0.000000000000000000 ) ) ;
#29460=ORIENTED_EDGE ( 'NONE', *, *, #48965, .F. ) ;
#29461=VECTOR ( 'NONE', #43283, 1000.000000000000000 ) ;
#29462=CIRCLE ( 'NONE', #61193, 0.5000000000079362072 ) ;
#29478=VERTEX_POINT ( 'NONE', #50797 ) ;
#29494=AXIS2_PLACEMENT_3D ( 'NONE', #34791, #56365, #62012 ) ;
#29499=CIRCLE ( 'NONE', #56606, 1.620999999999997332 ) ;
#29510=EDGE_LOOP ( 'NONE', ( #11277, #9675, #36074, #63843 ) ) ;
#29513=AXIS2_PLACEMENT_3D ( 'NONE', #84, #65136, #53482 ) ;
#29516=FACE_OUTER_BOUND ( 'NONE', #5374, .T. ) ;
#29521=DIRECTION ( 'NONE',  ( 0.000000000000000000, 0.7046037717862339012, 0.7096009616570518874 ) ) ;
#29532=DIRECTION ( 'NONE',  ( -1.000000000000000000, 0.000000000000000000, 0.000000000000000000 ) ) ;
#29537=LINE ( 'NONE', #3998, #59412 ) ;
#29541=EDGE_CURVE ( 'NONE', #24182, #51206, #62445, .T. ) ;
#29548=EDGE_CURVE ( 'NONE', #3375, #62137, #61765, .T. ) ;
#29553=VERTEX_POINT ( 'NONE', #24988 ) ;
#29557=DIRECTION ( 'NONE',  ( -1.000000000000000000, 0.000000000000000000, 0.000000000000000000 ) ) ;
#29565=DIRECTION ( 'NONE',  ( -0.9375000000000006661, 0.000000000000000000, 0.3479852726768744020 ) ) ;
#29585=DIRECTION ( 'NONE',  ( 0.000000000000000000, 1.000000000000000000, 0.000000000000000000 ) ) ;
#29595=DIRECTION ( 'NONE',  ( 0.000000000000000000, -5.800915303574361727E-12, 1.000000000000000000 ) ) ;
#29601=LINE ( 'NONE', #50820, #21808 ) ;
#29605=VECTOR ( 'NONE', #54759, 1000.000000000000000 ) ;
#29609=CARTESIAN_POINT ( 'NONE',  ( 14.25000000000000000, -2.500000000000000000, 21.77831216351300014 ) ) ;
#29610=AXIS2_PLACEMENT_3D ( 'NONE', #62549, #30743, #61867 ) ;
#29615=ORIENTED_EDGE ( 'NONE', *, *, #32157, .T. ) ;
#29617=ORIENTED_EDGE ( 'NONE', *, *, #28371, .T. ) ;
#29636=PRODUCT_DEFINITION ( 'UNKNOWN', '', #42640, #48782 ) ;
#29638=ADVANCED_FACE ( 'NONE', ( #30990 ), #66883, .F. ) ;
#29643=CYLINDRICAL_SURFACE ( 'NONE', #13360, 4.500000000000189182 ) ;
#29651=DIRECTION ( 'NONE',  ( 0.000000000000000000, -1.000000000000000000, 0.000000000000000000 ) ) ;
#29665=CARTESIAN_POINT ( 'NONE',  ( -11.75000000000000000, -5.000000000000000000, -21.10805890929250950 ) ) ;
#29669=ORIENTED_EDGE ( 'NONE', *, *, #56076, .T. ) ;
#29676=VECTOR ( 'NONE', #4977, 1000.000000000000114 ) ;
#29677=CARTESIAN_POINT ( 'NONE',  ( -11.00000000000000000, -12.00000000000000000, 10.52786404500095863 ) ) ;
#29683=AXIS2_PLACEMENT_3D ( 'NONE', #51796, #15372, #3353 ) ;
#29697=CARTESIAN_POINT ( 'NONE',  ( -11.00000000000000000, -12.00000000000000000, 12.20000000000000107 ) ) ;
#29699=DIRECTION ( 'NONE',  ( 0.000000000000000000, -0.7071067811865496822, 0.7071067811865454633 ) ) ;
#29705=EDGE_LOOP ( 'NONE', ( #45099, #13562, #45800, #63934 ) ) ;
#29711=CARTESIAN_POINT ( 'NONE',  ( 11.00000000000000000, -12.00000000000000000, -12.20000000000000107 ) ) ;
#29715=CARTESIAN_POINT ( 'NONE',  ( 30.00000000000000000, -14.04000000000000092, -17.04524521594300523 ) ) ;
#29716=CARTESIAN_POINT ( 'NONE',  ( -11.00000000000000000, -10.85999999999999943, 9.350000000000269651 ) ) ;
#29720=CARTESIAN_POINT ( 'NONE',  ( 17.00000000000000000, -15.50000000000000000, 2.000000000000000000 ) ) ;
#29722=VERTEX_POINT ( 'NONE', #26048 ) ;
#29727=CARTESIAN_POINT ( 'NONE',  ( -29.50000000000000355, -11.50000000000100009, 15.00000000000084910 ) ) ;
#29730=ORIENTED_EDGE ( 'NONE', *, *, #32991, .T. ) ;
#29734=VECTOR ( 'NONE', #19009, 1000.000000000000000 ) ;
#29739=CARTESIAN_POINT ( 'NONE',  ( 24.00000000000000000, -17.50000000000000000, -15.70500000000000007 ) ) ;
#29740=ORIENTED_EDGE ( 'NONE', *, *, #17921, .T. ) ;
#29741=CARTESIAN_POINT ( 'NONE',  ( 11.50000000000000000, -12.00000000000000000, 11.03137303340310282 ) ) ;
#29742=CARTESIAN_POINT ( 'NONE',  ( -11.00000000000000000, -15.97213595500069871, 14.50000000000000000 ) ) ;
#29744=EDGE_LOOP ( 'NONE', ( #23398, #33289, #50414, #50385, #2403, #4684, #57665, #15543, #27206, #65318, #21907, #37135 ) ) ;
#29748=FACE_OUTER_BOUND ( 'NONE', #40141, .T. ) ;
#29756=EDGE_CURVE ( 'NONE', #29819, #26009, #51098, .T. ) ;
#29759=CARTESIAN_POINT ( 'NONE',  ( -11.50000000000000000, -12.00000000000000000, -11.00000000000000000 ) ) ;
#29771=VERTEX_POINT ( 'NONE', #48309 ) ;
#29772=VECTOR ( 'NONE', #52431, 1000.000000000000000 ) ;
#29777=ORIENTED_EDGE ( 'NONE', *, *, #34416, .T. ) ;
#29783=CARTESIAN_POINT ( 'NONE',  ( 11.00000000000000000, -8.959999999999999076, -17.04524521594300523 ) ) ;
#29802=AXIS2_PLACEMENT_3D ( 'NONE', #64851, #64168, #42577 ) ;
#29804=CARTESIAN_POINT ( 'NONE',  ( -11.00000000000000000, -9.200000000000120082, 17.30000000000000071 ) ) ;
#29809=ORIENTED_EDGE ( 'NONE', *, *, #31690, .F. ) ;
#29810=LINE ( 'NONE', #19549, #22023 ) ;
#29817=VERTEX_POINT ( 'NONE', #22483 ) ;
#29819=VERTEX_POINT ( 'NONE', #59945 ) ;
#29820=LINE ( 'NONE', #60945, #47510 ) ;
#29824=DIRECTION ( 'NONE',  ( 0.000000000000000000, 0.7071067811865495711, -0.7071067811865455743 ) ) ;
#29827=DIRECTION ( 'NONE',  ( 0.000000000000000000, -1.000000000000000000, 0.000000000000000000 ) ) ;
#29828=CIRCLE ( 'NONE', #63721, 2.250000000000001776 ) ;
#29845=EDGE_CURVE ( 'NONE', #29817, #50067, #65933, .T. ) ;
#29847=LINE ( 'NONE', #51420, #15388 ) ;
#29852=DIRECTION ( 'NONE',  ( 0.000000000000000000, 1.000000000000000000, 0.000000000000000000 ) ) ;
#29856=AXIS2_PLACEMENT_3D ( 'NONE', #63428, #20629, #20981 ) ;
#29858=( LENGTH_UNIT ( ) NAMED_UNIT ( * ) SI_UNIT ( .MILLI., .METRE. ) );
#29863=EDGE_LOOP ( 'NONE', ( #53760, #478, #58173, #58731, #20988, #54093 ) ) ;
#29865=PLANE ( 'NONE',  #68165 ) ;
#29870=VERTEX_POINT ( 'NONE', #65604 ) ;
#29887=DIRECTION ( 'NONE',  ( 1.000000000000000000, -0.000000000000000000, -0.000000000000000000 ) ) ;
#29890=VERTEX_POINT ( 'NONE', #23507 ) ;
#29903=ORIENTED_EDGE ( 'NONE', *, *, #12770, .T. ) ;
#29904=AXIS2_PLACEMENT_3D ( 'NONE', #64857, #37639, #32672 ) ;
#29924=DIRECTION ( 'NONE',  ( 0.000000000000000000, 1.000000000000000000, 0.000000000000000000 ) ) ;
#29944=DIRECTION ( 'NONE',  ( 0.000000000000000000, 0.000000000000000000, 1.000000000000000000 ) ) ;
#29950=VECTOR ( 'NONE', #45694, 1000.000000000000000 ) ;
#29956=DIRECTION ( 'NONE',  ( 0.000000000000000000, 0.000000000000000000, -1.000000000000000000 ) ) ;
#29957=DIRECTION ( 'NONE',  ( 0.000000000000000000, 1.000000000000000000, 0.000000000000000000 ) ) ;
#29960=CIRCLE ( 'NONE', #68386, 0.3499999999999295341 ) ;
#29961=AXIS2_PLACEMENT_3D ( 'NONE', #45855, #46550, #56466 ) ;
#29985=CARTESIAN_POINT ( 'NONE',  ( -11.00000000000000000, -10.85999999999999943, -9.000000000000001776 ) ) ;
#29998=DIRECTION ( 'NONE',  ( 0.000000000000000000, -0.1111111111108840643, -0.9938079899999319178 ) ) ;
#30001=AXIS2_PLACEMENT_3D ( 'NONE', #38720, #11837, #59254 ) ;
#30002=ORIENTED_EDGE ( 'NONE', *, *, #31690, .T. ) ;
#30004=CIRCLE ( 'NONE', #66085, 3.300000002979700753 ) ;
#30009=DIRECTION ( 'NONE',  ( 0.000000000000000000, 0.000000000000000000, -1.000000000000000000 ) ) ;
#30010=ORIENTED_EDGE ( 'NONE', *, *, #29292, .F. ) ;
#30012=VECTOR ( 'NONE', #16361, 1000.000000000000000 ) ;
#30015=DIRECTION ( 'NONE',  ( -1.000000000000000000, 0.000000000000000000, 0.000000000000000000 ) ) ;
#30020=CIRCLE ( 'NONE', #60507, 4.000000000000000888 ) ;
#30026=CARTESIAN_POINT ( 'NONE',  ( 11.00000000000000000, -11.70000000000000284, 12.50000000000000000 ) ) ;
#30033=VERTEX_POINT ( 'NONE', #61677 ) ;
#30036=ADVANCED_FACE ( 'NONE', ( #13241 ), #13904, .T. ) ;
#30044=ORIENTED_EDGE ( 'NONE', *, *, #6622, .F. ) ;
#30049=DIRECTION ( 'NONE',  ( -0.000000000000000000, 1.000000000000000000, -0.000000000000000000 ) ) ;
#30059=AXIS2_PLACEMENT_3D ( 'NONE', #31176, #10293, #15947 ) ;
#30072=CARTESIAN_POINT ( 'NONE',  ( 25.50000000000000355, 0.000000000000000000, -24.75000000000000000 ) ) ;
#30079=FACE_OUTER_BOUND ( 'NONE', #34581, .T. ) ;
#30080=ORIENTED_EDGE ( 'NONE', *, *, #69942, .F. ) ;
#30093=ORIENTED_EDGE ( 'NONE', *, *, #45983, .T. ) ;
#30094=ORIENTED_EDGE ( 'NONE', *, *, #39432, .F. ) ;
#30105=DIRECTION ( 'NONE',  ( -1.000000000000000000, 0.000000000000000000, 0.000000000000000000 ) ) ;
#30125=VECTOR ( 'NONE', #60114, 1000.000000000000000 ) ;
#30126=AXIS2_PLACEMENT_3D ( 'NONE', #24954, #30959, #8691 ) ;
#30131=FACE_OUTER_BOUND ( 'NONE', #23781, .T. ) ;
#30136=EDGE_CURVE ( 'NONE', #23076, #8233, #28685, .T. ) ;
#30141=DIRECTION ( 'NONE',  ( 0.000000000000000000, -0.7046037717859411353, -0.7096009616573427659 ) ) ;
#30142=ORIENTED_EDGE ( 'NONE', *, *, #55349, .F. ) ;
#30144=DIRECTION ( 'NONE',  ( 0.000000000000000000, 0.7071067811865450192, 0.7071067811865500152 ) ) ;
#30146=CARTESIAN_POINT ( 'NONE',  ( -15.50000000000129852, -15.50000000000000000, 22.50000000000000000 ) ) ;
#30151=DIRECTION ( 'NONE',  ( -1.000000000000000000, 0.000000000000000000, 0.000000000000000000 ) ) ;
#30162=ORIENTED_EDGE ( 'NONE', *, *, #23879, .F. ) ;
#30165=ADVANCED_FACE ( 'NONE', ( #61196 ), #64740, .F. ) ;
#30168=CIRCLE ( 'NONE', #66302, 3.299999999999473577 ) ;
#30174=AXIS2_PLACEMENT_3D ( 'NONE', #57055, #61659, #40078 ) ;
#30176=ORIENTED_EDGE ( 'NONE', *, *, #48478, .T. ) ;
#30197=ORIENTED_EDGE ( 'NONE', *, *, #28837, .F. ) ;
#30203=EDGE_CURVE ( 'NONE', #54664, #10280, #68543, .T. ) ;
#30205=CARTESIAN_POINT ( 'NONE',  ( -29.25000000000000000, -5.200000000000001066, 60.00000000000000000 ) ) ;
#30213=CIRCLE ( 'NONE', #1984, 1.620999999999997332 ) ;
#30215=CARTESIAN_POINT ( 'NONE',  ( 29.50000000000000355, -11.50000000000100009, -15.00000000000084910 ) ) ;
#30216=EDGE_CURVE ( 'NONE', #65652, #36958, #5388, .T. ) ;
#30220=VECTOR ( 'NONE', #20797, 1000.000000000000000 ) ;
#30223=( NAMED_UNIT ( * ) SI_UNIT ( $, .STERADIAN. ) SOLID_ANGLE_UNIT ( ) );
#30224=EDGE_CURVE ( 'NONE', #4508, #22980, #25219, .T. ) ;
#30227=AXIS2_PLACEMENT_3D ( 'NONE', #3977, #31558, #25902 ) ;
#30237=DIRECTION ( 'NONE',  ( 0.000000000000000000, 0.000000000000000000, -1.000000000000000000 ) ) ;
#30238=VERTEX_POINT ( 'NONE', #51925 ) ;
#30239=CARTESIAN_POINT ( 'NONE',  ( 11.00000000000000000, -5.599999999999999645, -27.00000000000000000 ) ) ;
#30243=FACE_OUTER_BOUND ( 'NONE', #8305, .T. ) ;
#30248=FACE_OUTER_BOUND ( 'NONE', #62175, .T. ) ;
#30250=DIRECTION ( 'NONE',  ( 0.000000000000000000, 0.000000000000000000, 1.000000000000000000 ) ) ;
#30251=ORIENTED_EDGE ( 'NONE', *, *, #52118, .F. ) ;
#30258=CARTESIAN_POINT ( 'NONE',  ( -16.89194109070750116, -5.000000000000000000, -26.25000000000000000 ) ) ;
#30260=CARTESIAN_POINT ( 'NONE',  ( -28.00000000000000000, -16.28999999999710369, 15.00000000000794920 ) ) ;
#30261=DIRECTION ( 'NONE',  ( 0.000000000000000000, 0.000000000000000000, 1.000000000000000000 ) ) ;
#30266=FACE_OUTER_BOUND ( 'NONE', #23218, .T. ) ;
#30270=ORIENTED_EDGE ( 'NONE', *, *, #55188, .F. ) ;
#30276=CARTESIAN_POINT ( 'NONE',  ( 29.50000000000000355, -11.50000000000000000, 11.00000000000000000 ) ) ;
#30277=ORIENTED_EDGE ( 'NONE', *, *, #30964, .T. ) ;
#30279=DIRECTION ( 'NONE',  ( 0.000000000000000000, 0.000000000000000000, 1.000000000000000000 ) ) ;
#30286=DIRECTION ( 'NONE',  ( 0.000000000000000000, 1.000000000000000000, 0.000000000000000000 ) ) ;
#30289=AXIS2_PLACEMENT_3D ( 'NONE', #851, #11090, #53894 ) ;
#30292=FACE_OUTER_BOUND ( 'NONE', #19608, .T. ) ;
#30311=CARTESIAN_POINT ( 'NONE',  ( -11.00000000000000000, -14.04000000000000092, -14.80000000000000071 ) ) ;
#30322=ORIENTED_EDGE ( 'NONE', *, *, #18362, .F. ) ;
#30323=CARTESIAN_POINT ( 'NONE',  ( 23.48000000000000043, -17.50000000000000000, -26.00000000000000355 ) ) ;
#30324=CARTESIAN_POINT ( 'NONE',  ( 30.00000000000000000, -12.00000000000000000, -11.00000000000000000 ) ) ;
#30326=FACE_OUTER_BOUND ( 'NONE', #61033, .T. ) ;
#30347=EDGE_LOOP ( 'NONE', ( #43584, #30197 ) ) ;
#30350=ADVANCED_FACE ( 'NONE', ( #44417 ), #5923, .F. ) ;
#30357=DIRECTION ( 'NONE',  ( 0.000000000000000000, 1.000000000000000000, 0.000000000000000000 ) ) ;
#30363=ORIENTED_EDGE ( 'NONE', *, *, #34277, .F. ) ;
#30369=AXIS2_PLACEMENT_3D ( 'NONE', #40330, #18054, #45617 ) ;
#30373=ORIENTED_EDGE ( 'NONE', *, *, #9017, .F. ) ;
#30375=ORIENTED_EDGE ( 'NONE', *, *, #21200, .F. ) ;
#30391=EDGE_CURVE ( 'NONE', #2217, #8225, #27484, .T. ) ;
#30392=DIRECTION ( 'NONE',  ( 0.000000000000000000, -0.7071067811865455743, -0.7071067811865495711 ) ) ;
#30396=AXIS2_PLACEMENT_3D ( 'NONE', #47423, #46720, #14199 ) ;
#30407=LINE ( 'NONE', #19441, #3272 ) ;
#30419=ORIENTED_EDGE ( 'NONE', *, *, #27499, .F. ) ;
#30428=CIRCLE ( 'NONE', #66557, 3.499999999999849454 ) ;
#30435=EDGE_LOOP ( 'NONE', ( #23991, #55441, #18052, #8109 ) ) ;
#30436=ORIENTED_EDGE ( 'NONE', *, *, #62437, .F. ) ;
#30446=AXIS2_PLACEMENT_3D ( 'NONE', #8056, #45898, #67487 ) ;
#30450=ORIENTED_EDGE ( 'NONE', *, *, #49994, .F. ) ;
#30452=DIRECTION ( 'NONE',  ( 0.000000000000000000, 0.000000000000000000, 1.000000000000000000 ) ) ;
#30470=DIRECTION ( 'NONE',  ( 1.000000000000000000, 0.000000000000000000, 0.000000000000000000 ) ) ;
#30471=VECTOR ( 'NONE', #45157, 1000.000000000000000 ) ;
#30475=AXIS2_PLACEMENT_3D ( 'NONE', #3427, #31711, #53623 ) ;
#30479=EDGE_CURVE ( 'NONE', #44054, #7139, #17600, .T. ) ;
#30481=CIRCLE ( 'NONE', #54173, 4.500000000000191847 ) ;
#30484=CARTESIAN_POINT ( 'NONE',  ( 13.00000000000000178, -17.35230188589299871, -15.35019951917099945 ) ) ;
#30485=EDGE_LOOP ( 'NONE', ( #30093, #28170, #39814, #48251 ) ) ;
#30486=CARTESIAN_POINT ( 'NONE',  ( -16.89194109070750471, -5.000000000000000000, 26.25000000000000000 ) ) ;
#30491=CARTESIAN_POINT ( 'NONE',  ( 11.50000000000000000, -11.50000000000100009, 15.00000000000084910 ) ) ;
#30493=CARTESIAN_POINT ( 'NONE',  ( -11.00000000000000000, -5.599999999999999645, 9.000000000000001776 ) ) ;
#30495=EDGE_CURVE ( 'NONE', #7103, #37166, #54410, .T. ) ;
#30507=CARTESIAN_POINT ( 'NONE',  ( 11.00000000000000000, -13.54524521594299991, -17.53999999999999915 ) ) ;
#30514=CARTESIAN_POINT ( 'NONE',  ( -15.50000000000000000, -1.037157890325000054, 22.50000000000000000 ) ) ;
#30536=EDGE_CURVE ( 'NONE', #9391, #29478, #13789, .T. ) ;
#30537=CIRCLE ( 'NONE', #51992, 0.2999999999998732569 ) ;
#30540=EDGE_CURVE ( 'NONE', #45920, #57327, #22233, .T. ) ;
#30541=ORIENTED_EDGE ( 'NONE', *, *, #22177, .T. ) ;
#30542=CARTESIAN_POINT ( 'NONE',  ( -30.00000000000000000, -5.599999999999999645, -9.000000000000001776 ) ) ;
#30543=DIRECTION ( 'NONE',  ( 0.000000000000000000, 0.000000000000000000, -1.000000000000000000 ) ) ;
#30545=CARTESIAN_POINT ( 'NONE',  ( -13.00000000000000178, -15.50000000000000000, 20.05051025721700242 ) ) ;
#30547=ORIENTED_EDGE ( 'NONE', *, *, #64485, .F. ) ;
#30551=CYLINDRICAL_SURFACE ( 'NONE', #19347, 4.500000000000189182 ) ;
#30560=FACE_OUTER_BOUND ( 'NONE', #51445, .T. ) ;
#30561=DIRECTION ( 'NONE',  ( 0.000000000000000000, 1.000000000000000000, 0.000000000000000000 ) ) ;
#30570=CARTESIAN_POINT ( 'NONE',  ( -25.50000000000000355, -15.50000000000000000, 24.50000000000000000 ) ) ;
#30574=CARTESIAN_POINT ( 'NONE',  ( -14.24999999999999822, -0.2715193793361453389, 22.98718409945082541 ) ) ;
#30577=VERTEX_POINT ( 'NONE', #22907 ) ;
#30590=DIRECTION ( 'NONE',  ( 1.000000000000000000, 0.000000000000000000, 0.000000000000000000 ) ) ;
#30593=EDGE_CURVE ( 'NONE', #58343, #64845, #1676, .T. ) ;
#30596=EDGE_LOOP ( 'NONE', ( #42762, #50145, #22955, #68893 ) ) ;
#30597=ORIENTED_EDGE ( 'NONE', *, *, #21496, .F. ) ;
#30624=ORIENTED_EDGE ( 'NONE', *, *, #29118, .T. ) ;
#30626=VERTEX_POINT ( 'NONE', #28897 ) ;
#30637=CARTESIAN_POINT ( 'NONE',  ( 29.50000000000000355, -11.50000000000100009, 15.00000000000084910 ) ) ;
#30649=EDGE_CURVE ( 'NONE', #48624, #33817, #18633, .T. ) ;
#30654=EDGE_CURVE ( 'NONE', #35302, #48024, #24088, .T. ) ;
#30659=EDGE_CURVE ( 'NONE', #64180, #22939, #36518, .T. ) ;
#30677=CARTESIAN_POINT ( 'NONE',  ( 29.50000000000000355, -12.00000000000000000, -11.00000000000000000 ) ) ;
#30681=AXIS2_PLACEMENT_3D ( 'NONE', #36683, #48340, #47987 ) ;
#30682=EDGE_CURVE ( 'NONE', #37044, #11521, #13686, .T. ) ;
#30684=AXIS2_PLACEMENT_3D ( 'NONE', #30763, #62225, #13786 ) ;
#30686=VERTEX_POINT ( 'NONE', #66726 ) ;
#30693=FACE_OUTER_BOUND ( 'NONE', #8704, .T. ) ;
#30707=CARTESIAN_POINT ( 'NONE',  ( 16.75000000000000000, -0.2038245569916320166, -21.77831216351300014 ) ) ;
#30720=AXIS2_PLACEMENT_3D ( 'NONE', #55166, #44888, #67151 ) ;
#30730=CARTESIAN_POINT ( 'NONE',  ( -11.75000000000000000, -5.000000000000000000, -11.75000000000000000 ) ) ;
#30743=DIRECTION ( 'NONE',  ( -0.000000000000000000, 1.000000000000000000, -0.000000000000000000 ) ) ;
#30745=AXIS2_PLACEMENT_3D ( 'NONE', #44809, #39503, #34189 ) ;
#30752=ORIENTED_EDGE ( 'NONE', *, *, #6506, .T. ) ;
#30756=EDGE_CURVE ( 'NONE', #14841, #28718, #21690, .T. ) ;
#30757=EDGE_CURVE ( 'NONE', #55302, #63213, #66877, .T. ) ;
#30758=CARTESIAN_POINT ( 'NONE',  ( 30.00000000000000000, -11.70000000000000284, 12.50000000000000000 ) ) ;
#30761=CARTESIAN_POINT ( 'NONE',  ( 11.00000000000000000, -11.50000000000000000, -15.00000000000000000 ) ) ;
#30763=CARTESIAN_POINT ( 'NONE',  ( 25.50000000000000355, -5.200000000000001066, 22.50000000000000000 ) ) ;
#30774=ORIENTED_EDGE ( 'NONE', *, *, #18587, .F. ) ;
#30777=CARTESIAN_POINT ( 'NONE',  ( -16.33757311576526305, -0.3152598339554808504, -21.54019739087904384 ) ) ;
#30783=ORIENTED_EDGE ( 'NONE', *, *, #67403, .F. ) ;
#30785=ORIENTED_EDGE ( 'NONE', *, *, #1284, .F. ) ;
#30786=VERTEX_POINT ( 'NONE', #5190 ) ;
#30792=VERTEX_POINT ( 'NONE', #26404 ) ;
#30796=DIRECTION ( 'NONE',  ( 0.000000000000000000, 0.000000000000000000, -1.000000000000000000 ) ) ;
#30809=LINE ( 'NONE', #14193, #16323 ) ;
#30819=PLANE ( 'NONE',  #27730 ) ;
#30823=B_SPLINE_CURVE_WITH_KNOTS ( 'NONE', 3,
 ( #62744, #30574, #31985, #9358, #25635, #21011 ),
 .UNSPECIFIED., .F., .F.,
 ( 4, 2, 4 ),
 ( 1.820537833122031213, 2.555393473688635453, 3.290249114255239693 ),
 .UNSPECIFIED. ) ;
#30826=CARTESIAN_POINT ( 'NONE',  ( -18.85410196625000268, -15.50000000000000000, 21.50000000000000000 ) ) ;
#30827=VERTEX_POINT ( 'NONE', #52585 ) ;
#30828=CARTESIAN_POINT ( 'NONE',  ( -16.75000000000000355, -0.2715193793361416197, 22.01281590054916748 ) ) ;
#30830=CARTESIAN_POINT ( 'NONE',  ( -11.00000000000000000, -5.200000000000001066, 26.59999999999999787 ) ) ;
#30839=ORIENTED_EDGE ( 'NONE', *, *, #1483, .F. ) ;
#30846=DIRECTION ( 'NONE',  ( 1.000000000000000000, -0.000000000000000000, -0.000000000000000000 ) ) ;
#30855=EDGE_LOOP ( 'NONE', ( #19135, #17814, #49750, #65865 ) ) ;
#30857=VECTOR ( 'NONE', #21590, 1000.000000000000000 ) ;
#30858=CARTESIAN_POINT ( 'NONE',  ( -29.50000000000000355, -12.00000000000000000, 11.00000000000000000 ) ) ;
#30866=ORIENTED_EDGE ( 'NONE', *, *, #5944, .T. ) ;
#30869=DIRECTION ( 'NONE',  ( 0.000000000000000000, 0.5000000000000189848, 0.8660254037844277164 ) ) ;
#30876=ORIENTED_EDGE ( 'NONE', *, *, #19809, .F. ) ;
#30877=VECTOR ( 'NONE', #1722, 1000.000000000000114 ) ;
#30887=CARTESIAN_POINT ( 'NONE',  ( -17.00000000000000000, -17.50000000000000000, -19.33772233983200195 ) ) ;
#30892=VECTOR ( 'NONE', #10859, 1000.000000000000000 ) ;
#30898=EDGE_LOOP ( 'NONE', ( #61348, #67285, #599, #47377 ) ) ;
#30899=CARTESIAN_POINT ( 'NONE',  ( -28.00000000000000000, -16.64230188589299786, 14.64519951917100116 ) ) ;
#30901=VECTOR ( 'NONE', #12076, 1000.000000000000000 ) ;
#30902=CARTESIAN_POINT ( 'NONE',  ( -17.00000000000000000, -15.50000000000000000, -14.50000000000000000 ) ) ;
#30907=VERTEX_POINT ( 'NONE', #37031 ) ;
#30913=CYLINDRICAL_SURFACE ( 'NONE', #26117, 4.500000000000188294 ) ;
#30917=DIRECTION ( 'NONE',  ( 0.000000000000000000, 0.000000000000000000, 1.000000000000000000 ) ) ;
#30918=EDGE_CURVE ( 'NONE', #68236, #14490, #53634, .T. ) ;
#30921=ORIENTED_EDGE ( 'NONE', *, *, #22855, .T. ) ;
#30924=EDGE_CURVE ( 'NONE', #41126, #14914, #49017, .T. ) ;
#30928=ORIENTED_EDGE ( 'NONE', *, *, #56521, .T. ) ;
#30934=CARTESIAN_POINT ( 'NONE',  ( 15.50000000000000000, -5.000000000000000000, -26.50000000000000000 ) ) ;
#30936=EDGE_CURVE ( 'NONE', #26720, #13935, #54326, .T. ) ;
#30942=VECTOR ( 'NONE', #9386, 1000.000000000000000 ) ;
#30943=CARTESIAN_POINT ( 'NONE',  ( 13.00000000000000178, -15.50000000000000000, -14.50000000000000000 ) ) ;
#30944=CARTESIAN_POINT ( 'NONE',  ( 13.00000000000000178, -15.50000000000000000, -14.50000000000000000 ) ) ;
#30951=AXIS2_PLACEMENT_3D ( 'NONE', #24852, #46758, #68337 ) ;
#30959=DIRECTION ( 'NONE',  ( 0.000000000000000000, 0.000000000000000000, -1.000000000000000000 ) ) ;
#30961=DIRECTION ( 'NONE',  ( 1.000000000000000000, -0.000000000000000000, -0.000000000000000000 ) ) ;
#30962=VERTEX_POINT ( 'NONE', #43712 ) ;
#30964=EDGE_CURVE ( 'NONE', #47223, #11065, #55590, .T. ) ;
#30976=VERTEX_POINT ( 'NONE', #5535 ) ;
#30985=DIRECTION ( 'NONE',  ( 0.000000000000000000, 0.000000000000000000, 1.000000000000000000 ) ) ;
#30990=FACE_OUTER_BOUND ( 'NONE', #337, .T. ) ;
#30991=AXIS2_PLACEMENT_3D ( 'NONE', #28040, #7140, #49601 ) ;
#30992=CARTESIAN_POINT ( 'NONE',  ( -22.14589803375000088, -15.50000000000000000, -21.50000000000000000 ) ) ;
#30997=CARTESIAN_POINT ( 'NONE',  ( 16.75000000000000000, -2.500000000000000000, -21.77831216351300014 ) ) ;
#30998=LINE ( 'NONE', #21433, #66649 ) ;
#31001=ADVANCED_FACE ( 'NONE', ( #16835 ), #64934, .F. ) ;
#31007=VERTEX_POINT ( 'NONE', #38740 ) ;
#31021=CARTESIAN_POINT ( 'NONE',  ( -24.00000000000000000, -15.50000000000000000, 14.50000000000000000 ) ) ;
#31024=DIRECTION ( 'NONE',  ( 0.000000000000000000, 1.000000000000000000, 0.000000000000000000 ) ) ;
#31027=VECTOR ( 'NONE', #37374, 1000.000000000000000 ) ;
#31029=DIRECTION ( 'NONE',  ( -1.000000000000000000, 0.000000000000000000, 0.000000000000000000 ) ) ;
#31031=ORIENTED_EDGE ( 'NONE', *, *, #67640, .F. ) ;
#31037=VECTOR ( 'NONE', #55520, 1000.000000000000000 ) ;
#31041=EDGE_LOOP ( 'NONE', ( #25414, #7687, #18474, #15047, #57394, #37066 ) ) ;
#31042=CARTESIAN_POINT ( 'NONE',  ( -11.00000000000000000, -12.00000000000000000, 12.20000000000000107 ) ) ;
#31046=ORIENTED_EDGE ( 'NONE', *, *, #63085, .F. ) ;
#31055=ADVANCED_FACE ( 'NONE', ( #23170 ), #13259, .F. ) ;
#31061=ADVANCED_FACE ( 'NONE', ( #34458 ), #29167, .F. ) ;
#31065=ORIENTED_EDGE ( 'NONE', *, *, #21595, .T. ) ;
#31066=DIRECTION ( 'NONE',  ( 0.000000000000000000, 0.000000000000000000, -1.000000000000000000 ) ) ;
#31069=DIRECTION ( 'NONE',  ( 0.000000000000000000, 0.000000000000000000, -1.000000000000000000 ) ) ;
#31073=CARTESIAN_POINT ( 'NONE',  ( 30.00000000000000000, -17.50000000000000000, -26.64999999999999858 ) ) ;
#31090=ORIENTED_EDGE ( 'NONE', *, *, #50026, .T. ) ;
#31096=ORIENTED_EDGE ( 'NONE', *, *, #30757, .F. ) ;
#31099=VECTOR ( 'NONE', #4714, 1000.000000000000000 ) ;
#31106=VECTOR ( 'NONE', #25923, 1000.000000000000000 ) ;
#31117=CARTESIAN_POINT ( 'NONE',  ( 30.00000000000000000, -13.79999999999979998, 17.30000000000000071 ) ) ;
#31125=AXIS2_PLACEMENT_3D ( 'NONE', #31536, #24818, #41771 ) ;
#31127=EDGE_CURVE ( 'NONE', #46765, #55302, #18211, .T. ) ;
#31129=DIRECTION ( 'NONE',  ( 0.000000000000000000, -0.9938079899998859545, 0.1111111111112941946 ) ) ;
#31132=CARTESIAN_POINT ( 'NONE',  ( -30.00000000000000000, -17.50000000000000000, -26.64999999999999858 ) ) ;
#31139=ORIENTED_EDGE ( 'NONE', *, *, #52564, .T. ) ;
#31141=DIRECTION ( 'NONE',  ( 0.000000000000000000, 1.000000000000000000, 0.000000000000000000 ) ) ;
#31156=ORIENTED_EDGE ( 'NONE', *, *, #10361, .T. ) ;
#31170=ORIENTED_EDGE ( 'NONE', *, *, #8079, .T. ) ;
#31176=CARTESIAN_POINT ( 'NONE',  ( -19.00000000000000000, -5.000000000000000000, 22.50000000000000000 ) ) ;
#31181=DIRECTION ( 'NONE',  ( 0.000000000000000000, 0.000000000000000000, -1.000000000000000000 ) ) ;
#31194=AXIS2_PLACEMENT_3D ( 'NONE', #30324, #19693, #68857 ) ;
#31202=ADVANCED_FACE ( 'NONE', ( #52869 ), #19607, .T. ) ;
#31203=ADVANCED_FACE ( 'NONE', ( #63104 ), #63808, .F. ) ;
#31204=VECTOR ( 'NONE', #54914, 1000.000000000000000 ) ;
#31206=VECTOR ( 'NONE', #39899, 1000.000000000000114 ) ;
#31211=EDGE_CURVE ( 'NONE', #57411, #33481, #53439, .T. ) ;
#31219=AXIS2_PLACEMENT_3D ( 'NONE', #38707, #50004, #16455 ) ;
#31220=DIRECTION ( 'NONE',  ( 0.000000000000000000, 1.000000000000000000, 0.000000000000000000 ) ) ;
#31221=DIRECTION ( 'NONE',  ( 1.000000000000000000, 0.000000000000000000, 0.000000000000000000 ) ) ;
#31231=LINE ( 'NONE', #52803, #31106 ) ;
#31233=PLANE ( 'NONE',  #21052 ) ;
#31237=DIRECTION ( 'NONE',  ( 0.000000000000000000, -0.9921567416492215186, 0.1249999999999996531 ) ) ;
#31242=ORIENTED_EDGE ( 'NONE', *, *, #37969, .F. ) ;
#31243=AXIS2_PLACEMENT_3D ( 'NONE', #18811, #40384, #61941 ) ;
#31255=CIRCLE ( 'NONE', #53866, 1.620999999999997332 ) ;
#31291=CARTESIAN_POINT ( 'NONE',  ( -11.00000000000000000, -8.959999999999999076, -17.04524521594300523 ) ) ;
#31292=ORIENTED_EDGE ( 'NONE', *, *, #55251, .T. ) ;
#31295=DIRECTION ( 'NONE',  ( 0.000000000000000000, -0.9938079899998859545, 0.1111111111112941946 ) ) ;
#31296=EDGE_CURVE ( 'NONE', #30686, #373, #5107, .T. ) ;
#31304=DIRECTION ( 'NONE',  ( 1.000000000000000000, -0.000000000000000000, -0.000000000000000000 ) ) ;
#31311=CARTESIAN_POINT ( 'NONE',  ( 30.00000000000000000, -14.04000000000000092, -14.80000000000000071 ) ) ;
#31324=ORIENTED_EDGE ( 'NONE', *, *, #13542, .F. ) ;
#31346=DIRECTION ( 'NONE',  ( 0.000000000000000000, -1.000000000000000000, 0.000000000000000000 ) ) ;
#31350=ORIENTED_EDGE ( 'NONE', *, *, #33638, .F. ) ;
#31353=AXIS2_PLACEMENT_3D ( 'NONE', #12678, #46268, #7732 ) ;
#31357=AXIS2_PLACEMENT_3D ( 'NONE', #76, #21636, #16326 ) ;
#31361=DIRECTION ( 'NONE',  ( -0.000000000000000000, 1.000000000000000000, -0.000000000000000000 ) ) ;
#31362=CARTESIAN_POINT ( 'NONE',  ( -18.85410196625000268, -15.50000000000000000, -21.50000000000000000 ) ) ;
#31371=ORIENTED_EDGE ( 'NONE', *, *, #22449, .F. ) ;
#31372=FACE_OUTER_BOUND ( 'NONE', #51030, .T. ) ;
#31373=CARTESIAN_POINT ( 'NONE',  ( -25.50000000000000355, -15.12100000000000044, 22.50000000000000000 ) ) ;
#31376=ORIENTED_EDGE ( 'NONE', *, *, #46039, .T. ) ;
#31384=CARTESIAN_POINT ( 'NONE',  ( -17.51999999999999957, -17.50000000000000000, 26.00000000000000355 ) ) ;
#31389=CARTESIAN_POINT ( 'NONE',  ( -25.50000000000000355, 0.000000000000000000, -22.50000000000000000 ) ) ;
#31401=ORIENTED_EDGE ( 'NONE', *, *, #28645, .T. ) ;
#31410=VECTOR ( 'NONE', #23071, 1000.000000000000000 ) ;
#31411=CONICAL_SURFACE ( 'NONE', #55120, 1732.050807568785558, 1.047197551196574761 ) ;
#31418=ORIENTED_EDGE ( 'NONE', *, *, #60866, .F. ) ;
#31422=EDGE_CURVE ( 'NONE', #43603, #46652, #498, .T. ) ;
#31432=EDGE_LOOP ( 'NONE', ( #40951, #69458, #27699, #51051 ) ) ;
#31434=CARTESIAN_POINT ( 'NONE',  ( -15.29633693294650421, -0.2717122460102769921, -23.82579074638668715 ) ) ;
#31440=CARTESIAN_POINT ( 'NONE',  ( 14.25000000000000000, -0.2038245569916330158, 21.77831216351300014 ) ) ;
#31441=LINE ( 'NONE', #14097, #52758 ) ;
#31444=ORIENTED_EDGE ( 'NONE', *, *, #18587, .T. ) ;
#31447=CARTESIAN_POINT ( 'NONE',  ( 13.00000000000000178, -15.50000000000000000, 20.05051025721700242 ) ) ;
#31450=CARTESIAN_POINT ( 'NONE',  ( -25.50000000000000355, -5.200000000000001066, 24.75000000000000000 ) ) ;
#31469=CARTESIAN_POINT ( 'NONE',  ( -17.00000000000000000, -16.64230188589299786, 14.64519951917100116 ) ) ;
#31482=CARTESIAN_POINT ( 'NONE',  ( -11.00000000000000000, -17.00000000000000000, 15.70499999999969809 ) ) ;
#31485=DIRECTION ( 'NONE',  ( 0.000000000000000000, 0.000000000000000000, -1.000000000000000000 ) ) ;
#31489=CARTESIAN_POINT ( 'NONE',  ( 30.00000000000000000, -9.199999999999999289, -12.34999999999989839 ) ) ;
#31497=CARTESIAN_POINT ( 'NONE',  ( 30.00000000000000000, -5.599999999999999645, -9.400000000000000355 ) ) ;
#31504=FACE_OUTER_BOUND ( 'NONE', #39980, .T. ) ;
#31510=DIRECTION ( 'NONE',  ( -1.000000000000000000, 0.000000000000000000, 0.000000000000000000 ) ) ;
#31513=AXIS2_PLACEMENT_3D ( 'NONE', #1436, #24041, #34654 ) ;
#31519=VECTOR ( 'NONE', #12967, 1000.000000000000000 ) ;
#31536=CARTESIAN_POINT ( 'NONE',  ( 30.00000000000000000, -5.000000000000000000, 27.00000000000000000 ) ) ;
#31538=DIRECTION ( 'NONE',  ( 0.000000000000000000, 0.000000000000000000, 1.000000000000000000 ) ) ;
#31546=ADVANCED_FACE ( 'NONE', ( #13525, #33700, #7522, #67276, #12469, #17789, #66574, #56661, #50311 ), #35081, .T. ) ;
#31549=AXIS2_PLACEMENT_3D ( 'NONE', #47126, #43202, #20245 ) ;
#31557=CIRCLE ( 'NONE', #24723, 0.3999999999993835154 ) ;
#31558=DIRECTION ( 'NONE',  ( -1.000000000000000000, 0.000000000000000000, 0.000000000000000000 ) ) ;
#31559=CARTESIAN_POINT ( 'NONE',  ( -28.00000000000000000, -16.28999999999710369, 14.50000000000000000 ) ) ;
#31562=EDGE_CURVE ( 'NONE', #58992, #61956, #9278, .T. ) ;
#31566=PLANE ( 'NONE',  #170 ) ;
#31582=ADVANCED_FACE ( 'NONE', ( #36868 ), #62308, .F. ) ;
#31583=CARTESIAN_POINT ( 'NONE',  ( -25.50000000000000355, 0.000000000000000000, -22.50000000000000000 ) ) ;
#31584=FACE_OUTER_BOUND ( 'NONE', #61108, .T. ) ;
#31590=ORIENTED_EDGE ( 'NONE', *, *, #62041, .F. ) ;
#31591=ORIENTED_EDGE ( 'NONE', *, *, #2909, .T. ) ;
#31593=ORIENTED_EDGE ( 'NONE', *, *, #17318, .T. ) ;
#31598=ADVANCED_FACE ( 'NONE', ( #51719 ), #63731, .T. ) ;
#31601=AXIS2_PLACEMENT_3D ( 'NONE', #53644, #59285, #26076 ) ;
#31602=ORIENTED_EDGE ( 'NONE', *, *, #10473, .T. ) ;
#31606=CARTESIAN_POINT ( 'NONE',  ( 15.50000000000000000, -5.000000000000000000, -22.50000000000000000 ) ) ;
#31607=LINE ( 'NONE', #69425, #62796 ) ;
#31608=ORIENTED_EDGE ( 'NONE', *, *, #56139, .F. ) ;
#31610=VECTOR ( 'NONE', #27953, 1000.000000000000114 ) ;
#31613=DIRECTION ( 'NONE',  ( 0.000000000000000000, 1.000000000000000000, 0.000000000000000000 ) ) ;
#31623=DIRECTION ( 'NONE',  ( 0.000000000000000000, 0.000000000000000000, 1.000000000000000000 ) ) ;
#31624=FACE_OUTER_BOUND ( 'NONE', #65839, .T. ) ;
#31626=CARTESIAN_POINT ( 'NONE',  ( -16.75000000000000000, -2.500000000000000000, 23.22168783648699986 ) ) ;
#31628=LINE ( 'NONE', #68754, #33640 ) ;
#31636=CARTESIAN_POINT ( 'NONE',  ( 29.50000000000000355, -11.50000000000100009, -15.00000000000084910 ) ) ;
#31645=CYLINDRICAL_SURFACE ( 'NONE', #5252, 0.3499999999998886224 ) ;
#31649=ORIENTED_EDGE ( 'NONE', *, *, #37894, .F. ) ;
#31652=ORIENTED_EDGE ( 'NONE', *, *, #60779, .T. ) ;
#31653=VECTOR ( 'NONE', #36693, 1000.000000000000000 ) ;
#31656=DIRECTION ( 'NONE',  ( 0.000000000000000000, -1.000000000000000000, 0.000000000000000000 ) ) ;
#31674=CARTESIAN_POINT ( 'NONE',  ( 15.50000000000000000, -2.500000000000000000, -21.05662432702600029 ) ) ;
#31680=DIRECTION ( 'NONE',  ( 0.000000000000000000, 0.000000000000000000, 1.000000000000000000 ) ) ;
#31684=DIRECTION ( 'NONE',  ( 0.000000000000000000, 0.000000000000000000, 1.000000000000000000 ) ) ;
#31690=EDGE_CURVE ( 'NONE', #60747, #16870, #16688, .T. ) ;
#31694=DIRECTION ( 'NONE',  ( -1.000000000000000000, 0.000000000000000000, 0.000000000000000000 ) ) ;
#31707=VECTOR ( 'NONE', #57881, 1000.000000000000000 ) ;
#31709=ORIENTED_EDGE ( 'NONE', *, *, #6208, .F. ) ;
#31711=DIRECTION ( 'NONE',  ( -1.000000000000000000, 0.000000000000000000, 0.000000000000000000 ) ) ;
#31714=EDGE_CURVE ( 'NONE', #37597, #17477, #22975, .T. ) ;
#31729=EDGE_CURVE ( 'NONE', #50148, #27481, #62479, .T. ) ;
#31737=DIRECTION ( 'NONE',  ( 0.000000000000000000, 1.000000000000000000, 0.000000000000000000 ) ) ;
#31742=ORIENTED_EDGE ( 'NONE', *, *, #68292, .F. ) ;
#31746=CARTESIAN_POINT ( 'NONE',  ( -30.00000000000000000, -9.454754784057099570, -17.53999999999999915 ) ) ;
#31747=CARTESIAN_POINT ( 'NONE',  ( -29.25000000000000000, -5.000000000000000000, 11.75000000000000000 ) ) ;
#31751=VERTEX_POINT ( 'NONE', #6416 ) ;
#31765=EDGE_LOOP ( 'NONE', ( #4130, #58721, #9673, #3610 ) ) ;
#31776=ORIENTED_EDGE ( 'NONE', *, *, #16592, .F. ) ;
#31780=LINE ( 'NONE', #26122, #20421 ) ;
#31782=DIRECTION ( 'NONE',  ( 0.000000000000000000, 1.000000000000000000, 0.000000000000000000 ) ) ;
#31787=ORIENTED_EDGE ( 'NONE', *, *, #46377, .F. ) ;
#31804=CARTESIAN_POINT ( 'NONE',  ( -11.00000000000000000, -10.85999999999999943, -9.350000000000269651 ) ) ;
#31811=AXIS2_PLACEMENT_3D ( 'NONE', #60145, #65804, #49208 ) ;
#31813=LINE ( 'NONE', #59366, #54977 ) ;
#31815=DIRECTION ( 'NONE',  ( -0.7142857142857395036, 0.000000000000000000, -0.6998542122237394469 ) ) ;
#31823=ADVANCED_FACE ( 'NONE', ( #32934 ), #43885, .F. ) ;
#31826=AXIS2_PLACEMENT_3D ( 'NONE', #10396, #66215, #39337 ) ;
#31836=EDGE_LOOP ( 'NONE', ( #48704, #55069, #68630, #43687 ) ) ;
#31837=CARTESIAN_POINT ( 'NONE',  ( 15.29686605390242526, -0.2715358723600077018, -23.82609623451301317 ) ) ;
#31847=VERTEX_POINT ( 'NONE', #32239 ) ;
#31855=CARTESIAN_POINT ( 'NONE',  ( -30.00000000000000000, -14.04000000000000092, -17.04524521594300523 ) ) ;
#31858=VECTOR ( 'NONE', #27538, 1000.000000000000000 ) ;
#31859=VERTEX_POINT ( 'NONE', #5392 ) ;
#31864=AXIS2_PLACEMENT_3D ( 'NONE', #57288, #47378, #31485 ) ;
#31865=LINE ( 'NONE', #65083, #27850 ) ;
#31866=CARTESIAN_POINT ( 'NONE',  ( -11.00000000000000000, -5.599999999999999645, -9.000000000000001776 ) ) ;
#31878=EDGE_CURVE ( 'NONE', #8233, #5332, #33959, .T. ) ;
#31881=CARTESIAN_POINT ( 'NONE',  ( -11.50000000000000000, -11.50000000000100009, 15.00000000000084910 ) ) ;
#31882=DIRECTION ( 'NONE',  ( -1.000000000000000000, 0.000000000000000000, 0.000000000000000000 ) ) ;
#31890=AXIS2_PLACEMENT_3D ( 'NONE', #51877, #61066, #50475 ) ;
#31891=ADVANCED_FACE ( 'NONE', ( #40573 ), #41270, .T. ) ;
#31893=LINE ( 'NONE', #404, #40197 ) ;
#31897=EDGE_LOOP ( 'NONE', ( #5390, #5591, #22944, #44675 ) ) ;
#31899=DIRECTION ( 'NONE',  ( 0.000000000000000000, 0.000000000000000000, 1.000000000000000000 ) ) ;
#31900=VERTEX_POINT ( 'NONE', #55197 ) ;
#31914=ORIENTED_EDGE ( 'NONE', *, *, #19497, .T. ) ;
#31918=VECTOR ( 'NONE', #57175, 1000.000000000000000 ) ;
#31957=ADVANCED_FACE ( 'NONE', ( #12379 ), #6744, .T. ) ;
#31962=CIRCLE ( 'NONE', #38753, 1.620999999999997332 ) ;
#31963=CARTESIAN_POINT ( 'NONE',  ( 16.75000000000000000, -0.2714405302574886547, 22.01253933645462624 ) ) ;
#31973=EDGE_CURVE ( 'NONE', #2132, #32328, #28653, .T. ) ;
#31980=EDGE_CURVE ( 'NONE', #24537, #27925, #37253, .T. ) ;
#31985=CARTESIAN_POINT ( 'NONE',  ( -14.25000000000000000, -0.3156864504677174277, 22.74361999681791247 ) ) ;
#31996=ORIENTED_EDGE ( 'NONE', *, *, #22054, .T. ) ;
#32007=ORIENTED_EDGE ( 'NONE', *, *, #63917, .T. ) ;
#32008=ORIENTED_EDGE ( 'NONE', *, *, #30682, .T. ) ;
#32013=AXIS2_PLACEMENT_3D ( 'NONE', #67198, #2842, #25122 ) ;
#32017=PLANE ( 'NONE',  #2276 ) ;
#32028=ADVANCED_FACE ( 'NONE', ( #25730, #4164 ), #52238, .T. ) ;
#32030=CARTESIAN_POINT ( 'NONE',  ( -14.25000000000000000, -0.2038245569916330158, 21.77831216351300014 ) ) ;
#32031=DIRECTION ( 'NONE',  ( 0.000000000000000000, -0.9921567416492215186, 0.1249999999999996531 ) ) ;
#32036=CARTESIAN_POINT ( 'NONE',  ( 30.00000000000000000, -17.35230188589299871, 15.35019951917099945 ) ) ;
#32044=DIRECTION ( 'NONE',  ( 0.000000000000000000, 1.000000000000000000, 0.000000000000000000 ) ) ;
#32056=DIRECTION ( 'NONE',  ( 0.000000000000000000, -0.1111111111108836896, -0.9938079899999319178 ) ) ;
#32057=AXIS2_PLACEMENT_3D ( 'NONE', #12814, #66917, #67282 ) ;
#32080=ORIENTED_EDGE ( 'NONE', *, *, #58013, .F. ) ;
#32084=LINE ( 'NONE', #46679, #3775 ) ;
#32087=VERTEX_POINT ( 'NONE', #58601 ) ;
#32089=ORIENTED_EDGE ( 'NONE', *, *, #56640, .T. ) ;
#32090=PLANE ( 'NONE',  #39157 ) ;
#32100=FACE_OUTER_BOUND ( 'NONE', #33272, .T. ) ;
#32108=AXIS2_PLACEMENT_3D ( 'NONE', #58836, #27691, #48229 ) ;
#32123=VERTEX_POINT ( 'NONE', #11185 ) ;
#32124=CIRCLE ( 'NONE', #24191, 4.000000000000000888 ) ;
#32125=CARTESIAN_POINT ( 'NONE',  ( 25.50000000000000355, -15.50000000000000000, -24.50000000000000000 ) ) ;
#32126=CARTESIAN_POINT ( 'NONE',  ( -14.25000000000000000, -2.500000000000000000, 23.22168783648699986 ) ) ;
#32135=VERTEX_POINT ( 'NONE', #33103 ) ;
#32142=DIRECTION ( 'NONE',  ( 1.000000000000000000, -0.000000000000000000, -0.000000000000000000 ) ) ;
#32143=CARTESIAN_POINT ( 'NONE',  ( 18.85410196625000268, -15.50000000000000000, -21.50000000000000000 ) ) ;
#32146=CARTESIAN_POINT ( 'NONE',  ( 24.00000000000000000, -17.35230188589299516, -15.35019951917100478 ) ) ;
#32147=CARTESIAN_POINT ( 'NONE',  ( 30.00000000000000000, -12.00000000000000000, 10.69999999999999929 ) ) ;
#32150=FACE_OUTER_BOUND ( 'NONE', #18455, .T. ) ;
#32157=EDGE_CURVE ( 'NONE', #7905, #2702, #15783, .T. ) ;
#32161=EDGE_CURVE ( 'NONE', #17317, #48505, #11524, .T. ) ;
#32181=VERTEX_POINT ( 'NONE', #64945 ) ;
#32182=DIRECTION ( 'NONE',  ( -1.000000000000000000, 0.000000000000000000, 0.000000000000000000 ) ) ;
#32193=VERTEX_POINT ( 'NONE', #33790 ) ;
#32194=DIRECTION ( 'NONE',  ( 0.000000000000000000, -1.000000000000000000, 0.000000000000000000 ) ) ;
#32203=LINE ( 'NONE', #31866, #10240 ) ;
#32209=DIRECTION ( 'NONE',  ( 1.000000000000000000, -0.000000000000000000, -0.000000000000000000 ) ) ;
#32213=DIRECTION ( 'NONE',  ( 0.000000000000000000, 0.000000000000000000, 1.000000000000000000 ) ) ;
#32216=VECTOR ( 'NONE', #4004, 1000.000000000000000 ) ;
#32231=DIRECTION ( 'NONE',  ( -1.000000000000000000, 0.000000000000000000, 0.000000000000000000 ) ) ;
#32235=CYLINDRICAL_SURFACE ( 'NONE', #62109, 4.500000000000189182 ) ;
#32239=CARTESIAN_POINT ( 'NONE',  ( -17.00000000000000000, -15.50000000000000000, 19.33772233983200195 ) ) ;
#32251=CIRCLE ( 'NONE', #16457, 4.500000000000191847 ) ;
#32264=EDGE_LOOP ( 'NONE', ( #7636, #11725, #19187, #47314 ) ) ;
#32267=AXIS2_PLACEMENT_3D ( 'NONE', #29205, #40167, #30279 ) ;
#32272=VECTOR ( 'NONE', #53724, 1000.000000000000000 ) ;
#32278=CYLINDRICAL_SURFACE ( 'NONE', #18120, 4.500000000000188294 ) ;
#32285=CARTESIAN_POINT ( 'NONE',  ( -15.70313394609757296, -0.2715358723600092006, -23.82609623451302028 ) ) ;
#32286=ORIENTED_EDGE ( 'NONE', *, *, #40047, .F. ) ;
#32291=CIRCLE ( 'NONE', #44674, 3.499999999999849454 ) ;
#32307=ADVANCED_FACE ( 'NONE', ( #30248 ), #7619, .T. ) ;
#32310=PLANE ( 'NONE',  #17403 ) ;
#32311=DIRECTION ( 'NONE',  ( 0.000000000000000000, 0.000000000000000000, -1.000000000000000000 ) ) ;
#32324=LINE ( 'NONE', #16060, #65423 ) ;
#32325=EDGE_CURVE ( 'NONE', #58158, #45382, #18570, .T. ) ;
#32328=VERTEX_POINT ( 'NONE', #1971 ) ;
#32331=ORIENTED_EDGE ( 'NONE', *, *, #32991, .F. ) ;
#32344=ORIENTED_EDGE ( 'NONE', *, *, #22, .T. ) ;
#32345=VECTOR ( 'NONE', #37968, 1000.000000000000000 ) ;
#32347=LINE ( 'NONE', #49975, #1395 ) ;
#32349=ORIENTED_EDGE ( 'NONE', *, *, #64801, .T. ) ;
#32351=EDGE_LOOP ( 'NONE', ( #54884, #61189, #13619, #58624 ) ) ;
#32352=EDGE_CURVE ( 'NONE', #5599, #40609, #58697, .T. ) ;
#32355=DIRECTION ( 'NONE',  ( 1.000000000000000000, 0.000000000000000000, 0.000000000000000000 ) ) ;
#32370=VERTEX_POINT ( 'NONE', #23534 ) ;
#32386=DIRECTION ( 'NONE',  ( 0.000000000000000000, 0.7046037717862339012, 0.7096009616570518874 ) ) ;
#32391=EDGE_CURVE ( 'NONE', #35825, #57481, #63116, .T. ) ;
#32398=CARTESIAN_POINT ( 'NONE',  ( 11.00000000000000000, -12.00000000000000000, 10.20500000000000007 ) ) ;
#32413=LINE ( 'NONE', #37368, #40254 ) ;
#32414=DIRECTION ( 'NONE',  ( 0.000000000000000000, 0.000000000000000000, 1.000000000000000000 ) ) ;
#32422=FACE_OUTER_BOUND ( 'NONE', #68927, .T. ) ;
#32441=VERTEX_POINT ( 'NONE', #10423 ) ;
#32444=DIRECTION ( 'NONE',  ( 0.000000000000000000, 0.000000000000000000, -1.000000000000000000 ) ) ;
#32445=VECTOR ( 'NONE', #61681, 1000.000000000000000 ) ;
#32446=ORIENTED_EDGE ( 'NONE', *, *, #21564, .F. ) ;
#32463=AXIS2_PLACEMENT_3D ( 'NONE', #34246, #45210, #8073 ) ;
#32466=ORIENTED_EDGE ( 'NONE', *, *, #28577, .F. ) ;
#32467=VERTEX_POINT ( 'NONE', #25999 ) ;
#32474=EDGE_CURVE ( 'NONE', #32678, #68170, #33826, .T. ) ;
#32479=LINE ( 'NONE', #15859, #40303 ) ;
#32483=LINE ( 'NONE', #20121, #25298 ) ;
#32488=VERTEX_POINT ( 'NONE', #42240 ) ;
#32493=VERTEX_POINT ( 'NONE', #9371 ) ;
#32500=CARTESIAN_POINT ( 'NONE',  ( 15.50000000000000000, -5.000000000000000000, 22.50000000000000000 ) ) ;
#32504=CIRCLE ( 'NONE', #53955, 4.000000000000000000 ) ;
#32518=EDGE_CURVE ( 'NONE', #24504, #18955, #52882, .T. ) ;
#32520=AXIS2_PLACEMENT_3D ( 'NONE', #5092, #68747, #20298 ) ;
#32522=EDGE_CURVE ( 'NONE', #44169, #11224, #4438, .T. ) ;
#32523=EDGE_CURVE ( 'NONE', #61811, #59233, #53565, .T. ) ;
#32527=EDGE_CURVE ( 'NONE', #31007, #64218, #41188, .T. ) ;
#32529=EDGE_CURVE ( 'NONE', #19212, #33635, #35899, .T. ) ;
#32530=DIRECTION ( 'NONE',  ( 0.000000000000000000, 1.000000000000000000, 0.000000000000000000 ) ) ;
#32539=DIRECTION ( 'NONE',  ( -1.000000000000000000, 0.000000000000000000, 0.000000000000000000 ) ) ;
#32544=DIRECTION ( 'NONE',  ( 1.000000000000000000, -0.000000000000000000, -0.000000000000000000 ) ) ;
#32545=ORIENTED_EDGE ( 'NONE', *, *, #32860, .T. ) ;
#32557=DIRECTION ( 'NONE',  ( 0.000000000000000000, 1.000000000000000000, 0.000000000000000000 ) ) ;
#32560=CIRCLE ( 'NONE', #3171, 4.000000000000001776 ) ;
#32563=CARTESIAN_POINT ( 'NONE',  ( 11.00000000000000000, -5.599999999999999645, 9.000000000000001776 ) ) ;
#32565=EDGE_CURVE ( 'NONE', #14694, #67830, #65224, .T. ) ;
#32570=CARTESIAN_POINT ( 'NONE',  ( -30.00000000000000000, -5.200000000000001066, 9.400000000000000355 ) ) ;
#32573=CARTESIAN_POINT ( 'NONE',  ( -16.75000000000000000, -0.2714405302574915413, -22.01253933645463334 ) ) ;
#32578=ORIENTED_EDGE ( 'NONE', *, *, #67472, .T. ) ;
#32580=CARTESIAN_POINT ( 'NONE',  ( 13.00000000000000178, -17.50000000000000000, -15.70500000000000007 ) ) ;
#32588=DIRECTION ( 'NONE',  ( 0.000000000000000000, -0.6857142857147903170, 0.7278708115913530285 ) ) ;
#32589=ORIENTED_EDGE ( 'NONE', *, *, #1486, .T. ) ;
#32597=VERTEX_POINT ( 'NONE', #59896 ) ;
#32611=DIRECTION ( 'NONE',  ( 1.000000000000000000, -0.000000000000000000, -0.000000000000000000 ) ) ;
#32615=CARTESIAN_POINT ( 'NONE',  ( -11.00000000000000000, -8.959999999999999076, -12.95475478405700009 ) ) ;
#32621=ORIENTED_EDGE ( 'NONE', *, *, #50695, .F. ) ;
#32630=CARTESIAN_POINT ( 'NONE',  ( 25.50000000000000355, -5.200000000000001066, 22.50000000000000000 ) ) ;
#32640=ORIENTED_EDGE ( 'NONE', *, *, #41069, .F. ) ;
#32644=CARTESIAN_POINT ( 'NONE',  ( -15.50000000000000000, -0.2000000000000000111, -19.20000000000052509 ) ) ;
#32654=DIRECTION ( 'NONE',  ( 1.000000000000000000, 0.000000000000000000, 0.000000000000000000 ) ) ;
#32655=DIRECTION ( 'NONE',  ( 0.000000000000000000, 0.000000000000000000, -1.000000000000000000 ) ) ;
#32672=DIRECTION ( 'NONE',  ( 0.4998444328988824181, 0.000000000000000000, -0.8661152018640445593 ) ) ;
#32676=ORIENTED_EDGE ( 'NONE', *, *, #30203, .F. ) ;
#32678=VERTEX_POINT ( 'NONE', #65554 ) ;
#32687=CARTESIAN_POINT ( 'NONE',  ( -30.00000000000000000, -15.97213595500069871, -14.50000000000000000 ) ) ;
#32691=ORIENTED_EDGE ( 'NONE', *, *, #15311, .T. ) ;
#32697=EDGE_CURVE ( 'NONE', #48298, #33481, #66585, .T. ) ;
#32700=ORIENTED_EDGE ( 'NONE', *, *, #25340, .F. ) ;
#32707=VERTEX_POINT ( 'NONE', #40763 ) ;
#32713=VECTOR ( 'NONE', #39082, 1000.000000000000000 ) ;
#32718=VECTOR ( 'NONE', #45051, 1000.000000000000114 ) ;
#32726=CYLINDRICAL_SURFACE ( 'NONE', #62942, 0.5000000000079367624 ) ;
#32727=EDGE_CURVE ( 'NONE', #32123, #58343, #45010, .T. ) ;
#32729=CARTESIAN_POINT ( 'NONE',  ( 11.50000000000000000, -11.50000000000000000, -15.00000000000000000 ) ) ;
#32731=FACE_OUTER_BOUND ( 'NONE', #23257, .T. ) ;
#32736=VECTOR ( 'NONE', #5566, 1000.000000000000000 ) ;
#32748=CARTESIAN_POINT ( 'NONE',  ( -30.00000000000000000, -5.000000000000000000, 27.00000000000000000 ) ) ;
#32757=AXIS2_PLACEMENT_3D ( 'NONE', #67621, #19178, #65124 ) ;
#32758=EDGE_LOOP ( 'NONE', ( #3093, #30251, #35985, #31608, #18856, #69505 ) ) ;
#32759=CARTESIAN_POINT ( 'NONE',  ( 11.00000000000000000, -8.959999999999999076, 12.95475478405700009 ) ) ;
#32766=EDGE_LOOP ( 'NONE', ( #32331, #58087, #23838, #60218 ) ) ;
#32767=DIRECTION ( 'NONE',  ( 0.4999999999989361843, 0.000000000000000000, -0.8660254037850529940 ) ) ;
#32769=ORIENTED_EDGE ( 'NONE', *, *, #854, .F. ) ;
#32779=VERTEX_POINT ( 'NONE', #18844 ) ;
#32783=ORIENTED_EDGE ( 'NONE', *, *, #49736, .T. ) ;
#32785=ORIENTED_EDGE ( 'NONE', *, *, #28571, .F. ) ;
#32786=CYLINDRICAL_SURFACE ( 'NONE', #41268, 4.500000000000189182 ) ;
#32789=ORIENTED_EDGE ( 'NONE', *, *, #434, .T. ) ;
#32795=ORIENTED_EDGE ( 'NONE', *, *, #67714, .T. ) ;
#32802=EDGE_CURVE ( 'NONE', #16314, #60441, #24152, .T. ) ;
#32804=LINE ( 'NONE', #21504, #818 ) ;
#32807=ORIENTED_EDGE ( 'NONE', *, *, #3308, .F. ) ;
#32810=VECTOR ( 'NONE', #35669, 1000.000000000000000 ) ;
#32814=DIRECTION ( 'NONE',  ( 0.000000000000000000, 0.000000000000000000, 1.000000000000000000 ) ) ;
#32816=EDGE_CURVE ( 'NONE', #27463, #34438, #20246, .T. ) ;
#32828=CARTESIAN_POINT ( 'NONE',  ( -17.51999999999999957, -17.50000000000000000, 26.00000000000000355 ) ) ;
#32829=ADVANCED_FACE ( 'NONE', ( #19538 ), #4357, .F. ) ;
#32834=ORIENTED_EDGE ( 'NONE', *, *, #56098, .T. ) ;
#32837=EDGE_CURVE ( 'NONE', #16044, #40989, #25919, .T. ) ;
#32841=VECTOR ( 'NONE', #55336, 1000.000000000000000 ) ;
#32846=EDGE_LOOP ( 'NONE', ( #58930, #16627 ) ) ;
#32850=ORIENTED_EDGE ( 'NONE', *, *, #45492, .F. ) ;
#32851=AXIS2_PLACEMENT_3D ( 'NONE', #38578, #39258, #49187 ) ;
#32852=DIRECTION ( 'NONE',  ( 0.000000000000000000, 1.000000000000000000, 0.000000000000000000 ) ) ;
#32857=VERTEX_POINT ( 'NONE', #46412 ) ;
#32860=EDGE_CURVE ( 'NONE', #32488, #65011, #25566, .T. ) ;
#32888=FACE_OUTER_BOUND ( 'NONE', #48781, .T. ) ;
#32890=VECTOR ( 'NONE', #52116, 1000.000000000000000 ) ;
#32897=VERTEX_POINT ( 'NONE', #8930 ) ;
#32905=CARTESIAN_POINT ( 'NONE',  ( 30.00000000000000000, -17.50000000000000000, 26.64999999999999858 ) ) ;
#32908=ADVANCED_FACE ( 'NONE', ( #52800 ), #69035, .F. ) ;
#32911=ORIENTED_EDGE ( 'NONE', *, *, #43277, .T. ) ;
#32926=PLANE ( 'NONE',  #9986 ) ;
#32931=VERTEX_POINT ( 'NONE', #14591 ) ;
#32934=FACE_OUTER_BOUND ( 'NONE', #39549, .T. ) ;
#32956=EDGE_LOOP ( 'NONE', ( #68600, #13445, #5840, #27427 ) ) ;
#32963=AXIS2_PLACEMENT_3D ( 'NONE', #18390, #61892, #13093 ) ;
#32975=DIRECTION ( 'NONE',  ( -1.000000000000000000, 0.000000000000000000, 0.000000000000000000 ) ) ;
#32979=CARTESIAN_POINT ( 'NONE',  ( -29.50000000000000355, -11.50000000000000000, -15.00000000000000000 ) ) ;
#32987=AXIS2_PLACEMENT_3D ( 'NONE', #26067, #20741, #41252 ) ;
#32989=CARTESIAN_POINT ( 'NONE',  ( 15.70313394608857394, -0.2715358723588625622, 23.82609623451821079 ) ) ;
#32991=EDGE_CURVE ( 'NONE', #25346, #57801, #54636, .T. ) ;
#32992=ADVANCED_FACE ( 'NONE', ( #5740 ), #43204, .T. ) ;
#33010=VECTOR ( 'NONE', #32530, 1000.000000000000000 ) ;
#33017=CARTESIAN_POINT ( 'NONE',  ( 15.50000000000000000, -2.500000000000000000, 21.05662432702600029 ) ) ;
#33023=CARTESIAN_POINT ( 'NONE',  ( -30.00000000000000000, -13.54524521594299991, 17.53999999999999915 ) ) ;
#33028=FACE_OUTER_BOUND ( 'NONE', #46326, .T. ) ;
#33034=VECTOR ( 'NONE', #49378, 1000.000000000000000 ) ;
#33035=ORIENTED_EDGE ( 'NONE', *, *, #45661, .T. ) ;
#33036=ORIENTED_EDGE ( 'NONE', *, *, #37493, .F. ) ;
#33039=DIRECTION ( 'NONE',  ( 0.000000000000000000, -0.7084617869623469621, 0.7057491738671168857 ) ) ;
#33059=CARTESIAN_POINT ( 'NONE',  ( 17.00000000000000000, -17.50000000000000000, -19.33772233983200195 ) ) ;
#33065=VECTOR ( 'NONE', #39577, 1000.000000000000000 ) ;
#33069=ADVANCED_FACE ( 'NONE', ( #64438 ), #49555, .T. ) ;
#33071=CARTESIAN_POINT ( 'NONE',  ( -24.00000000000000000, -17.50000000000000000, 19.33772233983200195 ) ) ;
#33074=EDGE_CURVE ( 'NONE', #50086, #27584, #45563, .T. ) ;
#33076=DIRECTION ( 'NONE',  ( -1.000000000000000000, 0.000000000000000000, 0.000000000000000000 ) ) ;
#33080=FACE_OUTER_BOUND ( 'NONE', #8796, .T. ) ;
#33089=LINE ( 'NONE', #16832, #32713 ) ;
#33096=CARTESIAN_POINT ( 'NONE',  ( 11.00000000000000000, -5.599999999999379696, 26.60000000000059828 ) ) ;
#33097=DIRECTION ( 'NONE',  ( 0.000000000000000000, 1.000000000000000000, 0.000000000000000000 ) ) ;
#33100=ORIENTED_EDGE ( 'NONE', *, *, #41238, .F. ) ;
#33103=CARTESIAN_POINT ( 'NONE',  ( -11.00000000000000000, -9.454754784057099570, -17.53999999999999915 ) ) ;
#33112=ORIENTED_EDGE ( 'NONE', *, *, #8750, .T. ) ;
#33115=CARTESIAN_POINT ( 'NONE',  ( 30.00000000000000000, -11.85423089348099879, -9.852125413066602277 ) ) ;
#33127=ORIENTED_EDGE ( 'NONE', *, *, #10257, .F. ) ;
#33130=DIRECTION ( 'NONE',  ( 0.000000000000000000, -0.7071067811865455743, -0.7071067811865495711 ) ) ;
#33135=FACE_OUTER_BOUND ( 'NONE', #28380, .T. ) ;
#33137=ORIENTED_EDGE ( 'NONE', *, *, #17237, .F. ) ;
#33146=EDGE_CURVE ( 'NONE', #37986, #25888, #3844, .T. ) ;
#33157=CARTESIAN_POINT ( 'NONE',  ( 29.50000000000000355, -12.00000000000000000, 11.03137303340310282 ) ) ;
#33175=FACE_OUTER_BOUND ( 'NONE', #46755, .T. ) ;
#33176=CARTESIAN_POINT ( 'NONE',  ( 25.50000000000000355, -15.12100000000000044, 24.12099999999999511 ) ) ;
#33190=CARTESIAN_POINT ( 'NONE',  ( 17.51999999999999957, -15.50000000000000000, 26.00000000000000355 ) ) ;
#33205=VECTOR ( 'NONE', #2594, 1000.000000000000000 ) ;
#33209=CARTESIAN_POINT ( 'NONE',  ( -11.00000000000000000, -5.200000000000001066, -9.400000000000000355 ) ) ;
#33215=EDGE_LOOP ( 'NONE', ( #24889, #33903, #68071, #63206 ) ) ;
#33226=VECTOR ( 'NONE', #57381, 1000.000000000000000 ) ;
#33230=EDGE_CURVE ( 'NONE', #52237, #38194, #29828, .T. ) ;
#33236=CARTESIAN_POINT ( 'NONE',  ( 15.50000000000000000, -1.037157890325000054, -26.00000000000000000 ) ) ;
#33240=ADVANCED_FACE ( 'NONE', ( #24772 ), #10663, .F. ) ;
#33243=DIRECTION ( 'NONE',  ( 1.000000000000000000, -0.000000000000000000, -0.000000000000000000 ) ) ;
#33245=DIRECTION ( 'NONE',  ( 1.000000000000000000, 0.000000000000000000, 0.000000000000000000 ) ) ;
#33247=EDGE_CURVE ( 'NONE', #29049, #39153, #46273, .T. ) ;
#33249=DIRECTION ( 'NONE',  ( -1.000000000000000000, 0.000000000000000000, 0.000000000000000000 ) ) ;
#33251=CARTESIAN_POINT ( 'NONE',  ( -16.75000000000000355, -0.2715193793361450614, -22.98718409945082541 ) ) ;
#33259=EDGE_CURVE ( 'NONE', #53470, #18955, #52461, .T. ) ;
#33264=AXIS2_PLACEMENT_3D ( 'NONE', #29727, #3570, #68970 ) ;
#33266=CARTESIAN_POINT ( 'NONE',  ( 11.75000000000000000, -5.200000000000001066, 60.00000000000000000 ) ) ;
#33272=EDGE_LOOP ( 'NONE', ( #54553, #23189, #7032, #54433 ) ) ;
#33280=CARTESIAN_POINT ( 'NONE',  ( 11.50000000000000000, -11.50000000000100009, -15.00000000000084910 ) ) ;
#33283=AXIS2_PLACEMENT_3D ( 'NONE', #37835, #703, #43825 ) ;
#33289=ORIENTED_EDGE ( 'NONE', *, *, #51342, .T. ) ;
#33290=CARTESIAN_POINT ( 'NONE',  ( 11.00000000000000000, -11.50000000000000000, 15.00000000000000000 ) ) ;
#33296=PLANE ( 'NONE',  #27456 ) ;
#33302=EDGE_CURVE ( 'NONE', #67901, #4292, #53059, .T. ) ;
#33310=DIRECTION ( 'NONE',  ( 0.000000000000000000, 0.000000000000000000, -1.000000000000000000 ) ) ;
#33322=ORIENTED_EDGE ( 'NONE', *, *, #64318, .T. ) ;
#33324=CIRCLE ( 'NONE', #52556, 2.000000000000001776 ) ;
#33329=AXIS2_PLACEMENT_3D ( 'NONE', #12429, #55586, #27682 ) ;
#33332=AXIS2_PLACEMENT_3D ( 'NONE', #40728, #18102, #8189 ) ;
#33346=CARTESIAN_POINT ( 'NONE',  ( -17.00000000000000000, -17.35230188589299871, 15.35019951917099945 ) ) ;
#33349=VECTOR ( 'NONE', #11780, 1000.000000000000114 ) ;
#33350=ORIENTED_EDGE ( 'NONE', *, *, #47527, .F. ) ;
#33359=CARTESIAN_POINT ( 'NONE',  ( 17.00000000000000000, -17.00000000000000000, 15.70499999999969809 ) ) ;
#33365=AXIS2_PLACEMENT_3D ( 'NONE', #11118, #39369, #34051 ) ;
#33367=CARTESIAN_POINT ( 'NONE',  ( -30.00000000000000000, -8.959999999999999076, -12.95475478405700009 ) ) ;
#33385=ORIENTED_EDGE ( 'NONE', *, *, #54058, .T. ) ;
#33388=ORIENTED_EDGE ( 'NONE', *, *, #57655, .T. ) ;
#33394=EDGE_CURVE ( 'NONE', #16184, #5636, #42252, .T. ) ;
#33396=VERTEX_POINT ( 'NONE', #26522 ) ;
#33406=CARTESIAN_POINT ( 'NONE',  ( 29.25000000000000000, -5.200000000000001066, 26.25000000000000000 ) ) ;
#33407=LINE ( 'NONE', #42622, #14168 ) ;
#33409=CARTESIAN_POINT ( 'NONE',  ( -11.00000000000000000, -16.64230188589299786, -14.64519951917100116 ) ) ;
#33410=CIRCLE ( 'NONE', #52597, 3.499999999999056310 ) ;
#33430=EDGE_CURVE ( 'NONE', #19600, #8140, #48785, .T. ) ;
#33438=CARTESIAN_POINT ( 'NONE',  ( 30.00000000000000000, -16.64230188589299786, -14.64519951917100116 ) ) ;
#33441=VECTOR ( 'NONE', #32311, 1000.000000000000000 ) ;
#33449=CIRCLE ( 'NONE', #11977, 3.499999999999999556 ) ;
#33451=CARTESIAN_POINT ( 'NONE',  ( 17.51999999999999957, -17.50000000000000000, 26.00000000000000355 ) ) ;
#33457=LINE ( 'NONE', #6236, #51512 ) ;
#33465=VERTEX_POINT ( 'NONE', #65395 ) ;
#33481=VERTEX_POINT ( 'NONE', #38523 ) ;
#33491=CARTESIAN_POINT ( 'NONE',  ( 29.25000000000000000, -5.200000000000001066, -11.75000000000000000 ) ) ;
#33499=CIRCLE ( 'NONE', #18969, 3.499999999999999556 ) ;
#33505=VECTOR ( 'NONE', #19149, 1000.000000000000000 ) ;
#33511=DIRECTION ( 'NONE',  ( 1.000000000000000000, -0.000000000000000000, -0.000000000000000000 ) ) ;
#33516=DIRECTION ( 'NONE',  ( 0.000000000000000000, -1.000000000000000000, 0.000000000000000000 ) ) ;
#33522=ORIENTED_EDGE ( 'NONE', *, *, #28577, .T. ) ;
#33534=CARTESIAN_POINT ( 'NONE',  ( 15.50000000000000000, -0.2000000000000000111, 22.50000000000000000 ) ) ;
#33537=CARTESIAN_POINT ( 'NONE',  ( 11.50000000000000000, -12.00000000000000000, -11.00000000000000000 ) ) ;
#33553=DIRECTION ( 'NONE',  ( 0.000000000000000000, -2.854859206170826497E-12, 1.000000000000000000 ) ) ;
#33566=DIRECTION ( 'NONE',  ( -0.4998444328988824181, 0.000000000000000000, 0.8661152018640445593 ) ) ;
#33574=EDGE_LOOP ( 'NONE', ( #22888, #40868, #49631, #34971 ) ) ;
#33588=DIRECTION ( 'NONE',  ( -1.000000000000000000, 0.000000000000000000, 0.000000000000000000 ) ) ;
#33594=CIRCLE ( 'NONE', #69759, 3.499999999999054534 ) ;
#33599=CARTESIAN_POINT ( 'NONE',  ( 29.50000000000000355, -11.50000000000100009, 10.50000000000065903 ) ) ;
#33601=VECTOR ( 'NONE', #22715, 1000.000000000000000 ) ;
#33604=PLANE ( 'NONE',  #23341 ) ;
#33611=FACE_OUTER_BOUND ( 'NONE', #43870, .T. ) ;
#33620=ORIENTED_EDGE ( 'NONE', *, *, #10395, .F. ) ;
#33627=ADVANCED_FACE ( 'NONE', ( #28933 ), #50509, .F. ) ;
#33628=EDGE_CURVE ( 'NONE', #45304, #24526, #68297, .T. ) ;
#33635=VERTEX_POINT ( 'NONE', #23976 ) ;
#33638=EDGE_CURVE ( 'NONE', #17310, #47121, #58264, .T. ) ;
#33640=VECTOR ( 'NONE', #25264, 1000.000000000000000 ) ;
#33650=CARTESIAN_POINT ( 'NONE',  ( 30.00000000000000000, -9.200000000000120082, 17.30000000000000071 ) ) ;
#33658=FACE_OUTER_BOUND ( 'NONE', #14346, .T. ) ;
#33661=ORIENTED_EDGE ( 'NONE', *, *, #6927, .T. ) ;
#33664=EDGE_LOOP ( 'NONE', ( #5802, #69880, #3693, #36504 ) ) ;
#33667=EDGE_LOOP ( 'NONE', ( #60282, #1554, #28012, #30162 ) ) ;
#33669=DIRECTION ( 'NONE',  ( 0.000000000000000000, 0.000000000000000000, -1.000000000000000000 ) ) ;
#33671=CARTESIAN_POINT ( 'NONE',  ( -15.50000000000000000, -1.037157890325000054, 22.50000000000000000 ) ) ;
#33672=FACE_OUTER_BOUND ( 'NONE', #56707, .T. ) ;
#33676=VERTEX_POINT ( 'NONE', #35626 ) ;
#33681=LINE ( 'NONE', #48922, #33441 ) ;
#33685=FACE_OUTER_BOUND ( 'NONE', #54374, .T. ) ;
#33688=EDGE_LOOP ( 'NONE', ( #49583, #54537, #23619, #47140, #25379, #38638 ) ) ;
#33689=FACE_OUTER_BOUND ( 'NONE', #32264, .T. ) ;
#33693=DIRECTION ( 'NONE',  ( 0.000000000000000000, -0.9921567416492215186, 0.1249999999999996531 ) ) ;
#33700=FACE_BOUND ( 'NONE', #2073, .T. ) ;
#33706=DIRECTION ( 'NONE',  ( 0.000000000000000000, 0.000000000000000000, 1.000000000000000000 ) ) ;
#33717=EDGE_LOOP ( 'NONE', ( #36162, #37479, #1159, #37546 ) ) ;
#33723=ORIENTED_EDGE ( 'NONE', *, *, #33628, .F. ) ;
#33732=ORIENTED_EDGE ( 'NONE', *, *, #64726, .F. ) ;
#33749=DIRECTION ( 'NONE',  ( 0.000000000000000000, 0.000000000000000000, 1.000000000000000000 ) ) ;
#33756=EDGE_CURVE ( 'NONE', #45382, #37614, #69416, .T. ) ;
#33759=ORIENTED_EDGE ( 'NONE', *, *, #5157, .F. ) ;
#33760=CARTESIAN_POINT ( 'NONE',  ( 11.50000000000000000, -12.00000000000000000, -11.03137303340310282 ) ) ;
#33766=ADVANCED_FACE ( 'NONE', ( #17122 ), #23110, .T. ) ;
#33767=ORIENTED_EDGE ( 'NONE', *, *, #14793, .T. ) ;
#33789=VECTOR ( 'NONE', #22598, 1000.000000000000000 ) ;
#33790=CARTESIAN_POINT ( 'NONE',  ( -15.50000000000000000, 0.000000000000000000, -18.50000000000000000 ) ) ;
#33792=EDGE_LOOP ( 'NONE', ( #10935, #14334, #16743, #35786, #16257, #61662, #33620, #27740, #12066, #36889, #69334, #42971, #35121, #16760 ) ) ;
#33797=CARTESIAN_POINT ( 'NONE',  ( 30.00000000000000000, 0.000000000000000000, -27.00000000000000000 ) ) ;
#33810=DIRECTION ( 'NONE',  ( 8.659560562354963673E-17, 0.7071067811865450192, -0.7071067811865500152 ) ) ;
#33811=ORIENTED_EDGE ( 'NONE', *, *, #60362, .T. ) ;
#33815=CARTESIAN_POINT ( 'NONE',  ( 30.00000000000000000, -12.00000000000000000, 11.00000000000000000 ) ) ;
#33817=VERTEX_POINT ( 'NONE', #44668 ) ;
#33825=CARTESIAN_POINT ( 'NONE',  ( -17.00000000000000000, -15.50000000000000000, 19.33772233983200195 ) ) ;
#33826=CIRCLE ( 'NONE', #16947, 0.2999999999998732569 ) ;
#33828=EDGE_CURVE ( 'NONE', #65032, #32370, #22438, .T. ) ;
#33830=CARTESIAN_POINT ( 'NONE',  ( 14.24999999999999822, -0.2715193793361405095, 22.01281590054915327 ) ) ;
#33848=LINE ( 'NONE', #8013, #24387 ) ;
#33855=VECTOR ( 'NONE', #33810, 1000.000000000000000 ) ;
#33856=DIRECTION ( 'NONE',  ( -1.000000000000000000, 0.000000000000000000, 0.000000000000000000 ) ) ;
#33862=PLANE ( 'NONE',  #768 ) ;
#33863=CARTESIAN_POINT ( 'NONE',  ( -25.50000000000000355, 0.000000000000000000, 20.87899999999999778 ) ) ;
#33867=CARTESIAN_POINT ( 'NONE',  ( 24.00000000000000000, -15.50000000000000000, 19.33772233983200195 ) ) ;
#33871=ORIENTED_EDGE ( 'NONE', *, *, #50551, .F. ) ;
#33873=CARTESIAN_POINT ( 'NONE',  ( 28.00000000000000000, -16.64230188589299786, -14.64519951917100116 ) ) ;
#33877=DIRECTION ( 'NONE',  ( 0.000000000000000000, -0.7046037717806115097, 0.7096009616626348659 ) ) ;
#33878=VECTOR ( 'NONE', #60924, 1000.000000000000000 ) ;
#33898=AXIS2_PLACEMENT_3D ( 'NONE', #9097, #52951, #21112 ) ;
#33902=CARTESIAN_POINT ( 'NONE',  ( -11.50000000000000000, -12.00000000000000000, 11.03137303340310282 ) ) ;
#33903=ORIENTED_EDGE ( 'NONE', *, *, #60277, .F. ) ;
#33906=CARTESIAN_POINT ( 'NONE',  ( -30.00000000000000000, -11.85423089348099879, -9.852125413066602277 ) ) ;
#33907=DIRECTION ( 'NONE',  ( 0.000000000000000000, 0.000000000000000000, 1.000000000000000000 ) ) ;
#33908=ORIENTED_EDGE ( 'NONE', *, *, #34332, .F. ) ;
#33914=AXIS2_PLACEMENT_3D ( 'NONE', #64463, #55828, #16022 ) ;
#33916=CARTESIAN_POINT ( 'NONE',  ( 15.50000000000000000, -0.4000000000000000222, -25.99999999999999645 ) ) ;
#33920=CARTESIAN_POINT ( 'NONE',  ( 25.50000000000000355, 0.000000000000000000, -20.24999999999999645 ) ) ;
#33925=EDGE_LOOP ( 'NONE', ( #9672, #63450, #1973, #3404 ) ) ;
#33926=DIRECTION ( 'NONE',  ( 0.000000000000000000, 0.000000000000000000, -1.000000000000000000 ) ) ;
#33928=CIRCLE ( 'NONE', #59891, 4.500000000000190958 ) ;
#33929=EDGE_CURVE ( 'NONE', #43823, #43603, #7545, .T. ) ;
#33931=LINE ( 'NONE', #2119, #31037 ) ;
#33934=CARTESIAN_POINT ( 'NONE',  ( -24.00000000000000000, -16.28999999999999915, 14.50000000000000000 ) ) ;
#33948=EDGE_CURVE ( 'NONE', #5787, #65641, #29810, .T. ) ;
#33951=CIRCLE ( 'NONE', #58821, 4.000000000000001776 ) ;
#33954=DIRECTION ( 'NONE',  ( 0.000000000000000000, 0.000000000000000000, 1.000000000000000000 ) ) ;
#33957=CARTESIAN_POINT ( 'NONE',  ( 23.50000000000000000, -5.200000000000001066, 22.50000000000000000 ) ) ;
#33959=LINE ( 'NONE', #39274, #29734 ) ;
#33967=DIRECTION ( 'NONE',  ( -0.000000000000000000, 1.000000000000000000, -0.000000000000000000 ) ) ;
#33972=CARTESIAN_POINT ( 'NONE',  ( -11.50000000000000000, -11.50000000000100009, -10.50000000000065903 ) ) ;
#33974=DIRECTION ( 'NONE',  ( 0.000000000000000000, 0.7278708115913771204, 0.6857142857147648929 ) ) ;
#33975=ORIENTED_EDGE ( 'NONE', *, *, #16558, .F. ) ;
#33981=VECTOR ( 'NONE', #22212, 1000.000000000000000 ) ;
#33997=ORIENTED_EDGE ( 'NONE', *, *, #23443, .T. ) ;
#33998=AXIS2_PLACEMENT_3D ( 'NONE', #27636, #54178, #27988 ) ;
#34006=CARTESIAN_POINT ( 'NONE',  ( 25.50000000000000355, -15.50000000000000000, -24.50000000000000000 ) ) ;
#34009=EDGE_CURVE ( 'NONE', #20348, #36958, #45021, .T. ) ;
#34022=FACE_OUTER_BOUND ( 'NONE', #12828, .T. ) ;
#34031=VERTEX_POINT ( 'NONE', #56688 ) ;
#34041=LINE ( 'NONE', #48593, #68185 ) ;
#34045=VERTEX_POINT ( 'NONE', #40778 ) ;
#34051=DIRECTION ( 'NONE',  ( 0.000000000000000000, 0.000000000000000000, -1.000000000000000000 ) ) ;
#34053=ORIENTED_EDGE ( 'NONE', *, *, #23080, .T. ) ;
#34054=VERTEX_POINT ( 'NONE', #13901 ) ;
#34055=EDGE_CURVE ( 'NONE', #66537, #10509, #33324, .T. ) ;
#34056=VERTEX_POINT ( 'NONE', #53496 ) ;
#34058=DIRECTION ( 'NONE',  ( 1.000000000000000000, 0.000000000000000000, 0.000000000000000000 ) ) ;
#34061=VECTOR ( 'NONE', #13224, 1000.000000000000000 ) ;
#34068=EDGE_CURVE ( 'NONE', #32857, #5665, #61556, .T. ) ;
#34070=ORIENTED_EDGE ( 'NONE', *, *, #32527, .T. ) ;
#34071=ORIENTED_EDGE ( 'NONE', *, *, #48011, .F. ) ;
#34075=CARTESIAN_POINT ( 'NONE',  ( 11.50000000000000000, -11.50000000000000000, 15.00000000000000000 ) ) ;
#34079=CARTESIAN_POINT ( 'NONE',  ( -15.50000000000000000, -0.4000000000000000222, 25.99999999999999645 ) ) ;
#34084=EDGE_CURVE ( 'NONE', #39125, #14787, #42354, .T. ) ;
#34088=EDGE_CURVE ( 'NONE', #30792, #11691, #4370, .T. ) ;
#34089=ADVANCED_FACE ( 'NONE', ( #57735 ), #19908, .F. ) ;
#34097=CARTESIAN_POINT ( 'NONE',  ( 17.00000000000000000, -15.50000000000000000, 19.33772233983200195 ) ) ;
#34100=LINE ( 'NONE', #49000, #24531 ) ;
#34107=EDGE_CURVE ( 'NONE', #27508, #903, #41479, .T. ) ;
#34110=ADVANCED_FACE ( 'NONE', ( #68713 ), #47141, .F. ) ;
#34111=ORIENTED_EDGE ( 'NONE', *, *, #7020, .T. ) ;
#34133=DIRECTION ( 'NONE',  ( -1.000000000000000000, 0.000000000000000000, 0.000000000000000000 ) ) ;
#34142=EDGE_LOOP ( 'NONE', ( #28628, #43074, #63790, #18675, #47574, #47580 ) ) ;
#34154=AXIS2_PLACEMENT_3D ( 'NONE', #7311, #33511, #6968 ) ;
#34159=VECTOR ( 'NONE', #62978, 1000.000000000000000 ) ;
#34164=CARTESIAN_POINT ( 'NONE',  ( -30.00000000000000000, -17.35230188589299871, -15.35019951917099945 ) ) ;
#34168=DIRECTION ( 'NONE',  ( 0.000000000000000000, 0.000000000000000000, 1.000000000000000000 ) ) ;
#34173=AXIS2_PLACEMENT_3D ( 'NONE', #31497, #67914, #35730 ) ;
#34185=EDGE_CURVE ( 'NONE', #27132, #32493, #5752, .T. ) ;
#34189=DIRECTION ( 'NONE',  ( -0.3479852726768751237, 0.000000000000000000, 0.9375000000000004441 ) ) ;
#34204=CYLINDRICAL_SURFACE ( 'NONE', #4037, 4.000000000000000000 ) ;
#34210=ORIENTED_EDGE ( 'NONE', *, *, #19977, .F. ) ;
#34226=ORIENTED_EDGE ( 'NONE', *, *, #34084, .F. ) ;
#34229=EDGE_CURVE ( 'NONE', #27219, #15321, #69462, .T. ) ;
#34236=ORIENTED_EDGE ( 'NONE', *, *, #61101, .F. ) ;
#34237=DIRECTION ( 'NONE',  ( 0.000000000000000000, 0.000000000000000000, 1.000000000000000000 ) ) ;
#34240=ADVANCED_FACE ( 'NONE', ( #17379 ), #64452, .T. ) ;
#34241=FACE_OUTER_BOUND ( 'NONE', #24132, .T. ) ;
#34244=CIRCLE ( 'NONE', #64765, 2.000000000000001776 ) ;
#34246=CARTESIAN_POINT ( 'NONE',  ( 11.50000000000000000, -11.50000000000000000, -15.00000000000000000 ) ) ;
#34248=LINE ( 'NONE', #49836, #31206 ) ;
#34256=DIRECTION ( 'NONE',  ( 0.000000000000000000, 0.000000000000000000, -1.000000000000000000 ) ) ;
#34269=FACE_OUTER_BOUND ( 'NONE', #14630, .T. ) ;
#34272=EDGE_LOOP ( 'NONE', ( #36825, #36096, #55826, #15893, #33767, #2180, #61532, #69313, #17031, #66100, #21283, #52057, #15343, #19490, #899, #21161, #19742, #52083 ) ) ;
#34274=DIRECTION ( 'NONE',  ( 0.000000000000000000, 1.000000000000000000, 0.000000000000000000 ) ) ;
#34277=EDGE_CURVE ( 'NONE', #36987, #41126, #35569, .T. ) ;
#34289=VECTOR ( 'NONE', #12624, 1000.000000000000000 ) ;
#34307=CARTESIAN_POINT ( 'NONE',  ( 25.50000000000000355, -17.50000000000000000, -22.50000000000000000 ) ) ;
#34315=ORIENTED_EDGE ( 'NONE', *, *, #58057, .F. ) ;
#34331=CARTESIAN_POINT ( 'NONE',  ( 30.00000000000000000, -11.50000000000100009, 15.00000000000084910 ) ) ;
#34332=EDGE_CURVE ( 'NONE', #4441, #19992, #19775, .T. ) ;
#34351=CARTESIAN_POINT ( 'NONE',  ( -30.00000000000000000, -5.599999999999379696, -26.60000000000059828 ) ) ;
#34362=ORIENTED_EDGE ( 'NONE', *, *, #65506, .F. ) ;
#34366=VERTEX_POINT ( 'NONE', #47705 ) ;
#34367=CARTESIAN_POINT ( 'NONE',  ( 11.00000000000000000, -8.959999999999999076, 17.04524521594300523 ) ) ;
#34377=ADVANCED_FACE ( 'NONE', ( #68926 ), #64325, .F. ) ;
#34386=LINE ( 'NONE', #28747, #26956 ) ;
#34392=PLANE ( 'NONE',  #44290 ) ;
#34396=VERTEX_POINT ( 'NONE', #47004 ) ;
#34411=ORIENTED_EDGE ( 'NONE', *, *, #5633, .T. ) ;
#34413=ORIENTED_EDGE ( 'NONE', *, *, #22845, .T. ) ;
#34416=EDGE_CURVE ( 'NONE', #43499, #5667, #59010, .T. ) ;
#34424=VERTEX_POINT ( 'NONE', #25401 ) ;
#34426=VECTOR ( 'NONE', #63024, 1000.000000000000114 ) ;
#34427=CARTESIAN_POINT ( 'NONE',  ( -25.50000000000000355, -5.578999999999999737, 20.87900000000000134 ) ) ;
#34428=CARTESIAN_POINT ( 'NONE',  ( 30.00000000000000000, -9.487228132326899654, 12.50000000000000000 ) ) ;
#34429=DIRECTION ( 'NONE',  ( -1.000000000000000000, 0.000000000000000000, 0.000000000000000000 ) ) ;
#34434=VECTOR ( 'NONE', #54708, 1000.000000000000000 ) ;
#34436=DIRECTION ( 'NONE',  ( 0.4998444328988824181, 0.000000000000000000, -0.8661152018640445593 ) ) ;
#34437=ADVANCED_FACE ( 'NONE', ( #32100 ), #59318, .F. ) ;
#34438=VERTEX_POINT ( 'NONE', #46959 ) ;
#34448=LINE ( 'NONE', #7592, #60264 ) ;
#34458=FACE_OUTER_BOUND ( 'NONE', #66807, .T. ) ;
#34462=DIRECTION ( 'NONE',  ( 0.000000000000000000, 0.000000000000000000, -1.000000000000000000 ) ) ;
#34466=ORIENTED_EDGE ( 'NONE', *, *, #5872, .T. ) ;
#34480=EDGE_CURVE ( 'NONE', #701, #57822, #26453, .T. ) ;
#34489=CARTESIAN_POINT ( 'NONE',  ( 15.50000000000000000, 998.9628421096749662, -22.50000000000000000 ) ) ;
#34508=CARTESIAN_POINT ( 'NONE',  ( 11.50000000000000000, -11.70000000000012008, -11.00000000000000000 ) ) ;
#34517=DIRECTION ( 'NONE',  ( 0.000000000000000000, 1.000000000000000000, 0.000000000000000000 ) ) ;
#34530=VECTOR ( 'NONE', #46138, 1000.000000000000114 ) ;
#34533=DIRECTION ( 'NONE',  ( 0.000000000000000000, 0.000000000000000000, 1.000000000000000000 ) ) ;
#34537=AXIS2_PLACEMENT_3D ( 'NONE', #58120, #57766, #47509 ) ;
#34553=FACE_OUTER_BOUND ( 'NONE', #33925, .T. ) ;
#34558=CARTESIAN_POINT ( 'NONE',  ( -18.85410196625000268, -15.50000000000000000, -21.50000000000000000 ) ) ;
#34563=CARTESIAN_POINT ( 'NONE',  ( -24.00000000000000000, -17.00000000000000000, 15.70499999999969809 ) ) ;
#34565=LINE ( 'NONE', #18300, #5462 ) ;
#34567=EDGE_CURVE ( 'NONE', #19600, #28340, #5582, .T. ) ;
#34568=EDGE_CURVE ( 'NONE', #414, #22030, #10804, .T. ) ;
#34576=EDGE_CURVE ( 'NONE', #32493, #49918, #54712, .T. ) ;
#34579=DIRECTION ( 'NONE',  ( 0.000000000000000000, 0.000000000000000000, 1.000000000000000000 ) ) ;
#34581=EDGE_LOOP ( 'NONE', ( #38195, #15262, #8418, #46076 ) ) ;
#34587=ORIENTED_EDGE ( 'NONE', *, *, #1072, .T. ) ;
#34596=AXIS2_PLACEMENT_3D ( 'NONE', #13779, #62556, #34986 ) ;
#34603=AXIS2_PLACEMENT_3D ( 'NONE', #61366, #23203, #65982 ) ;
#34605=DIRECTION ( 'NONE',  ( 0.000000000000000000, -1.000000000000000000, 0.000000000000000000 ) ) ;
#34607=FACE_OUTER_BOUND ( 'NONE', #28019, .T. ) ;
#34614=DIRECTION ( 'NONE',  ( -1.000000000000000000, 0.000000000000000000, 0.000000000000000000 ) ) ;
#34615=DIRECTION ( 'NONE',  ( 0.000000000000000000, 0.000000000000000000, -1.000000000000000000 ) ) ;
#34618=ORIENTED_EDGE ( 'NONE', *, *, #34567, .F. ) ;
#34619=DIRECTION ( 'NONE',  ( 1.000000000000000000, -0.000000000000000000, -0.000000000000000000 ) ) ;
#34622=DIRECTION ( 'NONE',  ( 0.000000000000000000, -1.000000000000000000, -2.854859206170826497E-12 ) ) ;
#34625=DIRECTION ( 'NONE',  ( 1.000000000000000000, 0.000000000000000000, 0.000000000000000000 ) ) ;
#34630=ORIENTED_EDGE ( 'NONE', *, *, #60856, .T. ) ;
#34636=FACE_BOUND ( 'NONE', #35532, .T. ) ;
#34654=DIRECTION ( 'NONE',  ( 1.000000000000000000, 0.000000000000000000, 0.000000000000000000 ) ) ;
#34666=VERTEX_POINT ( 'NONE', #39132 ) ;
#34670=CARTESIAN_POINT ( 'NONE',  ( 29.50000000000000355, -11.50000000000100009, -10.50000000000065903 ) ) ;
#34672=CARTESIAN_POINT ( 'NONE',  ( 30.00000000000000000, -14.04000000000000092, 14.80000000000000071 ) ) ;
#34674=ORIENTED_EDGE ( 'NONE', *, *, #55251, .F. ) ;
#34687=ADVANCED_FACE ( 'NONE', ( #6948 ), #50088, .F. ) ;
#34690=ORIENTED_EDGE ( 'NONE', *, *, #57958, .T. ) ;
#34696=AXIS2_PLACEMENT_3D ( 'NONE', #16065, #9718, #63456 ) ;
#34697=CIRCLE ( 'NONE', #65223, 4.000000000000000888 ) ;
#34700=CARTESIAN_POINT ( 'NONE',  ( -17.00000000000000000, -15.50000000000000000, 14.50000000000000000 ) ) ;
#34705=AXIS2_PLACEMENT_3D ( 'NONE', #35146, #7585, #24561 ) ;
#34714=LINE ( 'NONE', #67250, #42793 ) ;
#34715=CARTESIAN_POINT ( 'NONE',  ( 11.50000000000000000, -15.97213595500069871, 14.50000000000000000 ) ) ;
#34720=FACE_OUTER_BOUND ( 'NONE', #58603, .T. ) ;
#34722=DIRECTION ( 'NONE',  ( 0.000000000000000000, 0.000000000000000000, 1.000000000000000000 ) ) ;
#34729=EDGE_CURVE ( 'NONE', #12276, #11704, #62793, .T. ) ;
#34732=EDGE_CURVE ( 'NONE', #11358, #4089, #45468, .T. ) ;
#34736=VECTOR ( 'NONE', #28052, 1000.000000000000000 ) ;
#34742=FACE_OUTER_BOUND ( 'NONE', #25483, .T. ) ;
#34753=FACE_BOUND ( 'NONE', #45482, .T. ) ;
#34756=( GEOMETRIC_REPRESENTATION_CONTEXT ( 3 ) GLOBAL_UNCERTAINTY_ASSIGNED_CONTEXT ( ( #25316 ) ) GLOBAL_UNIT_ASSIGNED_CONTEXT ( ( #43659, #17127, #56342 ) ) REPRESENTATION_CONTEXT ( 'NONE', 'WORKASPACE' ) );
#34758=LINE ( 'NONE', #7878, #54688 ) ;
#34768=EDGE_LOOP ( 'NONE', ( #55233, #26712, #24484, #59977 ) ) ;
#34770=ORIENTED_EDGE ( 'NONE', *, *, #16809, .F. ) ;
#34775=VERTEX_POINT ( 'NONE', #28857 ) ;
#34778=ORIENTED_EDGE ( 'NONE', *, *, #10046, .T. ) ;
#34791=CARTESIAN_POINT ( 'NONE',  ( -11.50000000000000000, -11.50000000000000000, -15.00000000000000000 ) ) ;
#34792=LINE ( 'NONE', #34428, #23250 ) ;
#34797=CARTESIAN_POINT ( 'NONE',  ( 30.00000000000000000, -8.959999999999999076, -12.95475478405700009 ) ) ;
#34798=CARTESIAN_POINT ( 'NONE',  ( 30.00000000000000000, -11.50000000000082068, -10.20500000000000007 ) ) ;
#34805=PLANE ( 'NONE',  #39019 ) ;
#34813=EDGE_CURVE ( 'NONE', #40705, #20348, #34857, .T. ) ;
#34817=EDGE_LOOP ( 'NONE', ( #6067, #19635, #63190, #19472, #210 ) ) ;
#34821=CARTESIAN_POINT ( 'NONE',  ( -29.50000000000000355, -11.50000000000100009, -19.50000000000103739 ) ) ;
#34826=ORIENTED_EDGE ( 'NONE', *, *, #56999, .T. ) ;
#34838=EDGE_LOOP ( 'NONE', ( #59995, #23125, #53141, #27323, #480, #15139 ) ) ;
#34856=VECTOR ( 'NONE', #40900, 1000.000000000000114 ) ;
#34857=LINE ( 'NONE', #13998, #48117 ) ;
#34862=CARTESIAN_POINT ( 'NONE',  ( 25.50000000000000355, 0.000000000000000000, -22.50000000000000000 ) ) ;
#34865=CARTESIAN_POINT ( 'NONE',  ( 29.50000000000000355, -11.50000000000100009, 15.00000000000084910 ) ) ;
#34870=ORIENTED_EDGE ( 'NONE', *, *, #68785, .T. ) ;
#34873=CYLINDRICAL_SURFACE ( 'NONE', #59518, 1.621000000000000885 ) ;
#34881=DIRECTION ( 'NONE',  ( 0.000000000000000000, 1.000000000000000000, 0.000000000000000000 ) ) ;
#34891=DIRECTION ( 'NONE',  ( 0.000000000000000000, 0.000000000000000000, 1.000000000000000000 ) ) ;
#34892=DIRECTION ( 'NONE',  ( 0.000000000000000000, 1.000000000000000000, 0.000000000000000000 ) ) ;
#34894=LINE ( 'NONE', #2042, #16524 ) ;
#34906=CARTESIAN_POINT ( 'NONE',  ( 11.00000000000000000, -9.454754784057099570, 17.53999999999999915 ) ) ;
#34908=DIRECTION ( 'NONE',  ( -1.000000000000000000, 0.000000000000000000, 0.000000000000000000 ) ) ;
#34909=AXIS2_PLACEMENT_3D ( 'NONE', #35402, #27774, #56974 ) ;
#34915=ORIENTED_EDGE ( 'NONE', *, *, #28864, .T. ) ;
#34916=CARTESIAN_POINT ( 'NONE',  ( 11.50000000000000000, -11.50000000000100009, 19.50000000000103739 ) ) ;
#34941=ORIENTED_EDGE ( 'NONE', *, *, #13749, .T. ) ;
#34948=DIRECTION ( 'NONE',  ( 0.000000000000000000, 0.000000000000000000, -1.000000000000000000 ) ) ;
#34950=ADVANCED_FACE ( 'NONE', ( #42273 ), #63850, .F. ) ;
#34953=CIRCLE ( 'NONE', #48570, 4.000000000000000888 ) ;
#34961=EDGE_CURVE ( 'NONE', #47101, #32931, #60517, .T. ) ;
#34963=CONICAL_SURFACE ( 'NONE', #23663, 1.621000000000000885, 0.7853981633974518317 ) ;
#34969=FACE_OUTER_BOUND ( 'NONE', #54177, .T. ) ;
#34971=ORIENTED_EDGE ( 'NONE', *, *, #31980, .T. ) ;
#34975=CARTESIAN_POINT ( 'NONE',  ( 23.48000000000000043, -15.50000000000000000, -26.00000000000000355 ) ) ;
#34982=ORIENTED_EDGE ( 'NONE', *, *, #23779, .T. ) ;
#34983=LINE ( 'NONE', #29328, #56863 ) ;
#34986=DIRECTION ( 'NONE',  ( 0.000000000000000000, -0.7084617869615142949, -0.7057491738679528837 ) ) ;
#35000=DIRECTION ( 'NONE',  ( 0.000000000000000000, -1.000000000000000000, 0.000000000000000000 ) ) ;
#35003=DIRECTION ( 'NONE',  ( -1.000000000000000000, 0.000000000000000000, 0.000000000000000000 ) ) ;
#35005=EDGE_LOOP ( 'NONE', ( #20515, #25267, #46815, #65921 ) ) ;
#35009=CARTESIAN_POINT ( 'NONE',  ( 29.50000000000000355, -11.50000000000000000, 15.00000000000000000 ) ) ;
#35015=CYLINDRICAL_SURFACE ( 'NONE', #48110, 4.500000000000189182 ) ;
#35020=ORIENTED_EDGE ( 'NONE', *, *, #47527, .T. ) ;
#35022=ORIENTED_EDGE ( 'NONE', *, *, #41907, .F. ) ;
#35038=ADVANCED_FACE ( 'NONE', ( #43678 ), #22794, .F. ) ;
#35039=CYLINDRICAL_SURFACE ( 'NONE', #21486, 3.499999999999999556 ) ;
#35041=ORIENTED_EDGE ( 'NONE', *, *, #9106, .T. ) ;
#35047=CIRCLE ( 'NONE', #41830, 1.620999999999997332 ) ;
#35054=EDGE_CURVE ( 'NONE', #18955, #57411, #56027, .T. ) ;
#35060=ORIENTED_EDGE ( 'NONE', *, *, #6013, .T. ) ;
#35062=CARTESIAN_POINT ( 'NONE',  ( 14.25000000000000000, -2.500000000000000000, -23.22168783648699986 ) ) ;
#35073=EDGE_CURVE ( 'NONE', #33396, #14490, #27063, .T. ) ;
#35078=EDGE_CURVE ( 'NONE', #32135, #47415, #54994, .T. ) ;
#35080=FACE_OUTER_BOUND ( 'NONE', #9834, .T. ) ;
#35081=PLANE ( 'NONE',  #65836 ) ;
#35083=DIRECTION ( 'NONE',  ( 1.000000000000000000, -0.000000000000000000, -0.000000000000000000 ) ) ;
#35089=DIRECTION ( 'NONE',  ( 0.000000000000000000, 0.000000000000000000, 1.000000000000000000 ) ) ;
#35097=VECTOR ( 'NONE', #14839, 1000.000000000000000 ) ;
#35100=ORIENTED_EDGE ( 'NONE', *, *, #34107, .F. ) ;
#35103=AXIS2_PLACEMENT_3D ( 'NONE', #67726, #67026, #68434 ) ;
#35115=CARTESIAN_POINT ( 'NONE',  ( -15.50000000000000000, -5.000000000000000000, -22.50000000000000000 ) ) ;
#35117=ORIENTED_EDGE ( 'NONE', *, *, #16313, .F. ) ;
#35118=EDGE_CURVE ( 'NONE', #15458, #14694, #16105, .T. ) ;
#35119=CARTESIAN_POINT ( 'NONE',  ( 11.00000000000000000, -17.14999999999900027, 27.00000000000000000 ) ) ;
#35121=ORIENTED_EDGE ( 'NONE', *, *, #38569, .T. ) ;
#35146=CARTESIAN_POINT ( 'NONE',  ( 30.00000000000000000, -9.487228132326899654, 12.50000000000000000 ) ) ;
#35157=DIRECTION ( 'NONE',  ( -1.000000000000000000, 0.000000000000000000, 0.000000000000000000 ) ) ;
#35160=EDGE_CURVE ( 'NONE', #39463, #4089, #66957, .T. ) ;
#35164=VERTEX_POINT ( 'NONE', #61654 ) ;
#35167=DIRECTION ( 'NONE',  ( 1.000000000000000000, -0.000000000000000000, -0.000000000000000000 ) ) ;
#35183=CARTESIAN_POINT ( 'NONE',  ( 22.14589803375000088, -15.50000000000000000, 21.50000000000000000 ) ) ;
#35190=CYLINDRICAL_SURFACE ( 'NONE', #34603, 3.499999999999850342 ) ;
#35191=PLANE ( 'NONE',  #42914 ) ;
#35213=DIRECTION ( 'NONE',  ( -1.000000000000000000, 0.000000000000000000, 0.000000000000000000 ) ) ;
#35215=PLANE ( 'NONE',  #61354 ) ;
#35223=DIRECTION ( 'NONE',  ( 0.000000000000000000, 0.000000000000000000, 1.000000000000000000 ) ) ;
#35230=CARTESIAN_POINT ( 'NONE',  ( 15.50000000000000000, -1.037157890325000054, -26.50000000000000000 ) ) ;
#35234=ORIENTED_EDGE ( 'NONE', *, *, #64801, .F. ) ;
#35235=CARTESIAN_POINT ( 'NONE',  ( 30.00000000000000000, -11.70000000000012008, 10.70000000000011831 ) ) ;
#35249=DIRECTION ( 'NONE',  ( -1.000000000000000000, 0.000000000000000000, 0.000000000000000000 ) ) ;
#35256=ADVANCED_FACE ( 'NONE', ( #32888 ), #42801, .F. ) ;
#35262=ORIENTED_EDGE ( 'NONE', *, *, #27070, .T. ) ;
#35263=CARTESIAN_POINT ( 'NONE',  ( -11.00000000000000000, -11.70000000000000284, 12.50000000000000000 ) ) ;
#35270=CARTESIAN_POINT ( 'NONE',  ( -11.50000000000000000, -12.00000000000000000, 11.03137303340310282 ) ) ;
#35277=ORIENTED_EDGE ( 'NONE', *, *, #17948, .F. ) ;
#35279=DIRECTION ( 'NONE',  ( 0.000000000000000000, -1.000000000000000000, 0.000000000000000000 ) ) ;
#35281=EDGE_CURVE ( 'NONE', #48070, #2815, #53425, .T. ) ;
#35283=ADVANCED_FACE ( 'NONE', ( #21591 ), #64045, .T. ) ;
#35284=EDGE_LOOP ( 'NONE', ( #10009, #54276, #3186, #65665, #17666, #17780 ) ) ;
#35293=CARTESIAN_POINT ( 'NONE',  ( 17.00000000000000000, -15.50000000000000000, 14.50000000000000000 ) ) ;
#35296=AXIS2_PLACEMENT_3D ( 'NONE', #61793, #13353, #14043 ) ;
#35298=CARTESIAN_POINT ( 'NONE',  ( 30.00000000000000000, -16.28999999999999915, -14.50000000000000000 ) ) ;
#35302=VERTEX_POINT ( 'NONE', #4978 ) ;
#35307=CARTESIAN_POINT ( 'NONE',  ( 30.00000000000000000, -9.199999999999999289, -12.34999999999989839 ) ) ;
#35315=CYLINDRICAL_SURFACE ( 'NONE', #63852, 4.000000000000000000 ) ;
#35323=PLANE ( 'NONE',  #20735 ) ;
#35338=ORIENTED_EDGE ( 'NONE', *, *, #42090, .F. ) ;
#35341=EDGE_CURVE ( 'NONE', #41169, #27481, #16278, .T. ) ;
#35350=CONICAL_SURFACE ( 'NONE', #13867, 1732.050807568785558, 1.047197551196574761 ) ;
#35351=CARTESIAN_POINT ( 'NONE',  ( 25.50000000000000355, -15.50000000000000000, 22.50000000000000000 ) ) ;
#35365=EDGE_CURVE ( 'NONE', #13975, #23202, #69327, .T. ) ;
#35366=VERTEX_POINT ( 'NONE', #10981 ) ;
#35368=EDGE_CURVE ( 'NONE', #62314, #4508, #54122, .T. ) ;
#35380=DIRECTION ( 'NONE',  ( 0.000000000000000000, 0.7084617869628681008, -0.7057491738665939707 ) ) ;
#35386=LINE ( 'NONE', #29739, #10238 ) ;
#35391=AXIS2_PLACEMENT_3D ( 'NONE', #56737, #35157, #28809 ) ;
#35393=ORIENTED_EDGE ( 'NONE', *, *, #68265, .F. ) ;
#35399=LINE ( 'NONE', #67243, #3044 ) ;
#35402=CARTESIAN_POINT ( 'NONE',  ( 11.50000000000000000, -11.50000000000100009, 15.00000000000084910 ) ) ;
#35407=DIRECTION ( 'NONE',  ( 0.4999999999999827360, 0.000000000000000000, -0.8660254037844485886 ) ) ;
#35408=AXIS2_PLACEMENT_3D ( 'NONE', #13775, #45957, #12710 ) ;
#35410=CARTESIAN_POINT ( 'NONE',  ( 30.00000000000000000, -15.46862696659690073, 14.50000000000000000 ) ) ;
#35414=DIRECTION ( 'NONE',  ( 1.000000000000000000, 0.000000000000000000, 0.000000000000000000 ) ) ;
#35415=AXIS2_PLACEMENT_3D ( 'NONE', #46278, #67853, #56539 ) ;
#35416=ORIENTED_EDGE ( 'NONE', *, *, #57655, .F. ) ;
#35418=CARTESIAN_POINT ( 'NONE',  ( 11.75000000000000000, -5.200000000000001066, 60.00000000000000000 ) ) ;
#35419=EDGE_LOOP ( 'NONE', ( #23141, #45943, #49029, #40580 ) ) ;
#35420=ADVANCED_FACE ( 'NONE', ( #11647 ), #55152, .T. ) ;
#35424=CARTESIAN_POINT ( 'NONE',  ( -17.51999999999999957, -15.50000000000000000, 26.00000000000000355 ) ) ;
#35427=ORIENTED_EDGE ( 'NONE', *, *, #46913, .T. ) ;
#35428=ADVANCED_FACE ( 'NONE', ( #56189 ), #44514, .F. ) ;
#35430=CYLINDRICAL_SURFACE ( 'NONE', #57272, 0.3500000000009988455 ) ;
#35434=DIRECTION ( 'NONE',  ( 0.000000000000000000, 0.000000000000000000, 1.000000000000000000 ) ) ;
#35444=CARTESIAN_POINT ( 'NONE',  ( 15.50000000000129852, -15.50000000000000000, 22.50000000000000000 ) ) ;
#35454=EDGE_LOOP ( 'NONE', ( #17885, #23345, #62431, #53941 ) ) ;
#35455=CARTESIAN_POINT ( 'NONE',  ( 25.50000000000000355, -15.50000000000000000, -22.50000000000000000 ) ) ;
#35460=VERTEX_POINT ( 'NONE', #12333 ) ;
#35470=VERTEX_POINT ( 'NONE', #50180 ) ;
#35484=AXIS2_PLACEMENT_3D ( 'NONE', #29804, #51373, #2938 ) ;
#35489=ORIENTED_EDGE ( 'NONE', *, *, #31296, .T. ) ;
#35500=EDGE_CURVE ( 'NONE', #30976, #55205, #16977, .T. ) ;
#35503=DIRECTION ( 'NONE',  ( -1.000000000000000000, 0.000000000000000000, 0.000000000000000000 ) ) ;
#35506=CARTESIAN_POINT ( 'NONE',  ( 17.00000000000000000, -16.64230188589299786, -14.64519951917100116 ) ) ;
#35509=CARTESIAN_POINT ( 'NONE',  ( -15.50000000000000000, -2.500000000000000000, -23.94337567297399971 ) ) ;
#35514=CARTESIAN_POINT ( 'NONE',  ( -28.00000000000000000, -17.50000000000000000, 15.70499999999969809 ) ) ;
#35525=VERTEX_POINT ( 'NONE', #45927 ) ;
#35532=EDGE_LOOP ( 'NONE', ( #35338, #28039 ) ) ;
#35539=DIRECTION ( 'NONE',  ( -0.000000000000000000, 1.000000000000000000, -0.000000000000000000 ) ) ;
#35540=DIRECTION ( 'NONE',  ( 0.000000000000000000, 0.000000000000000000, 1.000000000000000000 ) ) ;
#35543=ORIENTED_EDGE ( 'NONE', *, *, #15594, .T. ) ;
#35545=FACE_OUTER_BOUND ( 'NONE', #67491, .T. ) ;
#35546=ORIENTED_EDGE ( 'NONE', *, *, #62930, .T. ) ;
#35547=AXIS2_PLACEMENT_3D ( 'NONE', #68412, #25274, #20318 ) ;
#35549=ORIENTED_EDGE ( 'NONE', *, *, #19474, .T. ) ;
#35550=EDGE_LOOP ( 'NONE', ( #54218, #23565, #24683, #68159 ) ) ;
#35551=CARTESIAN_POINT ( 'NONE',  ( 29.50000000000000355, -12.00000000000000000, 10.52786404500095863 ) ) ;
#35554=DIRECTION ( 'NONE',  ( 0.000000000000000000, 0.000000000000000000, -1.000000000000000000 ) ) ;
#35562=ORIENTED_EDGE ( 'NONE', *, *, #48521, .T. ) ;
#35564=AXIS2_PLACEMENT_3D ( 'NONE', #56851, #61825, #24339 ) ;
#35569=CIRCLE ( 'NONE', #68351, 1.620999999999997332 ) ;
#35574=ORIENTED_EDGE ( 'NONE', *, *, #16643, .F. ) ;
#35581=CARTESIAN_POINT ( 'NONE',  ( 16.75000000000000000, -2.500000000000000000, 21.77831216351300014 ) ) ;
#35584=FACE_OUTER_BOUND ( 'NONE', #60627, .T. ) ;
#35602=VERTEX_POINT ( 'NONE', #25063 ) ;
#35608=EDGE_CURVE ( 'NONE', #22607, #62442, #41667, .T. ) ;
#35609=CARTESIAN_POINT ( 'NONE',  ( -29.50000000000000355, -11.50000000000000000, 15.00000000000000000 ) ) ;
#35617=VERTEX_POINT ( 'NONE', #50870 ) ;
#35626=CARTESIAN_POINT ( 'NONE',  ( -30.00000000000000000, -14.33999999999999986, -14.50000000000000000 ) ) ;
#35640=DIRECTION ( 'NONE',  ( 0.000000000000000000, 0.000000000000000000, -1.000000000000000000 ) ) ;
#35644=EDGE_LOOP ( 'NONE', ( #31156, #13471 ) ) ;
#35650=CARTESIAN_POINT ( 'NONE',  ( -29.25000000000000000, -5.000000000000000000, 26.25000000000000000 ) ) ;
#35669=DIRECTION ( 'NONE',  ( 0.000000000000000000, 0.000000000000000000, -1.000000000000000000 ) ) ;
#35670=VECTOR ( 'NONE', #65918, 1000.000000000000000 ) ;
#35671=EDGE_CURVE ( 'NONE', #47415, #6609, #25778, .T. ) ;
#35675=DIRECTION ( 'NONE',  ( -1.000000000000000000, 0.000000000000000000, 0.000000000000000000 ) ) ;
#35677=CYLINDRICAL_SURFACE ( 'NONE', #23143, 3.499999999999850342 ) ;
#35678=ORIENTED_EDGE ( 'NONE', *, *, #18406, .T. ) ;
#35683=ORIENTED_EDGE ( 'NONE', *, *, #41686, .T. ) ;
#35701=EDGE_CURVE ( 'NONE', #46404, #3061, #7396, .T. ) ;
#35702=AXIS2_PLACEMENT_3D ( 'NONE', #21378, #22081, #64523 ) ;
#35710=EDGE_LOOP ( 'NONE', ( #40378, #26188, #62026, #42208 ) ) ;
#35712=EDGE_CURVE ( 'NONE', #58904, #35825, #4896, .T. ) ;
#35714=ORIENTED_EDGE ( 'NONE', *, *, #66446, .T. ) ;
#35720=DIRECTION ( 'NONE',  ( 0.000000000000000000, 1.000000000000000000, 0.000000000000000000 ) ) ;
#35725=AXIS2_PLACEMENT_3D ( 'NONE', #51292, #18768, #45991 ) ;
#35730=DIRECTION ( 'NONE',  ( 0.000000000000000000, 0.000000000000000000, 1.000000000000000000 ) ) ;
#35741=DIRECTION ( 'NONE',  ( 0.000000000000000000, 0.7071067811865496822, -0.7071067811865454633 ) ) ;
#35745=CARTESIAN_POINT ( 'NONE',  ( 29.25000000000000000, -5.200000000000001066, 11.75000000000000000 ) ) ;
#35746=DIRECTION ( 'NONE',  ( -0.000000000000000000, 1.000000000000000000, -0.000000000000000000 ) ) ;
#35753=ORIENTED_EDGE ( 'NONE', *, *, #22456, .F. ) ;
#35754=CARTESIAN_POINT ( 'NONE',  ( -11.00000000000000000, -13.54524521594299991, 17.53999999999999915 ) ) ;
#35756=VECTOR ( 'NONE', #57498, 1000.000000000000000 ) ;
#35761=AXIS2_PLACEMENT_3D ( 'NONE', #19071, #55517, #23334 ) ;
#35766=CARTESIAN_POINT ( 'NONE',  ( -29.50000000000000355, -11.50000000000100009, 15.00000000000084910 ) ) ;
#35767=FACE_OUTER_BOUND ( 'NONE', #14354, .T. ) ;
#35771=FACE_OUTER_BOUND ( 'NONE', #30898, .T. ) ;
#35772=DIRECTION ( 'NONE',  ( 0.000000000000000000, 0.000000000000000000, 1.000000000000000000 ) ) ;
#35774=LINE ( 'NONE', #47095, #56628 ) ;
#35777=VERTEX_POINT ( 'NONE', #42716 ) ;
#35786=ORIENTED_EDGE ( 'NONE', *, *, #24133, .F. ) ;
#35804=DIRECTION ( 'NONE',  ( -1.000000000000000000, 0.000000000000000000, 0.000000000000000000 ) ) ;
#35808=DIRECTION ( 'NONE',  ( -1.000000000000000000, 0.000000000000000000, 0.000000000000000000 ) ) ;
#35813=VECTOR ( 'NONE', #31066, 1000.000000000000000 ) ;
#35814=AXIS2_PLACEMENT_3D ( 'NONE', #21518, #16572, #48395 ) ;
#35825=VERTEX_POINT ( 'NONE', #15850 ) ;
#35831=VERTEX_POINT ( 'NONE', #37425 ) ;
#35846=DIRECTION ( 'NONE',  ( 0.000000000000000000, -0.7046037717806115097, -0.7096009616626348659 ) ) ;
#35849=CYLINDRICAL_SURFACE ( 'NONE', #34537, 0.5000000000079367624 ) ;
#35868=AXIS2_PLACEMENT_3D ( 'NONE', #27847, #16890, #64631 ) ;
#35869=AXIS2_PLACEMENT_3D ( 'NONE', #62449, #24993, #26055 ) ;
#35877=VERTEX_POINT ( 'NONE', #2009 ) ;
#35880=CARTESIAN_POINT ( 'NONE',  ( -11.00000000000000000, -17.50000000000000000, -15.70500000000000007 ) ) ;
#35886=ORIENTED_EDGE ( 'NONE', *, *, #38386, .F. ) ;
#35894=ORIENTED_EDGE ( 'NONE', *, *, #17650, .F. ) ;
#35899=LINE ( 'NONE', #57454, #22593 ) ;
#35902=ORIENTED_EDGE ( 'NONE', *, *, #3455, .F. ) ;
#35907=VERTEX_POINT ( 'NONE', #45125 ) ;
#35915=ORIENTED_EDGE ( 'NONE', *, *, #17808, .T. ) ;
#35924=CARTESIAN_POINT ( 'NONE',  ( -25.50000000000000355, -15.12100000000000044, -20.87900000000000134 ) ) ;
#35926=CIRCLE ( 'NONE', #52912, 3.300000002979700753 ) ;
#35933=CIRCLE ( 'NONE', #66409, 0.5000000000079367624 ) ;
#35939=CARTESIAN_POINT ( 'NONE',  ( 28.00000000000000000, -17.35230188589299871, 15.35019951917099945 ) ) ;
#35944=ORIENTED_EDGE ( 'NONE', *, *, #65826, .F. ) ;
#35945=CARTESIAN_POINT ( 'NONE',  ( 15.50000000000000000, -5.000000000000000000, -22.50000000000000000 ) ) ;
#35959=ORIENTED_EDGE ( 'NONE', *, *, #15237, .T. ) ;
#35971=ADVANCED_FACE ( 'NONE', ( #61382 ), #40876, .F. ) ;
#35972=ORIENTED_EDGE ( 'NONE', *, *, #13190, .F. ) ;
#35979=LINE ( 'NONE', #23368, #2452 ) ;
#35982=EDGE_LOOP ( 'NONE', ( #30839, #59570, #41389, #16336 ) ) ;
#35985=ORIENTED_EDGE ( 'NONE', *, *, #46134, .F. ) ;
#35988=PLANE ( 'NONE',  #47153 ) ;
#36000=DIRECTION ( 'NONE',  ( 0.000000000000000000, 0.6857142857146703019, -0.7278708115914659382 ) ) ;
#36001=ORIENTED_EDGE ( 'NONE', *, *, #50264, .T. ) ;
#36018=AXIS2_PLACEMENT_3D ( 'NONE', #36880, #59127, #36505 ) ;
#36021=CARTESIAN_POINT ( 'NONE',  ( 11.00000000000000000, -11.50000000000000000, 15.00000000000000000 ) ) ;
#36027=LINE ( 'NONE', #46282, #39776 ) ;
#36036=AXIS2_PLACEMENT_3D ( 'NONE', #50783, #46182, #61381 ) ;
#36049=DIRECTION ( 'NONE',  ( -1.000000000000000000, 0.000000000000000000, 0.000000000000000000 ) ) ;
#36052=EDGE_LOOP ( 'NONE', ( #774, #34770, #40396, #952 ) ) ;
#36059=EDGE_CURVE ( 'NONE', #47155, #7800, #3408, .T. ) ;
#36062=CARTESIAN_POINT ( 'NONE',  ( -11.50000000000000000, -11.50000000000100009, -15.00000000000084910 ) ) ;
#36064=ORIENTED_EDGE ( 'NONE', *, *, #28571, .T. ) ;
#36073=LINE ( 'NONE', #29711, #10544 ) ;
#36074=ORIENTED_EDGE ( 'NONE', *, *, #4196, .T. ) ;
#36080=CARTESIAN_POINT ( 'NONE',  ( -15.50000000000000000, 998.9628421096749662, -22.50000000000000000 ) ) ;
#36096=ORIENTED_EDGE ( 'NONE', *, *, #54295, .T. ) ;
#36113=CARTESIAN_POINT ( 'NONE',  ( -11.00000000000000000, -11.85423089348099879, 9.852125413066602277 ) ) ;
#36127=LINE ( 'NONE', #30830, #24919 ) ;
#36129=CARTESIAN_POINT ( 'NONE',  ( 30.00000000000000000, -5.200000000000001066, 11.75000000000000000 ) ) ;
#36131=VECTOR ( 'NONE', #4339, 1000.000000000000000 ) ;
#36132=DIRECTION ( 'NONE',  ( -1.000000000000000000, 0.000000000000000000, 0.000000000000000000 ) ) ;
#36135=ORIENTED_EDGE ( 'NONE', *, *, #43405, .F. ) ;
#36140=VECTOR ( 'NONE', #26355, 1000.000000000000000 ) ;
#36141=CARTESIAN_POINT ( 'NONE',  ( -11.50000000000000000, -11.50000000000000000, 15.00000000000000000 ) ) ;
#36144=DIRECTION ( 'NONE',  ( 0.000000000000000000, 0.000000000000000000, -1.000000000000000000 ) ) ;
#36146=ORIENTED_EDGE ( 'NONE', *, *, #65826, .T. ) ;
#36155=DIRECTION ( 'NONE',  ( 0.000000000000000000, 0.000000000000000000, 1.000000000000000000 ) ) ;
#36160=ORIENTED_EDGE ( 'NONE', *, *, #17801, .T. ) ;
#36162=ORIENTED_EDGE ( 'NONE', *, *, #14652, .F. ) ;
#36163=ADVANCED_FACE ( 'NONE', ( #27069 ), #63861, .F. ) ;
#36164=DIRECTION ( 'NONE',  ( -0.000000000000000000, 1.000000000000000000, -0.000000000000000000 ) ) ;
#36166=VECTOR ( 'NONE', #43842, 1000.000000000000114 ) ;
#36167=CARTESIAN_POINT ( 'NONE',  ( -16.33757311576526305, -0.3152598339554828488, 23.45980260912095616 ) ) ;
#36170=EDGE_LOOP ( 'NONE', ( #25807, #2525, #15632, #44421 ) ) ;
#36184=ORIENTED_EDGE ( 'NONE', *, *, #61539, .F. ) ;
#36188=CARTESIAN_POINT ( 'NONE',  ( 18.85410196625000268, -17.50000000000000000, 21.50000000000000000 ) ) ;
#36191=VERTEX_POINT ( 'NONE', #5512 ) ;
#36192=VECTOR ( 'NONE', #26919, 1000.000000000000000 ) ;
#36193=CARTESIAN_POINT ( 'NONE',  ( 15.29686605390242704, -0.2715358723600077573, 21.17390376548697972 ) ) ;
#36194=VECTOR ( 'NONE', #40787, 1000.000000000000000 ) ;
#36213=AXIS2_PLACEMENT_3D ( 'NONE', #15519, #22468, #69604 ) ;
#36214=CARTESIAN_POINT ( 'NONE',  ( -15.50000000000000000, -2.500000000000000000, -21.05662432702600029 ) ) ;
#36217=EDGE_LOOP ( 'NONE', ( #60575, #39939, #2075, #68057 ) ) ;
#36242=AXIS2_PLACEMENT_3D ( 'NONE', #22557, #17236, #60364 ) ;
#36245=EDGE_CURVE ( 'NONE', #57618, #49327, #11830, .T. ) ;
#36258=CYLINDRICAL_SURFACE ( 'NONE', #26757, 0.5000000000079367624 ) ;
#36267=VERTEX_POINT ( 'NONE', #6876 ) ;
#36268=CARTESIAN_POINT ( 'NONE',  ( 11.00000000000000000, -11.50000000000100009, -10.50000000000065903 ) ) ;
#36277=ORIENTED_EDGE ( 'NONE', *, *, #24666, .T. ) ;
#36278=CIRCLE ( 'NONE', #13556, 4.000000000000001776 ) ;
#36280=EDGE_CURVE ( 'NONE', #43574, #33481, #17488, .T. ) ;
#36282=CIRCLE ( 'NONE', #47591, 1.449999999999996403 ) ;
#36286=ORIENTED_EDGE ( 'NONE', *, *, #16812, .T. ) ;
#36304=DIRECTION ( 'NONE',  ( -0.9375000000000006661, 0.000000000000000000, 0.3479852726768744020 ) ) ;
#36317=ADVANCED_FACE ( 'NONE', ( #12182 ), #22116, .F. ) ;
#36332=EDGE_LOOP ( 'NONE', ( #68981, #61469 ) ) ;
#36334=ORIENTED_EDGE ( 'NONE', *, *, #54722, .F. ) ;
#36335=EDGE_LOOP ( 'NONE', ( #44069, #36877, #42672, #49596 ) ) ;
#36341=CIRCLE ( 'NONE', #29610, 3.499999999999849454 ) ;
#36345=CARTESIAN_POINT ( 'NONE',  ( 30.00000000000000000, -5.599999999999999645, -27.00000000000000000 ) ) ;
#36355=VECTOR ( 'NONE', #23490, 1000.000000000000000 ) ;
#36361=CARTESIAN_POINT ( 'NONE',  ( 22.14589803375000088, -15.50000000000000000, -21.50000000000000000 ) ) ;
#36365=ADVANCED_FACE ( 'NONE', ( #12863 ), #24551, .F. ) ;
#36366=ORIENTED_EDGE ( 'NONE', *, *, #58715, .T. ) ;
#36367=EDGE_CURVE ( 'NONE', #27925, #25470, #49224, .T. ) ;
#36370=CARTESIAN_POINT ( 'NONE',  ( -25.50000000000000355, -5.200000000000001066, 22.50000000000000000 ) ) ;
#36380=CARTESIAN_POINT ( 'NONE',  ( -15.50000000000000000, -0.4000000000000000222, 22.50000000000000000 ) ) ;
#36392=VECTOR ( 'NONE', #22232, 1000.000000000000000 ) ;
#36393=DIRECTION ( 'NONE',  ( 0.000000000000000000, 0.000000000000000000, 1.000000000000000000 ) ) ;
#36395=PLANE ( 'NONE',  #27554 ) ;
#36401=FACE_OUTER_BOUND ( 'NONE', #59062, .T. ) ;
#36402=EDGE_CURVE ( 'NONE', #54090, #49938, #34792, .T. ) ;
#36406=ORIENTED_EDGE ( 'NONE', *, *, #28485, .T. ) ;
#36411=DIRECTION ( 'NONE',  ( 0.000000000000000000, 0.000000000000000000, 1.000000000000000000 ) ) ;
#36416=CARTESIAN_POINT ( 'NONE',  ( 25.50000000000000355, 0.000000000000000000, 22.50000000000000000 ) ) ;
#36420=ADVANCED_FACE ( 'NONE', ( #18894 ), #41149, .F. ) ;
#36423=ORIENTED_EDGE ( 'NONE', *, *, #44320, .F. ) ;
#36426=DIRECTION ( 'NONE',  ( 0.000000000000000000, 0.000000000000000000, 1.000000000000000000 ) ) ;
#36427=CARTESIAN_POINT ( 'NONE',  ( -11.00000000000000000, -11.10796162543699950, -9.102987789146602893 ) ) ;
#36445=DIRECTION ( 'NONE',  ( 0.000000000000000000, 1.000000000000000000, 0.000000000000000000 ) ) ;
#36450=DIRECTION ( 'NONE',  ( -1.000000000000000000, 0.000000000000000000, 0.000000000000000000 ) ) ;
#36452=ADVANCED_FACE ( 'NONE', ( #13931 ), #8628, .T. ) ;
#36470=VERTEX_POINT ( 'NONE', #37611 ) ;
#36475=CARTESIAN_POINT ( 'NONE',  ( -11.00000000000000000, -11.10796162543699950, 9.102987789146602893 ) ) ;
#36482=ORIENTED_EDGE ( 'NONE', *, *, #56447, .T. ) ;
#36490=ORIENTED_EDGE ( 'NONE', *, *, #31211, .F. ) ;
#36499=ORIENTED_EDGE ( 'NONE', *, *, #33828, .T. ) ;
#36502=DIRECTION ( 'NONE',  ( 0.000000000000000000, 1.000000000000000000, 0.000000000000000000 ) ) ;
#36504=ORIENTED_EDGE ( 'NONE', *, *, #4293, .T. ) ;
#36505=DIRECTION ( 'NONE',  ( 0.000000000000000000, 0.000000000000000000, 1.000000000000000000 ) ) ;
#36517=CARTESIAN_POINT ( 'NONE',  ( -25.49999999999869971, -15.50000000000000000, -22.50000000000000000 ) ) ;
#36518=CIRCLE ( 'NONE', #15071, 3.499999999999999556 ) ;
#36526=VECTOR ( 'NONE', #45901, 1000.000000000000000 ) ;
#36530=CARTESIAN_POINT ( 'NONE',  ( -17.24945551514599984, -15.50000000000000000, 25.53140320652400064 ) ) ;
#36545=ORIENTED_EDGE ( 'NONE', *, *, #55332, .F. ) ;
#36551=EDGE_CURVE ( 'NONE', #44628, #21397, #47173, .T. ) ;
#36554=ORIENTED_EDGE ( 'NONE', *, *, #49780, .T. ) ;
#36557=CARTESIAN_POINT ( 'NONE',  ( -16.75000000000000000, -2.500000000000000000, -21.77831216351300014 ) ) ;
#36558=DIRECTION ( 'NONE',  ( 0.000000000000000000, 1.000000000000000000, 0.000000000000000000 ) ) ;
#36566=LINE ( 'NONE', #31291, #48563 ) ;
#36571=AXIS2_PLACEMENT_3D ( 'NONE', #62740, #8995, #52496 ) ;
#36575=DIRECTION ( 'NONE',  ( 0.000000000000000000, 0.000000000000000000, -1.000000000000000000 ) ) ;
#36577=FACE_OUTER_BOUND ( 'NONE', #19228, .T. ) ;
#36578=CYLINDRICAL_SURFACE ( 'NONE', #55716, 4.000000000000000000 ) ;
#36580=ORIENTED_EDGE ( 'NONE', *, *, #21988, .F. ) ;
#36588=CARTESIAN_POINT ( 'NONE',  ( 11.50000000000000000, -11.50000000000000000, 11.00000000000000000 ) ) ;
#36594=CARTESIAN_POINT ( 'NONE',  ( -11.75000000000000000, -5.000000000000000000, -23.89194109070750471 ) ) ;
#36597=ORIENTED_EDGE ( 'NONE', *, *, #51834, .T. ) ;
#36601=ORIENTED_EDGE ( 'NONE', *, *, #49305, .T. ) ;
#36607=ORIENTED_EDGE ( 'NONE', *, *, #14252, .T. ) ;
#36609=CARTESIAN_POINT ( 'NONE',  ( 15.50000000000000000, -0.2038245569916610489, 21.05662432702600029 ) ) ;
#36611=CARTESIAN_POINT ( 'NONE',  ( 17.24945551514599984, -17.50000000000000000, 25.53140320652400064 ) ) ;
#36618=FACE_OUTER_BOUND ( 'NONE', #35005, .T. ) ;
#36622=EDGE_CURVE ( 'NONE', #14877, #66251, #6362, .T. ) ;
#36624=EDGE_LOOP ( 'NONE', ( #4794, #61379, #52096, #51199 ) ) ;
#36641=CIRCLE ( 'NONE', #63765, 0.5000000000001357803 ) ;
#36647=CARTESIAN_POINT ( 'NONE',  ( -30.00000000000000000, -5.599999999999999645, 9.000000000000001776 ) ) ;
#36655=DIRECTION ( 'NONE',  ( 0.000000000000000000, 0.000000000000000000, 1.000000000000000000 ) ) ;
#36658=CIRCLE ( 'NONE', #6180, 3.499999999999040323 ) ;
#36663=CARTESIAN_POINT ( 'NONE',  ( 14.66242688423474583, -0.3152598339554803508, 23.45980260912095616 ) ) ;
#36666=DIRECTION ( 'NONE',  ( -1.000000000000000000, 0.000000000000000000, 0.000000000000000000 ) ) ;
#36669=DIRECTION ( 'NONE',  ( 0.000000000000000000, -0.1111111111108840643, -0.9938079899999319178 ) ) ;
#36675=ORIENTED_EDGE ( 'NONE', *, *, #40958, .T. ) ;
#36678=CARTESIAN_POINT ( 'NONE',  ( -15.08757311576351690, -0.3152598339557960427, 23.70526090033903444 ) ) ;
#36683=CARTESIAN_POINT ( 'NONE',  ( 11.00000000000000000, -17.50000000000000000, 60.00000000000000000 ) ) ;
#36688=VERTEX_POINT ( 'NONE', #1165 ) ;
#36692=EDGE_CURVE ( 'NONE', #1993, #69377, #53497, .T. ) ;
#36693=DIRECTION ( 'NONE',  ( 0.000000000000000000, -1.000000000000000000, 0.000000000000000000 ) ) ;
#36695=AXIS2_PLACEMENT_3D ( 'NONE', #36845, #11336, #15626 ) ;
#36709=AXIS2_PLACEMENT_3D ( 'NONE', #63986, #58331, #53374 ) ;
#36710=FACE_BOUND ( 'NONE', #7913, .T. ) ;
#36721=ORIENTED_EDGE ( 'NONE', *, *, #39298, .T. ) ;
#36723=FACE_OUTER_BOUND ( 'NONE', #57666, .T. ) ;
#36725=DIRECTION ( 'NONE',  ( -1.000000000000000000, 0.000000000000000000, 0.000000000000000000 ) ) ;
#36732=CARTESIAN_POINT ( 'NONE',  ( 17.00000000000000000, -16.28999999999999915, 14.50000000000000000 ) ) ;
#36738=CIRCLE ( 'NONE', #35547, 0.5000000000079367624 ) ;
#36740=LINE ( 'NONE', #37096, #13672 ) ;
#36746=LINE ( 'NONE', #53705, #10192 ) ;
#36747=CYLINDRICAL_SURFACE ( 'NONE', #10792, 3.499999999999853895 ) ;
#36748=VERTEX_POINT ( 'NONE', #24464 ) ;
#36751=VECTOR ( 'NONE', #63222, 1000.000000000000000 ) ;
#36758=CIRCLE ( 'NONE', #68344, 0.5000000000001362244 ) ;
#36769=CARTESIAN_POINT ( 'NONE',  ( -16.75000000000000000, -2.500000000000000000, 23.22168783648699986 ) ) ;
#36770=FACE_OUTER_BOUND ( 'NONE', #67355, .T. ) ;
#36771=EDGE_CURVE ( 'NONE', #35602, #56028, #66879, .T. ) ;
#36772=DIRECTION ( 'NONE',  ( 1.000000000000000000, 0.000000000000000000, 0.000000000000000000 ) ) ;
#36784=ORIENTED_EDGE ( 'NONE', *, *, #67406, .T. ) ;
#36791=DIRECTION ( 'NONE',  ( 0.000000000000000000, -0.1111111111108840643, -0.9938079899999319178 ) ) ;
#36792=CARTESIAN_POINT ( 'NONE',  ( -30.00000000000000000, -11.50000000000100009, 15.00000000000084910 ) ) ;
#36793=CIRCLE ( 'NONE', #54851, 3.499999999999056310 ) ;
#36801=VECTOR ( 'NONE', #51182, 1000.000000000000000 ) ;
#36805=AXIS2_PLACEMENT_3D ( 'NONE', #34075, #40794, #4387 ) ;
#36811=AXIS2_PLACEMENT_3D ( 'NONE', #44064, #5902, #6594 ) ;
#36815=VERTEX_POINT ( 'NONE', #13140 ) ;
#36816=ORIENTED_EDGE ( 'NONE', *, *, #69354, .F. ) ;
#36817=LINE ( 'NONE', #59418, #29676 ) ;
#36820=ORIENTED_EDGE ( 'NONE', *, *, #63392, .T. ) ;
#36825=ORIENTED_EDGE ( 'NONE', *, *, #14521, .F. ) ;
#36837=EDGE_CURVE ( 'NONE', #43499, #21463, #50979, .T. ) ;
#36841=DIRECTION ( 'NONE',  ( 0.000000000000000000, 0.000000000000000000, 1.000000000000000000 ) ) ;
#36844=ORIENTED_EDGE ( 'NONE', *, *, #57211, .F. ) ;
#36845=CARTESIAN_POINT ( 'NONE',  ( 30.00000000000000000, -9.200000000000120082, 17.30000000000000071 ) ) ;
#36850=CIRCLE ( 'NONE', #25534, 0.4999999999991867061 ) ;
#36854=EDGE_LOOP ( 'NONE', ( #8500, #25720 ) ) ;
#36856=AXIS2_PLACEMENT_3D ( 'NONE', #60577, #49960, #1521 ) ;
#36860=CIRCLE ( 'NONE', #48156, 4.000000000000000888 ) ;
#36868=FACE_OUTER_BOUND ( 'NONE', #57245, .T. ) ;
#36877=ORIENTED_EDGE ( 'NONE', *, *, #39736, .F. ) ;
#36879=AXIS2_PLACEMENT_3D ( 'NONE', #51058, #7573, #45393 ) ;
#36880=CARTESIAN_POINT ( 'NONE',  ( 25.50000000000000355, -5.578999999999999737, 22.50000000000000000 ) ) ;
#36882=CARTESIAN_POINT ( 'NONE',  ( -15.50000000000000000, -5.000000000000000000, 22.50000000000000000 ) ) ;
#36886=DIRECTION ( 'NONE',  ( -1.000000000000000000, 0.000000000000000000, 0.000000000000000000 ) ) ;
#36889=ORIENTED_EDGE ( 'NONE', *, *, #19087, .F. ) ;
#36899=VERTEX_POINT ( 'NONE', #3597 ) ;
#36901=DIRECTION ( 'NONE',  ( -1.000000000000000000, 0.000000000000000000, 0.000000000000000000 ) ) ;
#36911=EDGE_CURVE ( 'NONE', #68975, #52878, #41762, .T. ) ;
#36917=EDGE_LOOP ( 'NONE', ( #67476, #3908, #53847, #35902 ) ) ;
#36921=CARTESIAN_POINT ( 'NONE',  ( 15.08757311576526128, -0.3152598339554890106, 21.29473909965996015 ) ) ;
#36924=DIRECTION ( 'NONE',  ( -1.000000000000000000, 0.000000000000000000, 0.000000000000000000 ) ) ;
#36936=DIRECTION ( 'NONE',  ( 0.000000000000000000, 0.000000000000000000, 1.000000000000000000 ) ) ;
#36953=DIRECTION ( 'NONE',  ( 0.000000000000000000, -0.7084617869623469621, -0.7057491738671168857 ) ) ;
#36956=CARTESIAN_POINT ( 'NONE',  ( 11.50000000000000000, -11.50000000000000000, -15.00000000000000000 ) ) ;
#36958=VERTEX_POINT ( 'NONE', #41062 ) ;
#36959=CARTESIAN_POINT ( 'NONE',  ( 30.00000000000000000, -14.04000000000000092, -17.04524521594300523 ) ) ;
#36969=ADVANCED_FACE ( 'NONE', ( #9962 ), #52386, .F. ) ;
#36973=VERTEX_POINT ( 'NONE', #8890 ) ;
#36980=AXIS2_PLACEMENT_3D ( 'NONE', #50550, #2451, #18011 ) ;
#36986=ORIENTED_EDGE ( 'NONE', *, *, #34009, .F. ) ;
#36987=VERTEX_POINT ( 'NONE', #63701 ) ;
#36991=CARTESIAN_POINT ( 'NONE',  ( 30.00000000000000000, -10.85999999999999943, 9.000000000000001776 ) ) ;
#37000=CARTESIAN_POINT ( 'NONE',  ( -28.00000000000000000, -17.50000000000000000, 15.70500000000000007 ) ) ;
#37017=EDGE_CURVE ( 'NONE', #32897, #34396, #4650, .T. ) ;
#37031=CARTESIAN_POINT ( 'NONE',  ( 11.75000000000000000, -5.000000000000000000, -21.10805890929250239 ) ) ;
#37036=CARTESIAN_POINT ( 'NONE',  ( -11.00000000000000000, -5.599999999999999645, -9.000000000000001776 ) ) ;
#37040=ORIENTED_EDGE ( 'NONE', *, *, #39226, .T. ) ;
#37044=VERTEX_POINT ( 'NONE', #48832 ) ;
#37045=CARTESIAN_POINT ( 'NONE',  ( 15.50000000000000000, -2.500000000000000000, -23.94337567297399971 ) ) ;
#37053=VECTOR ( 'NONE', #60062, 1000.000000000000000 ) ;
#37065=VERTEX_POINT ( 'NONE', #65092 ) ;
#37066=ORIENTED_EDGE ( 'NONE', *, *, #42090, .T. ) ;
#37070=DIRECTION ( 'NONE',  ( 0.000000000000000000, 0.000000000000000000, 1.000000000000000000 ) ) ;
#37072=ORIENTED_EDGE ( 'NONE', *, *, #69732, .F. ) ;
#37075=DIRECTION ( 'NONE',  ( 0.000000000000000000, 0.000000000000000000, 1.000000000000000000 ) ) ;
#37082=DIRECTION ( 'NONE',  ( 0.000000000000000000, 0.000000000000000000, 1.000000000000000000 ) ) ;
#37085=VERTEX_POINT ( 'NONE', #27265 ) ;
#37096=CARTESIAN_POINT ( 'NONE',  ( 30.00000000000000000, -5.599999999999999645, 27.00000000000000000 ) ) ;
#37104=CIRCLE ( 'NONE', #6600, 0.5000000000079367624 ) ;
#37107=PLANE ( 'NONE',  #42579 ) ;
#37108=LINE ( 'NONE', #15878, #20191 ) ;
#37109=DIRECTION ( 'NONE',  ( 1.000000000000000000, -0.000000000000000000, -0.000000000000000000 ) ) ;
#37110=AXIS2_PLACEMENT_3D ( 'NONE', #57936, #25418, #49347 ) ;
#37114=DIRECTION ( 'NONE',  ( 0.000000000000000000, 1.000000000000000000, 0.000000000000000000 ) ) ;
#37115=ADVANCED_FACE ( 'NONE', ( #11326 ), #37869, .F. ) ;
#37118=LINE ( 'NONE', #9896, #66089 ) ;
#37129=EDGE_CURVE ( 'NONE', #67310, #1682, #65768, .T. ) ;
#37131=DIRECTION ( 'NONE',  ( 0.000000000000000000, -1.000000000000000000, 0.000000000000000000 ) ) ;
#37134=DIRECTION ( 'NONE',  ( 0.7142857142857395036, 0.000000000000000000, 0.6998542122237394469 ) ) ;
#37135=ORIENTED_EDGE ( 'NONE', *, *, #17891, .F. ) ;
#37139=DIRECTION ( 'NONE',  ( 0.000000000000000000, 1.000000000000000000, 0.000000000000000000 ) ) ;
#37144=LINE ( 'NONE', #9569, #46799 ) ;
#37150=VERTEX_POINT ( 'NONE', #54825 ) ;
#37151=CIRCLE ( 'NONE', #57461, 0.5000000000079362072 ) ;
#37166=VERTEX_POINT ( 'NONE', #46539 ) ;
#37172=EDGE_CURVE ( 'NONE', #18065, #52249, #40261, .T. ) ;
#37174=LINE ( 'NONE', #19486, #61696 ) ;
#37181=CIRCLE ( 'NONE', #4423, 0.5000000000001357803 ) ;
#37189=DIRECTION ( 'NONE',  ( -0.4998444328988824181, 0.000000000000000000, 0.8661152018640445593 ) ) ;
#37194=FACE_OUTER_BOUND ( 'NONE', #23426, .T. ) ;
#37203=VECTOR ( 'NONE', #64689, 1000.000000000000000 ) ;
#37205=EDGE_LOOP ( 'NONE', ( #65581, #28820, #62938, #26780, #2186 ) ) ;
#37215=ORIENTED_EDGE ( 'NONE', *, *, #35054, .F. ) ;
#37223=DIRECTION ( 'NONE',  ( 0.000000000000000000, -0.7071067811865460184, -0.7071067811865489050 ) ) ;
#37224=ADVANCED_FACE ( 'NONE', ( #24986 ), #34873, .F. ) ;
#37228=CARTESIAN_POINT ( 'NONE',  ( -30.00000000000000000, -11.10796162543699950, -9.102987789146602893 ) ) ;
#37231=ORIENTED_EDGE ( 'NONE', *, *, #22390, .F. ) ;
#37241=ORIENTED_EDGE ( 'NONE', *, *, #48482, .T. ) ;
#37253=CIRCLE ( 'NONE', #12320, 0.3499999999999611200 ) ;
#37267=EDGE_LOOP ( 'NONE', ( #45039, #20925, #15053, #7200 ) ) ;
#37275=DIRECTION ( 'NONE',  ( 1.000000000000000000, 0.000000000000000000, 0.000000000000000000 ) ) ;
#37282=EDGE_LOOP ( 'NONE', ( #1423, #60426, #3904, #15578, #23710 ) ) ;
#37283=VECTOR ( 'NONE', #5503, 1000.000000000000000 ) ;
#37284=FACE_OUTER_BOUND ( 'NONE', #62690, .T. ) ;
#37307=DIRECTION ( 'NONE',  ( 0.000000000000000000, 0.000000000000000000, -1.000000000000000000 ) ) ;
#37312=CIRCLE ( 'NONE', #44046, 1.449999999999999956 ) ;
#37318=VECTOR ( 'NONE', #44559, 1000.000000000000114 ) ;
#37322=ORIENTED_EDGE ( 'NONE', *, *, #63032, .T. ) ;
#37325=DIRECTION ( 'NONE',  ( -0.9375000000000004441, 0.000000000000000000, 0.3479852726768752902 ) ) ;
#37342=AXIS2_PLACEMENT_3D ( 'NONE', #55578, #28694, #50269 ) ;
#37354=DIRECTION ( 'NONE',  ( 0.000000000000000000, -0.9938079899998859545, 0.1111111111112941946 ) ) ;
#37364=ORIENTED_EDGE ( 'NONE', *, *, #20942, .F. ) ;
#37368=CARTESIAN_POINT ( 'NONE',  ( -17.51999999999999957, -15.50000000000000000, -26.00000000000000355 ) ) ;
#37374=DIRECTION ( 'NONE',  ( -1.000000000000000000, 0.000000000000000000, 0.000000000000000000 ) ) ;
#37384=CARTESIAN_POINT ( 'NONE',  ( -29.50000000000000355, -11.50000000000100009, -10.50000000000065903 ) ) ;
#37402=FACE_OUTER_BOUND ( 'NONE', #28680, .T. ) ;
#37411=DIRECTION ( 'NONE',  ( -1.000000000000000000, 0.000000000000000000, 0.000000000000000000 ) ) ;
#37415=AXIS2_PLACEMENT_3D ( 'NONE', #15296, #36502, #62316 ) ;
#37416=DIRECTION ( 'NONE',  ( -1.000000000000000000, 0.000000000000000000, 0.000000000000000000 ) ) ;
#37420=EDGE_LOOP ( 'NONE', ( #1130, #55219, #43497, #57988 ) ) ;
#37425=CARTESIAN_POINT ( 'NONE',  ( -11.00000000000000000, -5.200000000000001066, -26.59999999999999787 ) ) ;
#37427=ORIENTED_EDGE ( 'NONE', *, *, #580, .T. ) ;
#37432=VERTEX_POINT ( 'NONE', #9783 ) ;
#37433=VERTEX_POINT ( 'NONE', #41948 ) ;
#37449=PLANE ( 'NONE',  #24559 ) ;
#37455=LINE ( 'NONE', #59362, #45601 ) ;
#37458=DIRECTION ( 'NONE',  ( 1.000000000000000000, 0.000000000000000000, 0.000000000000000000 ) ) ;
#37459=VECTOR ( 'NONE', #37559, 1000.000000000000000 ) ;
#37463=EDGE_CURVE ( 'NONE', #57937, #7800, #10465, .T. ) ;
#37474=CARTESIAN_POINT ( 'NONE',  ( 15.50000000000000000, -0.1999999999999999556, -22.50000000000000000 ) ) ;
#37479=ORIENTED_EDGE ( 'NONE', *, *, #10270, .T. ) ;
#37486=EDGE_CURVE ( 'NONE', #49938, #64845, #43693, .T. ) ;
#37487=ORIENTED_EDGE ( 'NONE', *, *, #48386, .T. ) ;
#37492=CARTESIAN_POINT ( 'NONE',  ( -17.00000000000000000, -15.50000000000000000, 19.33772233983200195 ) ) ;
#37493=EDGE_CURVE ( 'NONE', #12012, #37614, #34100, .T. ) ;
#37498=FACE_OUTER_BOUND ( 'NONE', #55476, .T. ) ;
#37503=DIRECTION ( 'NONE',  ( 0.000000000000000000, 0.000000000000000000, -1.000000000000000000 ) ) ;
#37515=CYLINDRICAL_SURFACE ( 'NONE', #26092, 4.500000000000189182 ) ;
#37520=VECTOR ( 'NONE', #45152, 1000.000000000000000 ) ;
#37521=DIRECTION ( 'NONE',  ( 0.000000000000000000, 0.000000000000000000, 1.000000000000000000 ) ) ;
#37523=CARTESIAN_POINT ( 'NONE',  ( -24.00000000000000000, -17.50000000000000000, 15.70499999999969809 ) ) ;
#37524=DIRECTION ( 'NONE',  ( 0.000000000000000000, 1.000000000000000000, 0.000000000000000000 ) ) ;
#37531=LINE ( 'NONE', #32580, #67237 ) ;
#37534=ORIENTED_EDGE ( 'NONE', *, *, #31211, .T. ) ;
#37535=CARTESIAN_POINT ( 'NONE',  ( -24.00000000000000000, -17.35230188589299871, 15.35019951917099945 ) ) ;
#37537=ORIENTED_EDGE ( 'NONE', *, *, #19407, .T. ) ;
#37541=DIRECTION ( 'NONE',  ( -1.000000000000000000, 0.000000000000000000, 0.000000000000000000 ) ) ;
#37543=CARTESIAN_POINT ( 'NONE',  ( -11.00000000000000000, -12.00000000000000000, -11.03137303340310282 ) ) ;
#37546=ORIENTED_EDGE ( 'NONE', *, *, #34055, .F. ) ;
#37552=EDGE_CURVE ( 'NONE', #26707, #15366, #38388, .T. ) ;
#37553=CARTESIAN_POINT ( 'NONE',  ( -28.00000000000000000, -17.35230188589299871, 15.35019951917099945 ) ) ;
#37555=EDGE_CURVE ( 'NONE', #57481, #67199, #28451, .T. ) ;
#37557=ADVANCED_FACE ( 'NONE', ( #50375 ), #32726, .T. ) ;
#37559=DIRECTION ( 'NONE',  ( -1.000000000000000000, 0.000000000000000000, 0.000000000000000000 ) ) ;
#37561=ORIENTED_EDGE ( 'NONE', *, *, #20103, .F. ) ;
#37570=CARTESIAN_POINT ( 'NONE',  ( -29.50000000000000355, -11.50000000000100009, -19.50000000000103739 ) ) ;
#37578=CARTESIAN_POINT ( 'NONE',  ( -11.75000000000000000, -5.000000000000000000, 26.25000000000000000 ) ) ;
#37584=EDGE_CURVE ( 'NONE', #54936, #24780, #46120, .T. ) ;
#37597=VERTEX_POINT ( 'NONE', #40816 ) ;
#37607=ORIENTED_EDGE ( 'NONE', *, *, #19778, .F. ) ;
#37611=CARTESIAN_POINT ( 'NONE',  ( -29.50000000000000355, -15.97213595500069871, -14.50000000000000000 ) ) ;
#37614=VERTEX_POINT ( 'NONE', #19247 ) ;
#37616=ADVANCED_FACE ( 'NONE', ( #3688 ), #2288, .F. ) ;
#37623=VECTOR ( 'NONE', #2302, 1000.000000000000000 ) ;
#37629=DIRECTION ( 'NONE',  ( 1.000000000000000000, 0.000000000000000000, 0.000000000000000000 ) ) ;
#37639=DIRECTION ( 'NONE',  ( -0.000000000000000000, 1.000000000000000000, -0.000000000000000000 ) ) ;
#37642=ADVANCED_FACE ( 'NONE', ( #30560 ), #24204, .F. ) ;
#37646=VERTEX_POINT ( 'NONE', #57428 ) ;
#37661=CYLINDRICAL_SURFACE ( 'NONE', #45035, 3.499999999999850342 ) ;
#37664=VECTOR ( 'NONE', #4666, 1000.000000000000000 ) ;
#37665=VECTOR ( 'NONE', #44070, 1000.000000000000000 ) ;
#37677=DIRECTION ( 'NONE',  ( -1.000000000000000000, 0.000000000000000000, 0.000000000000000000 ) ) ;
#37678=VERTEX_POINT ( 'NONE', #18903 ) ;
#37694=CARTESIAN_POINT ( 'NONE',  ( -15.50000000000000000, 0.000000000000000000, 22.50000000000000000 ) ) ;
#37695=DIRECTION ( 'NONE',  ( 0.000000000000000000, 1.000000000000000000, 0.000000000000000000 ) ) ;
#37702=CARTESIAN_POINT ( 'NONE',  ( 30.00000000000000000, -10.85999999999999943, -9.350000000000269651 ) ) ;
#37704=CARTESIAN_POINT ( 'NONE',  ( 15.50000000000000000, -5.000000000000000000, -22.50000000000000000 ) ) ;
#37706=CIRCLE ( 'NONE', #27555, 4.000000000000000888 ) ;
#37715=CARTESIAN_POINT ( 'NONE',  ( 23.75054448485400016, -17.50000000000000000, 25.53140320652400064 ) ) ;
#37722=VECTOR ( 'NONE', #15637, 1000.000000000000000 ) ;
#37724=ORIENTED_EDGE ( 'NONE', *, *, #34567, .T. ) ;
#37730=AXIS2_PLACEMENT_3D ( 'NONE', #6434, #53841, #91 ) ;
#37731=LINE ( 'NONE', #52959, #21705 ) ;
#37733=CARTESIAN_POINT ( 'NONE',  ( 23.48000000000000043, -17.50000000000000000, 26.00000000000000355 ) ) ;
#37736=CARTESIAN_POINT ( 'NONE',  ( 30.00000000000000000, -11.50000000000100009, -15.00000000000084910 ) ) ;
#37741=EDGE_CURVE ( 'NONE', #5332, #62566, #51686, .T. ) ;
#37744=ORIENTED_EDGE ( 'NONE', *, *, #63028, .F. ) ;
#37749=LINE ( 'NONE', #48006, #43501 ) ;
#37752=EDGE_LOOP ( 'NONE', ( #19479, #64379, #19012, #19371 ) ) ;
#37753=EDGE_CURVE ( 'NONE', #50075, #62767, #53199, .T. ) ;
#37756=DIRECTION ( 'NONE',  ( 0.000000000000000000, -1.000000000000000000, 0.000000000000000000 ) ) ;
#37769=DIRECTION ( 'NONE',  ( 0.000000000000000000, 0.000000000000000000, 1.000000000000000000 ) ) ;
#37782=DIRECTION ( 'NONE',  ( 0.000000000000000000, 0.000000000000000000, 1.000000000000000000 ) ) ;
#37787=EDGE_CURVE ( 'NONE', #18785, #39920, #9959, .T. ) ;
#37798=ORIENTED_EDGE ( 'NONE', *, *, #62949, .T. ) ;
#37805=CARTESIAN_POINT ( 'NONE',  ( 28.00000000000000000, -15.50000000000000000, -14.50000000000000000 ) ) ;
#37808=AXIS2_PLACEMENT_3D ( 'NONE', #22147, #43714, #42664 ) ;
#37810=ORIENTED_EDGE ( 'NONE', *, *, #17650, .T. ) ;
#37811=VERTEX_POINT ( 'NONE', #26305 ) ;
#37817=CARTESIAN_POINT ( 'NONE',  ( 15.50000000000000000, -5.000000000000000000, 22.50000000000000000 ) ) ;
#37821=ORIENTED_EDGE ( 'NONE', *, *, #56977, .T. ) ;
#37830=EDGE_CURVE ( 'NONE', #14935, #18504, #15571, .T. ) ;
#37831=VECTOR ( 'NONE', #52926, 1000.000000000000000 ) ;
#37832=EDGE_CURVE ( 'NONE', #31859, #15321, #42568, .T. ) ;
#37834=ADVANCED_FACE ( 'NONE', ( #10394 ), #53538, .T. ) ;
#37835=CARTESIAN_POINT ( 'NONE',  ( 25.50000000000000355, -5.578999999999999737, 22.50000000000000000 ) ) ;
#37837=ORIENTED_EDGE ( 'NONE', *, *, #26038, .F. ) ;
#37840=ORIENTED_EDGE ( 'NONE', *, *, #24275, .T. ) ;
#37850=ORIENTED_EDGE ( 'NONE', *, *, #53850, .F. ) ;
#37853=DIRECTION ( 'NONE',  ( -1.000000000000000000, 0.000000000000000000, 0.000000000000000000 ) ) ;
#37861=DIRECTION ( 'NONE',  ( 0.000000000000000000, 0.000000000000000000, 1.000000000000000000 ) ) ;
#37864=ORIENTED_EDGE ( 'NONE', *, *, #34813, .F. ) ;
#37869=PLANE ( 'NONE',  #52773 ) ;
#37870=LINE ( 'NONE', #54138, #36192 ) ;
#37871=VECTOR ( 'NONE', #61272, 1000.000000000000000 ) ;
#37876=FACE_OUTER_BOUND ( 'NONE', #25020, .T. ) ;
#37882=EDGE_CURVE ( 'NONE', #44394, #122, #65276, .T. ) ;
#37884=AXIS2_PLACEMENT_3D ( 'NONE', #67159, #28289, #1418 ) ;
#37894=EDGE_CURVE ( 'NONE', #2965, #36815, #48924, .T. ) ;
#37898=ORIENTED_EDGE ( 'NONE', *, *, #52934, .T. ) ;
#37904=CIRCLE ( 'NONE', #40135, 0.5000000000001357803 ) ;
#37907=CARTESIAN_POINT ( 'NONE',  ( -15.50000000000000000, -2.500000000000000000, 21.05662432702600029 ) ) ;
#37912=VERTEX_POINT ( 'NONE', #33346 ) ;
#37915=AXIS2_PLACEMENT_3D ( 'NONE', #58384, #8514, #52368 ) ;
#37937=VECTOR ( 'NONE', #38232, 1000.000000000000000 ) ;
#37947=EDGE_LOOP ( 'NONE', ( #39, #69212, #23988, #33100 ) ) ;
#37961=ORIENTED_EDGE ( 'NONE', *, *, #42758, .T. ) ;
#37967=LINE ( 'NONE', #5089, #16309 ) ;
#37968=DIRECTION ( 'NONE',  ( -1.000000000000000000, 0.000000000000000000, 0.000000000000000000 ) ) ;
#37969=EDGE_CURVE ( 'NONE', #58919, #36973, #44285, .T. ) ;
#37972=VECTOR ( 'NONE', #11149, 1000.000000000000000 ) ;
#37976=ORIENTED_EDGE ( 'NONE', *, *, #48011, .T. ) ;
#37979=ADVANCED_FACE ( 'NONE', ( #65860, #54233 ), #38988, .F. ) ;
#37986=VERTEX_POINT ( 'NONE', #55604 ) ;
#37994=DIRECTION ( 'NONE',  ( 1.000000000000000000, -0.000000000000000000, -0.000000000000000000 ) ) ;
#37995=ORIENTED_EDGE ( 'NONE', *, *, #986, .F. ) ;
#37996=PLANE ( 'NONE',  #59954 ) ;
#37999=CARTESIAN_POINT ( 'NONE',  ( 15.50000000000000000, -0.2038245569916604938, -21.05662432702600029 ) ) ;
#38003=CARTESIAN_POINT ( 'NONE',  ( 29.25000000000000000, -5.000000000000000000, -26.25000000000000000 ) ) ;
#38014=CARTESIAN_POINT ( 'NONE',  ( 30.00000000000000000, -17.50000000000000000, 26.64999999999999858 ) ) ;
#38019=VERTEX_POINT ( 'NONE', #23770 ) ;
#38026=ADVANCED_FACE ( 'NONE', ( #45322 ), #40733, .T. ) ;
#38033=EDGE_CURVE ( 'NONE', #13102, #60914, #5427, .T. ) ;
#38034=DIRECTION ( 'NONE',  ( 1.000000000000000000, -0.000000000000000000, -0.000000000000000000 ) ) ;
#38044=EDGE_CURVE ( 'NONE', #4484, #65633, #24113, .T. ) ;
#38048=DIRECTION ( 'NONE',  ( 1.000000000000000000, -0.000000000000000000, -0.000000000000000000 ) ) ;
#38057=CARTESIAN_POINT ( 'NONE',  ( -11.00000000000000000, -17.50000000000000000, 26.64999999999999858 ) ) ;
#38058=AXIS2_PLACEMENT_3D ( 'NONE', #66719, #61400, #34533 ) ;
#38065=LINE ( 'NONE', #16830, #48105 ) ;
#38069=EDGE_LOOP ( 'NONE', ( #65911, #48767 ) ) ;
#38070=CARTESIAN_POINT ( 'NONE',  ( 30.00000000000000000, -5.000000000000000000, -11.75000000000000000 ) ) ;
#38076=VERTEX_POINT ( 'NONE', #56983 ) ;
#38081=CARTESIAN_POINT ( 'NONE',  ( 11.50000000000000000, -11.50000000000000000, 19.00000000000000000 ) ) ;
#38101=ORIENTED_EDGE ( 'NONE', *, *, #63883, .F. ) ;
#38108=EDGE_CURVE ( 'NONE', #27679, #41539, #55144, .T. ) ;
#38115=EDGE_CURVE ( 'NONE', #30238, #65126, #2055, .T. ) ;
#38118=CARTESIAN_POINT ( 'NONE',  ( -17.00000000000000000, -15.50000000000000000, -19.33772233983200195 ) ) ;
#38132=ORIENTED_EDGE ( 'NONE', *, *, #3619, .T. ) ;
#38133=AXIS2_PLACEMENT_3D ( 'NONE', #65278, #28124, #37354 ) ;
#38134=LINE ( 'NONE', #11232, #18855 ) ;
#38144=CARTESIAN_POINT ( 'NONE',  ( 30.00000000000000000, -5.000000000000000000, -27.00000000000000000 ) ) ;
#38156=ORIENTED_EDGE ( 'NONE', *, *, #18194, .F. ) ;
#38158=CARTESIAN_POINT ( 'NONE',  ( -15.50000000000000000, -0.2000000000000000111, 25.79999999999947136 ) ) ;
#38170=ORIENTED_EDGE ( 'NONE', *, *, #28881, .F. ) ;
#38171=CARTESIAN_POINT ( 'NONE',  ( 30.00000000000000000, -8.959999999999999076, -17.04524521594300523 ) ) ;
#38176=AXIS2_PLACEMENT_3D ( 'NONE', #50988, #13155, #62290 ) ;
#38183=VERTEX_POINT ( 'NONE', #59752 ) ;
#38194=VERTEX_POINT ( 'NONE', #65411 ) ;
#38195=ORIENTED_EDGE ( 'NONE', *, *, #55805, .F. ) ;
#38201=EDGE_CURVE ( 'NONE', #59852, #3061, #49830, .T. ) ;
#38202=EDGE_CURVE ( 'NONE', #66963, #54936, #35933, .T. ) ;
#38211=EDGE_LOOP ( 'NONE', ( #58825, #12651, #31376, #18247 ) ) ;
#38212=CARTESIAN_POINT ( 'NONE',  ( -30.00000000000000000, -5.000000000000000000, -27.00000000000000000 ) ) ;
#38222=VERTEX_POINT ( 'NONE', #11303 ) ;
#38226=DIRECTION ( 'NONE',  ( 0.8660254037844485886, 0.000000000000000000, -0.4999999999999827360 ) ) ;
#38232=DIRECTION ( 'NONE',  ( 0.000000000000000000, 1.000000000000000000, 0.000000000000000000 ) ) ;
#38234=CIRCLE ( 'NONE', #979, 3.499999999999054534 ) ;
#38240=ORIENTED_EDGE ( 'NONE', *, *, #45489, .F. ) ;
#38242=DIRECTION ( 'NONE',  ( 0.000000000000000000, 0.000000000000000000, -1.000000000000000000 ) ) ;
#38247=DIRECTION ( 'NONE',  ( 0.000000000000000000, 0.000000000000000000, -1.000000000000000000 ) ) ;
#38248=DIRECTION ( 'NONE',  ( -0.4999999999989361843, 0.000000000000000000, -0.8660254037850529940 ) ) ;
#38261=ORIENTED_EDGE ( 'NONE', *, *, #33394, .T. ) ;
#38272=CARTESIAN_POINT ( 'NONE',  ( -24.00000000000000000, -15.50000000000000000, -14.50000000000000000 ) ) ;
#38279=EDGE_CURVE ( 'NONE', #11521, #65734, #46260, .T. ) ;
#38284=EDGE_LOOP ( 'NONE', ( #14192, #57001, #53409, #12527 ) ) ;
#38285=EDGE_CURVE ( 'NONE', #32488, #18662, #67498, .T. ) ;
#38286=ORIENTED_EDGE ( 'NONE', *, *, #66895, .F. ) ;
#38291=VERTEX_POINT ( 'NONE', #50858 ) ;
#38299=CARTESIAN_POINT ( 'NONE',  ( 30.00000000000000000, -12.00000000000000000, 10.20500000000000007 ) ) ;
#38300=ORIENTED_EDGE ( 'NONE', *, *, #45853, .T. ) ;
#38305=CARTESIAN_POINT ( 'NONE',  ( 15.50000000000000000, -0.2038245569916604938, 23.94337567297399971 ) ) ;
#38306=AXIS2_PLACEMENT_3D ( 'NONE', #62408, #41908, #19998 ) ;
#38324=CIRCLE ( 'NONE', #7760, 2.000000000000001776 ) ;
#38332=ADVANCED_FACE ( 'NONE', ( #57574 ), #29643, .F. ) ;
#38344=CARTESIAN_POINT ( 'NONE',  ( -25.50000000000000355, -15.50000000000000000, -22.50000000000000000 ) ) ;
#38347=CARTESIAN_POINT ( 'NONE',  ( 13.00000000000000178, -17.50000000000000000, -15.70500000000000007 ) ) ;
#38354=VECTOR ( 'NONE', #22507, 1000.000000000000000 ) ;
#38356=PLANE ( 'NONE',  #63124 ) ;
#38357=ADVANCED_FACE ( 'NONE', ( #62166 ), #13731, .F. ) ;
#38372=EDGE_CURVE ( 'NONE', #57112, #18754, #11100, .T. ) ;
#38380=ORIENTED_EDGE ( 'NONE', *, *, #68385, .T. ) ;
#38385=CIRCLE ( 'NONE', #39498, 2.250000000000001776 ) ;
#38386=EDGE_CURVE ( 'NONE', #9129, #58645, #50612, .T. ) ;
#38388=LINE ( 'NONE', #33760, #47152 ) ;
#38389=DIRECTION ( 'NONE',  ( 0.000000000000000000, 0.000000000000000000, 1.000000000000000000 ) ) ;
#38390=CARTESIAN_POINT ( 'NONE',  ( -30.00000000000000000, -17.50000000000000000, 15.70500000000000007 ) ) ;
#38391=EDGE_CURVE ( 'NONE', #3700, #21874, #57226, .T. ) ;
#38397=VECTOR ( 'NONE', #42340, 1000.000000000000000 ) ;
#38401=ORIENTED_EDGE ( 'NONE', *, *, #4612, .F. ) ;
#38404=EDGE_CURVE ( 'NONE', #4079, #16582, #14098, .T. ) ;
#38407=EDGE_LOOP ( 'NONE', ( #62327, #6604, #55749, #925 ) ) ;
#38408=CYLINDRICAL_SURFACE ( 'NONE', #2753, 0.4000000000000600298 ) ;
#38409=CARTESIAN_POINT ( 'NONE',  ( -11.00000000000000000, -12.00000000000000000, 10.20500000000000007 ) ) ;
#38417=AXIS2_PLACEMENT_3D ( 'NONE', #43269, #59542, #27367 ) ;
#38430=EDGE_CURVE ( 'NONE', #13935, #39920, #2444, .T. ) ;
#38432=ORIENTED_EDGE ( 'NONE', *, *, #44613, .T. ) ;
#38445=EDGE_CURVE ( 'NONE', #51774, #64699, #68199, .T. ) ;
#38470=DIRECTION ( 'NONE',  ( 0.000000000000000000, -5.800915303574361727E-12, -1.000000000000000000 ) ) ;
#38477=CARTESIAN_POINT ( 'NONE',  ( 30.00000000000000000, -17.14999999999900027, 26.64999999999900027 ) ) ;
#38480=VERTEX_POINT ( 'NONE', #12687 ) ;
#38481=DIRECTION ( 'NONE',  ( 0.000000000000000000, -0.7071067811865495711, -0.7071067811865455743 ) ) ;
#38492=CARTESIAN_POINT ( 'NONE',  ( -15.29633693294650421, -0.2717122460102743275, 21.17420925361331641 ) ) ;
#38501=CARTESIAN_POINT ( 'NONE',  ( 16.89194109070750116, -5.000000000000000000, -26.25000000000000000 ) ) ;
#38505=CARTESIAN_POINT ( 'NONE',  ( 16.54686605390242349, -0.2715358723599884394, -23.33896727494797929 ) ) ;
#38509=CARTESIAN_POINT ( 'NONE',  ( -11.00000000000000000, -8.959999999999999076, 17.04524521594300523 ) ) ;
#38514=LINE ( 'NONE', #49803, #11826 ) ;
#38523=CARTESIAN_POINT ( 'NONE',  ( -30.00000000000000000, -15.97213595500069871, 14.50000000000000000 ) ) ;
#38531=DIRECTION ( 'NONE',  ( 0.000000000000000000, -0.1249999999999996531, -0.9921567416492215186 ) ) ;
#38532=ORIENTED_EDGE ( 'NONE', *, *, #55502, .T. ) ;
#38537=CARTESIAN_POINT ( 'NONE',  ( 13.00000000000000178, -16.28999999999710369, -15.00000000000794920 ) ) ;
#38540=ADVANCED_FACE ( 'NONE', ( #46981 ), #65267, .F. ) ;
#38541=ORIENTED_EDGE ( 'NONE', *, *, #3612, .F. ) ;
#38545=CARTESIAN_POINT ( 'NONE',  ( -25.50000000000000355, -15.50000000000000000, -22.50000000000000000 ) ) ;
#38547=DIRECTION ( 'NONE',  ( -0.4285714285711681448, 0.000000000000000000, -0.9035079029053748600 ) ) ;
#38549=EDGE_LOOP ( 'NONE', ( #59316, #30010 ) ) ;
#38550=VECTOR ( 'NONE', #69785, 1000.000000000000000 ) ;
#38555=DIRECTION ( 'NONE',  ( 0.000000000000000000, 0.000000000000000000, 1.000000000000000000 ) ) ;
#38556=ORIENTED_EDGE ( 'NONE', *, *, #24133, .T. ) ;
#38558=DIRECTION ( 'NONE',  ( 0.000000000000000000, 0.7278708115913746779, -0.6857142857147672244 ) ) ;
#38563=CARTESIAN_POINT ( 'NONE',  ( 29.50000000000000355, -11.50000000000100009, 15.00000000000084910 ) ) ;
#38564=LINE ( 'NONE', #60117, #29256 ) ;
#38566=CARTESIAN_POINT ( 'NONE',  ( -30.00000000000000000, -5.000000000000000000, -27.00000000000000000 ) ) ;
#38569=EDGE_CURVE ( 'NONE', #41911, #51508, #43688, .T. ) ;
#38571=VERTEX_POINT ( 'NONE', #64907 ) ;
#38573=EDGE_CURVE ( 'NONE', #52657, #52369, #27422, .T. ) ;
#38577=EDGE_CURVE ( 'NONE', #20791, #35525, #20115, .T. ) ;
#38578=CARTESIAN_POINT ( 'NONE',  ( 30.00000000000000000, -5.000000000000000000, 27.00000000000000000 ) ) ;
#38590=FACE_OUTER_BOUND ( 'NONE', #64886, .T. ) ;
#38598=ORIENTED_EDGE ( 'NONE', *, *, #289, .T. ) ;
#38600=DIRECTION ( 'NONE',  ( 0.000000000000000000, -1.000000000000000000, 0.000000000000000000 ) ) ;
#38602=EDGE_LOOP ( 'NONE', ( #30785, #35714, #54271, #21645, #32640, #45560 ) ) ;
#38603=AXIS2_PLACEMENT_3D ( 'NONE', #10291, #33243, #26910 ) ;
#38611=CARTESIAN_POINT ( 'NONE',  ( 25.50000000000000355, -15.50000000000000000, -22.50000000000000000 ) ) ;
#38614=EDGE_LOOP ( 'NONE', ( #67593, #6399, #41792, #37231 ) ) ;
#38619=EDGE_CURVE ( 'NONE', #9955, #55205, #16813, .T. ) ;
#38627=CARTESIAN_POINT ( 'NONE',  ( 11.00000000000000000, -11.10796162543699950, 9.102987789146602893 ) ) ;
#38638=ORIENTED_EDGE ( 'NONE', *, *, #64658, .F. ) ;
#38654=CIRCLE ( 'NONE', #8141, 2.250000000000001776 ) ;
#38660=DIRECTION ( 'NONE',  ( 0.000000000000000000, 0.000000000000000000, -1.000000000000000000 ) ) ;
#38670=CARTESIAN_POINT ( 'NONE',  ( -25.50000000000000355, -5.578999999999999737, 22.50000000000000000 ) ) ;
#38673=LINE ( 'NONE', #7864, #29950 ) ;
#38675=LINE ( 'NONE', #22073, #55762 ) ;
#38679=VERTEX_POINT ( 'NONE', #7580 ) ;
#38681=CARTESIAN_POINT ( 'NONE',  ( 14.66242688423474050, -0.3152598339554796292, -21.54019739087904384 ) ) ;
#38682=CARTESIAN_POINT ( 'NONE',  ( 23.75054448485400016, -15.50000000000000000, 25.53140320652400064 ) ) ;
#38684=DIRECTION ( 'NONE',  ( -1.000000000000000000, 0.000000000000000000, 0.000000000000000000 ) ) ;
#38707=CARTESIAN_POINT ( 'NONE',  ( -30.00000000000000000, -11.50000000000100009, 15.00000000000084910 ) ) ;
#38708=CIRCLE ( 'NONE', #62368, 4.500000000000190958 ) ;
#38713=DIRECTION ( 'NONE',  ( 0.000000000000000000, -0.7096009616570518874, 0.7046037717862339012 ) ) ;
#38720=CARTESIAN_POINT ( 'NONE',  ( 30.00000000000000000, -9.200000000000120082, 17.30000000000000071 ) ) ;
#38721=ORIENTED_EDGE ( 'NONE', *, *, #56919, .F. ) ;
#38726=CYLINDRICAL_SURFACE ( 'NONE', #58006, 0.3499999999999614531 ) ;
#38730=FACE_OUTER_BOUND ( 'NONE', #67970, .T. ) ;
#38731=LINE ( 'NONE', #49694, #54868 ) ;
#38734=ORIENTED_EDGE ( 'NONE', *, *, #44613, .F. ) ;
#38739=CARTESIAN_POINT ( 'NONE',  ( 11.00000000000000000, -11.85423089348099879, -9.852125413066602277 ) ) ;
#38740=CARTESIAN_POINT ( 'NONE',  ( -13.00000000000000178, -15.50000000000000000, -20.05051025721700242 ) ) ;
#38748=LINE ( 'NONE', #55037, #8312 ) ;
#38753=AXIS2_PLACEMENT_3D ( 'NONE', #13540, #24508, #36155 ) ;
#38761=VECTOR ( 'NONE', #48191, 1000.000000000000114 ) ;
#38767=ORIENTED_EDGE ( 'NONE', *, *, #66697, .T. ) ;
#38773=EDGE_CURVE ( 'NONE', #33676, #38888, #67682, .T. ) ;
#38775=ORIENTED_EDGE ( 'NONE', *, *, #49736, .F. ) ;
#38777=CARTESIAN_POINT ( 'NONE',  ( -28.00000000000000000, -16.28999999999999915, -14.50000000000000000 ) ) ;
#38782=CARTESIAN_POINT ( 'NONE',  ( -11.00000000000000000, -14.04000000000000092, -17.04524521594300523 ) ) ;
#38788=ORIENTED_EDGE ( 'NONE', *, *, #45019, .T. ) ;
#38789=AXIS2_PLACEMENT_3D ( 'NONE', #67357, #67697, #55694 ) ;
#38814=CARTESIAN_POINT ( 'NONE',  ( 30.00000000000000000, -17.00000000000000000, -15.70499999999969809 ) ) ;
#38837=AXIS2_PLACEMENT_3D ( 'NONE', #36769, #15558, #19435 ) ;
#38842=DIRECTION ( 'NONE',  ( 0.000000000000000000, -0.7046037717859445770, 0.7096009616573392131 ) ) ;
#38847=CARTESIAN_POINT ( 'NONE',  ( 14.25000000000000000, -2.500000000000000000, -21.77831216351300014 ) ) ;
#38849=AXIS2_PLACEMENT_3D ( 'NONE', #20342, #35539, #26011 ) ;
#38856=CIRCLE ( 'NONE', #3837, 2.000000000000001776 ) ;
#38857=CIRCLE ( 'NONE', #32108, 0.3499999999999308664 ) ;
#38858=ORIENTED_EDGE ( 'NONE', *, *, #24453, .F. ) ;
#38862=B_SPLINE_CURVE_WITH_KNOTS ( 'NONE', 3,
 ( #7116, #39640, #6774, #44596, #28344, #28689 ),
 .UNSPECIFIED., .F., .F.,
 ( 4, 2, 4 ),
 ( 0.0002380763768129734448, 0.7291065797294589146, 1.457975083082104995 ),
 .UNSPECIFIED. ) ;
#38866=CARTESIAN_POINT ( 'NONE',  ( 11.00000000000000000, -10.85999999999999943, 9.350000000000269651 ) ) ;
#38867=AXIS2_PLACEMENT_3D ( 'NONE', #14013, #23930, #62096 ) ;
#38870=EDGE_CURVE ( 'NONE', #36470, #58038, #40510, .T. ) ;
#38877=DIRECTION ( 'NONE',  ( 0.000000000000000000, -1.000000000000000000, 0.000000000000000000 ) ) ;
#38882=DIRECTION ( 'NONE',  ( -1.000000000000000000, 0.000000000000000000, 0.000000000000000000 ) ) ;
#38888=VERTEX_POINT ( 'NONE', #62719 ) ;
#38904=ORIENTED_EDGE ( 'NONE', *, *, #61716, .T. ) ;
#38910=CIRCLE ( 'NONE', #66001, 0.3499999999999597877 ) ;
#38913=PLANE ( 'NONE',  #20429 ) ;
#38918=ADVANCED_FACE ( 'NONE', ( #25256 ), #46806, .T. ) ;
#38933=ORIENTED_EDGE ( 'NONE', *, *, #27320, .F. ) ;
#38934=DIRECTION ( 'NONE',  ( 0.000000000000000000, 0.000000000000000000, 1.000000000000000000 ) ) ;
#38945=ORIENTED_EDGE ( 'NONE', *, *, #28311, .F. ) ;
#38949=DIRECTION ( 'NONE',  ( -0.8660254037844482555, 0.000000000000000000, 0.4999999999999831801 ) ) ;
#38965=AXIS2_PLACEMENT_3D ( 'NONE', #54889, #60168, #446 ) ;
#38971=DIRECTION ( 'NONE',  ( 0.000000000000000000, -0.9921567416492215186, 0.1249999999999996531 ) ) ;
#38987=CARTESIAN_POINT ( 'NONE',  ( -30.00000000000000000, -5.200000000000001066, -26.59999999999999787 ) ) ;
#38988=PLANE ( 'NONE',  #24577 ) ;
#38990=DIRECTION ( 'NONE',  ( 0.000000000000000000, 0.000000000000000000, 1.000000000000000000 ) ) ;
#38995=LINE ( 'NONE', #1185, #20065 ) ;
#38999=VECTOR ( 'NONE', #5276, 1000.000000000000000 ) ;
#39000=VECTOR ( 'NONE', #15143, 1000.000000000000000 ) ;
#39002=CARTESIAN_POINT ( 'NONE',  ( -11.50000000000000000, -11.50000000000000000, -15.00000000000000000 ) ) ;
#39003=ORIENTED_EDGE ( 'NONE', *, *, #27971, .F. ) ;
#39008=AXIS2_PLACEMENT_3D ( 'NONE', #40925, #24677, #61088 ) ;
#39012=CYLINDRICAL_SURFACE ( 'NONE', #36856, 0.3499999999998886224 ) ;
#39019=AXIS2_PLACEMENT_3D ( 'NONE', #41165, #67694, #7933 ) ;
#39026=CARTESIAN_POINT ( 'NONE',  ( 11.50000000000000000, -11.50000000000100009, -15.00000000000084910 ) ) ;
#39028=ORIENTED_EDGE ( 'NONE', *, *, #63650, .F. ) ;
#39036=EDGE_LOOP ( 'NONE', ( #41277, #13567, #65158, #18651 ) ) ;
#39046=DIRECTION ( 'NONE',  ( -1.000000000000000000, 0.000000000000000000, 0.000000000000000000 ) ) ;
#39048=ADVANCED_FACE ( 'NONE', ( #16045 ), #59175, .F. ) ;
#39050=ORIENTED_EDGE ( 'NONE', *, *, #63155, .F. ) ;
#39066=ORIENTED_EDGE ( 'NONE', *, *, #52118, .T. ) ;
#39082=DIRECTION ( 'NONE',  ( 0.000000000000000000, -1.000000000000000000, 0.000000000000000000 ) ) ;
#39086=EDGE_CURVE ( 'NONE', #49722, #12416, #19114, .T. ) ;
#39093=AXIS2_PLACEMENT_3D ( 'NONE', #43018, #43727, #60314 ) ;
#39096=CIRCLE ( 'NONE', #22152, 0.2000000000005226763 ) ;
#39098=B_SPLINE_CURVE_WITH_KNOTS ( 'NONE', 3,
 ( #18561, #1962, #51088, #24226, #23525, #28468 ),
 .UNSPECIFIED., .F., .F.,
 ( 4, 2, 4 ),
 ( 0.0002380763768129734448, 0.7291065797294584705, 1.457975083082104106 ),
 .UNSPECIFIED. ) ;
#39108=VECTOR ( 'NONE', #59741, 1000.000000000000000 ) ;
#39112=DIRECTION ( 'NONE',  ( 0.000000000000000000, 1.000000000000000000, 0.000000000000000000 ) ) ;
#39118=DIRECTION ( 'NONE',  ( 1.000000000000000000, -0.000000000000000000, -0.000000000000000000 ) ) ;
#39125=VERTEX_POINT ( 'NONE', #44619 ) ;
#39128=PLANE ( 'NONE',  #9646 ) ;
#39130=EDGE_LOOP ( 'NONE', ( #40406, #26784, #61424, #33908 ) ) ;
#39132=CARTESIAN_POINT ( 'NONE',  ( 30.00000000000000000, -13.79999999999979998, 17.64999999999988844 ) ) ;
#39136=AXIS2_PLACEMENT_3D ( 'NONE', #64412, #27279, #48843 ) ;
#39138=ORIENTED_EDGE ( 'NONE', *, *, #63883, .T. ) ;
#39140=AXIS2_PLACEMENT_3D ( 'NONE', #27727, #884, #43976 ) ;
#39143=CIRCLE ( 'NONE', #8662, 4.000000000000001776 ) ;
#39150=DIRECTION ( 'NONE',  ( 0.000000000000000000, -1.000000000000000000, 0.000000000000000000 ) ) ;
#39151=DIRECTION ( 'NONE',  ( -1.000000000000000000, 0.000000000000000000, 0.000000000000000000 ) ) ;
#39152=FACE_BOUND ( 'NONE', #4365, .T. ) ;
#39153=VERTEX_POINT ( 'NONE', #50284 ) ;
#39157=AXIS2_PLACEMENT_3D ( 'NONE', #17548, #39460, #61021 ) ;
#39185=LINE ( 'NONE', #11607, #55950 ) ;
#39194=ORIENTED_EDGE ( 'NONE', *, *, #20143, .T. ) ;
#39199=AXIS2_PLACEMENT_3D ( 'NONE', #48938, #54595, #55281 ) ;
#39216=VECTOR ( 'NONE', #3164, 1000.000000000000000 ) ;
#39220=ORIENTED_EDGE ( 'NONE', *, *, #15378, .T. ) ;
#39225=DIRECTION ( 'NONE',  ( 0.000000000000000000, 0.000000000000000000, 1.000000000000000000 ) ) ;
#39226=EDGE_CURVE ( 'NONE', #19062, #20091, #31557, .T. ) ;
#39234=ORIENTED_EDGE ( 'NONE', *, *, #31714, .F. ) ;
#39239=EDGE_CURVE ( 'NONE', #18603, #37912, #39665, .T. ) ;
#39242=VECTOR ( 'NONE', #13862, 1000.000000000000000 ) ;
#39248=VECTOR ( 'NONE', #47114, 1000.000000000000000 ) ;
#39251=EDGE_LOOP ( 'NONE', ( #45666, #64113, #48284, #14467 ) ) ;
#39256=EDGE_LOOP ( 'NONE', ( #38156, #39893, #28691, #40673, #56267, #66494, #28863 ) ) ;
#39258=DIRECTION ( 'NONE',  ( 1.000000000000000000, 0.000000000000000000, 0.000000000000000000 ) ) ;
#39262=LINE ( 'NONE', #61158, #15399 ) ;
#39264=CARTESIAN_POINT ( 'NONE',  ( -24.00000000000000000, -17.35230188589299871, -15.35019951917099945 ) ) ;
#39265=EDGE_CURVE ( 'NONE', #39153, #62566, #34714, .T. ) ;
#39269=PLANE ( 'NONE',  #31513 ) ;
#39274=CARTESIAN_POINT ( 'NONE',  ( -15.50000000000000000, -1.037157890325000054, -22.50000000000000000 ) ) ;
#39298=EDGE_CURVE ( 'NONE', #24504, #32181, #51829, .T. ) ;
#39301=VECTOR ( 'NONE', #19099, 1000.000000000000000 ) ;
#39312=ORIENTED_EDGE ( 'NONE', *, *, #2157, .T. ) ;
#39318=EDGE_CURVE ( 'NONE', #28244, #57835, #41067, .T. ) ;
#39320=LINE ( 'NONE', #12769, #60599 ) ;
#39329=CARTESIAN_POINT ( 'NONE',  ( -11.50000000000000000, -12.00000000000000000, -11.00000000000000000 ) ) ;
#39337=DIRECTION ( 'NONE',  ( 0.000000000000000000, 0.7096009616570518874, 0.7046037717862339012 ) ) ;
#39339=ORIENTED_EDGE ( 'NONE', *, *, #42180, .T. ) ;
#39351=VECTOR ( 'NONE', #27770, 1000.000000000000000 ) ;
#39352=DIRECTION ( 'NONE',  ( 0.000000000000000000, 1.000000000000000000, 0.000000000000000000 ) ) ;
#39363=TOROIDAL_SURFACE ( 'NONE', #21317, 3.299999999999470024, 0.2000000000005275058 ) ;
#39367=DIRECTION ( 'NONE',  ( 0.000000000000000000, 0.000000000000000000, 1.000000000000000000 ) ) ;
#39369=DIRECTION ( 'NONE',  ( 0.000000000000000000, -1.000000000000000000, 0.000000000000000000 ) ) ;
#39370=CARTESIAN_POINT ( 'NONE',  ( -29.25000000000000000, -5.200000000000001066, 11.75000000000000000 ) ) ;
#39373=EDGE_CURVE ( 'NONE', #17297, #65633, #30428, .T. ) ;
#39375=DIRECTION ( 'NONE',  ( -1.000000000000000000, 0.000000000000000000, 0.000000000000000000 ) ) ;
#39376=CARTESIAN_POINT ( 'NONE',  ( 30.00000000000000000, -11.50000000000000000, -15.00000000000000000 ) ) ;
#39382=ORIENTED_EDGE ( 'NONE', *, *, #24453, .T. ) ;
#39387=DIRECTION ( 'NONE',  ( 0.000000000000000000, -0.7096009616570518874, -0.7046037717862339012 ) ) ;
#39392=CARTESIAN_POINT ( 'NONE',  ( 30.00000000000000000, 0.000000000000000000, 27.00000000000000000 ) ) ;
#39398=ORIENTED_EDGE ( 'NONE', *, *, #2539, .F. ) ;
#39399=AXIS2_PLACEMENT_3D ( 'NONE', #10729, #53888, #27001 ) ;
#39402=VECTOR ( 'NONE', #50095, 1000.000000000000000 ) ;
#39420=EDGE_CURVE ( 'NONE', #7006, #62810, #42822, .T. ) ;
#39429=DIRECTION ( 'NONE',  ( 1.000000000000000000, 0.000000000000000000, 0.000000000000000000 ) ) ;
#39432=EDGE_CURVE ( 'NONE', #30827, #9139, #27272, .T. ) ;
#39437=LINE ( 'NONE', #61699, #39593 ) ;
#39443=EDGE_CURVE ( 'NONE', #69392, #42454, #52762, .T. ) ;
#39453=DIRECTION ( 'NONE',  ( 0.000000000000000000, 1.000000000000000000, 0.000000000000000000 ) ) ;
#39454=CARTESIAN_POINT ( 'NONE',  ( -17.24945551514599984, -15.50000000000000000, 25.53140320652400064 ) ) ;
#39458=EDGE_LOOP ( 'NONE', ( #47375, #5828, #57427, #8393 ) ) ;
#39460=DIRECTION ( 'NONE',  ( 0.000000000000000000, 0.000000000000000000, -1.000000000000000000 ) ) ;
#39463=VERTEX_POINT ( 'NONE', #10640 ) ;
#39475=ADVANCED_FACE ( 'NONE', ( #15623 ), #58748, .T. ) ;
#39481=VECTOR ( 'NONE', #20423, 1000.000000000000000 ) ;
#39489=VECTOR ( 'NONE', #29585, 1000.000000000000000 ) ;
#39493=CIRCLE ( 'NONE', #9023, 3.499999999999855227 ) ;
#39495=VERTEX_POINT ( 'NONE', #21949 ) ;
#39496=CYLINDRICAL_SURFACE ( 'NONE', #38058, 0.5000000000001357803 ) ;
#39497=CARTESIAN_POINT ( 'NONE',  ( -30.00000000000000000, -11.50000000000000000, 15.00000000000000000 ) ) ;
#39498=AXIS2_PLACEMENT_3D ( 'NONE', #21754, #10106, #31680 ) ;
#39503=DIRECTION ( 'NONE',  ( 0.000000000000000000, 1.000000000000000000, 0.000000000000000000 ) ) ;
#39510=DIRECTION ( 'NONE',  ( 1.000000000000000000, 0.000000000000000000, 0.000000000000000000 ) ) ;
#39511=DIRECTION ( 'NONE',  ( 0.8660254037850523279, 0.000000000000000000, -0.4999999999989371835 ) ) ;
#39519=EDGE_CURVE ( 'NONE', #24440, #58530, #59784, .T. ) ;
#39521=LINE ( 'NONE', #28917, #36801 ) ;
#39532=ORIENTED_EDGE ( 'NONE', *, *, #25297, .T. ) ;
#39535=CIRCLE ( 'NONE', #12423, 0.3999999999993835154 ) ;
#39545=AXIS2_PLACEMENT_3D ( 'NONE', #31389, #53641, #68505 ) ;
#39548=AXIS2_PLACEMENT_3D ( 'NONE', #10027, #69779, #5063 ) ;
#39549=EDGE_LOOP ( 'NONE', ( #15227, #57764, #17129, #63719 ) ) ;
#39554=CIRCLE ( 'NONE', #57647, 4.500000000000190958 ) ;
#39558=ORIENTED_EDGE ( 'NONE', *, *, #37172, .T. ) ;
#39565=AXIS2_PLACEMENT_3D ( 'NONE', #50172, #28953, #10366 ) ;
#39566=CARTESIAN_POINT ( 'NONE',  ( -28.00000000000000000, -15.50000000000000000, -20.05051025721700242 ) ) ;
#39570=ORIENTED_EDGE ( 'NONE', *, *, #8153, .F. ) ;
#39576=EDGE_CURVE ( 'NONE', #20601, #30238, #16662, .T. ) ;
#39577=DIRECTION ( 'NONE',  ( 0.000000000000000000, 1.000000000000000000, 0.000000000000000000 ) ) ;
#39585=AXIS2_PLACEMENT_3D ( 'NONE', #41055, #23750, #19487 ) ;
#39588=AXIS2_PLACEMENT_3D ( 'NONE', #48494, #5716, #38242 ) ;
#39590=DIRECTION ( 'NONE',  ( 1.000000000000000000, 0.000000000000000000, 0.000000000000000000 ) ) ;
#39593=VECTOR ( 'NONE', #1966, 1000.000000000000000 ) ;
#39594=CIRCLE ( 'NONE', #43148, 0.5000000000079362072 ) ;
#39599=AXIS2_PLACEMENT_3D ( 'NONE', #36959, #9727, #4436 ) ;
#39603=ADVANCED_FACE ( 'NONE', ( #65772 ), #44897, .T. ) ;
#39605=ORIENTED_EDGE ( 'NONE', *, *, #6199, .T. ) ;
#39611=EDGE_CURVE ( 'NONE', #44584, #23076, #28630, .T. ) ;
#39614=ORIENTED_EDGE ( 'NONE', *, *, #30964, .F. ) ;
#39617=DIRECTION ( 'NONE',  ( 0.000000000000000000, 0.000000000000000000, 1.000000000000000000 ) ) ;
#39619=ORIENTED_EDGE ( 'NONE', *, *, #36911, .F. ) ;
#39620=CYLINDRICAL_SURFACE ( 'NONE', #48450, 0.3499999999999614531 ) ;
#39622=CARTESIAN_POINT ( 'NONE',  ( -16.94999999999999929, -0.2000000000000000111, 22.50000000000000000 ) ) ;
#39627=PLANE ( 'NONE',  #54460 ) ;
#39634=CARTESIAN_POINT ( 'NONE',  ( -15.50000000000000000, -0.4000000000005236034, -22.50000000000000000 ) ) ;
#39636=ORIENTED_EDGE ( 'NONE', *, *, #66230, .F. ) ;
#39640=CARTESIAN_POINT ( 'NONE',  ( 15.70313394608856683, -0.2715358723588608414, -21.17390376548178210 ) ) ;
#39641=ORIENTED_EDGE ( 'NONE', *, *, #38430, .F. ) ;
#39643=CIRCLE ( 'NONE', #58863, 4.500000000000191847 ) ;
#39644=ADVANCED_FACE ( 'NONE', ( #34269 ), #7406, .F. ) ;
#39645=ORIENTED_EDGE ( 'NONE', *, *, #18362, .T. ) ;
#39654=VERTEX_POINT ( 'NONE', #40288 ) ;
#39655=CIRCLE ( 'NONE', #57745, 0.3500000000002719824 ) ;
#39665=LINE ( 'NONE', #61224, #57474 ) ;
#39675=DIRECTION ( 'NONE',  ( -1.000000000000000000, 0.000000000000000000, 0.000000000000000000 ) ) ;
#39679=EDGE_CURVE ( 'NONE', #60441, #49549, #55263, .T. ) ;
#39688=ADVANCED_FACE ( 'NONE', ( #57603 ), #13057, .T. ) ;
#39690=VERTEX_POINT ( 'NONE', #56210 ) ;
#39697=CIRCLE ( 'NONE', #53261, 3.499999999999850342 ) ;
#39698=CYLINDRICAL_SURFACE ( 'NONE', #54672, 1.621000000000000885 ) ;
#39709=CIRCLE ( 'NONE', #19428, 0.3499999999999597877 ) ;
#39715=CARTESIAN_POINT ( 'NONE',  ( 16.75000000000000000, -2.500000000000000000, -23.22168783648699986 ) ) ;
#39736=EDGE_CURVE ( 'NONE', #56607, #58645, #3516, .T. ) ;
#39739=EDGE_LOOP ( 'NONE', ( #45296, #18874, #60814, #14180 ) ) ;
#39740=EDGE_CURVE ( 'NONE', #29722, #24086, #19164, .T. ) ;
#39746=ORIENTED_EDGE ( 'NONE', *, *, #4171, .F. ) ;
#39750=DIRECTION ( 'NONE',  ( 1.000000000000000000, -0.000000000000000000, -0.000000000000000000 ) ) ;
#39751=VERTEX_POINT ( 'NONE', #21183 ) ;
#39759=DIRECTION ( 'NONE',  ( 0.000000000000000000, 1.000000000000000000, 0.000000000000000000 ) ) ;
#39768=CARTESIAN_POINT ( 'NONE',  ( 11.00000000000000000, -12.00000000000000000, 10.20500000000000007 ) ) ;
#39776=VECTOR ( 'NONE', #52297, 1000.000000000000000 ) ;
#39797=CYLINDRICAL_SURFACE ( 'NONE', #17713, 3.499999999999038547 ) ;
#39809=DIRECTION ( 'NONE',  ( 0.000000000000000000, 0.000000000000000000, -1.000000000000000000 ) ) ;
#39810=AXIS2_PLACEMENT_3D ( 'NONE', #18419, #19481, #45297 ) ;
#39813=ADVANCED_FACE ( 'NONE', ( #25431 ), #4230, .T. ) ;
#39814=ORIENTED_EDGE ( 'NONE', *, *, #9044, .F. ) ;
#39815=EDGE_CURVE ( 'NONE', #42264, #44065, #36746, .T. ) ;
#39827=ORIENTED_EDGE ( 'NONE', *, *, #6206, .T. ) ;
#39835=LINE ( 'NONE', #2717, #1160 ) ;
#39841=AXIS2_PLACEMENT_3D ( 'NONE', #3890, #30049, #14133 ) ;
#39854=CARTESIAN_POINT ( 'NONE',  ( -11.00000000000000000, -5.200000000000001066, 9.400000000000000355 ) ) ;
#39858=VECTOR ( 'NONE', #49152, 1000.000000000000000 ) ;
#39864=AXIS2_PLACEMENT_3D ( 'NONE', #27296, #11697, #69738 ) ;
#39870=VECTOR ( 'NONE', #25052, 1000.000000000000000 ) ;
#39880=DIRECTION ( 'NONE',  ( 0.000000000000000000, 0.000000000000000000, 1.000000000000000000 ) ) ;
#39887=VERTEX_POINT ( 'NONE', #20128 ) ;
#39893=ORIENTED_EDGE ( 'NONE', *, *, #43543, .T. ) ;
#39899=DIRECTION ( 'NONE',  ( 0.000000000000000000, -0.7057491738665943037, 0.7084617869628675457 ) ) ;
#39901=DIRECTION ( 'NONE',  ( 0.000000000000000000, 0.000000000000000000, 1.000000000000000000 ) ) ;
#39912=ORIENTED_EDGE ( 'NONE', *, *, #44147, .F. ) ;
#39920=VERTEX_POINT ( 'NONE', #65355 ) ;
#39923=DIRECTION ( 'NONE',  ( 1.000000000000000000, 0.000000000000000000, 0.000000000000000000 ) ) ;
#39926=FACE_OUTER_BOUND ( 'NONE', #29744, .T. ) ;
#39929=CARTESIAN_POINT ( 'NONE',  ( 29.50000000000000355, -15.46862696659690073, 14.50000000000000000 ) ) ;
#39935=CARTESIAN_POINT ( 'NONE',  ( 18.85410196625000268, -17.50000000000000000, 21.50000000000000000 ) ) ;
#39936=CARTESIAN_POINT ( 'NONE',  ( 30.00000000000000000, -16.28999999999710369, -15.00000000000794920 ) ) ;
#39939=ORIENTED_EDGE ( 'NONE', *, *, #14919, .T. ) ;
#39940=CARTESIAN_POINT ( 'NONE',  ( 15.50000000000000000, -5.000000000000000000, -22.50000000000000000 ) ) ;
#39954=DIRECTION ( 'NONE',  ( -1.000000000000000000, 0.000000000000000000, 0.000000000000000000 ) ) ;
#39961=DIRECTION ( 'NONE',  ( 0.000000000000000000, 1.000000000000000000, 0.000000000000000000 ) ) ;
#39963=CARTESIAN_POINT ( 'NONE',  ( 29.25000000000000000, -5.000000000000000000, 11.75000000000000000 ) ) ;
#39966=VERTEX_POINT ( 'NONE', #60726 ) ;
#39968=EDGE_LOOP ( 'NONE', ( #67459, #38170, #9667, #48207 ) ) ;
#39975=AXIS2_PLACEMENT_3D ( 'NONE', #57090, #8652, #9356 ) ;
#39976=DIRECTION ( 'NONE',  ( 0.8660254037844485886, 0.000000000000000000, -0.4999999999999827360 ) ) ;
#39979=ORIENTED_EDGE ( 'NONE', *, *, #34480, .T. ) ;
#39980=EDGE_LOOP ( 'NONE', ( #45032, #1175, #52182, #26632 ) ) ;
#39986=AXIS2_PLACEMENT_3D ( 'NONE', #67210, #17380, #66171 ) ;
#39992=ORIENTED_EDGE ( 'NONE', *, *, #30924, .F. ) ;
#39994=CARTESIAN_POINT ( 'NONE',  ( 0.000000000000000000, -2.500000000000000000, 45.00000000000000000 ) ) ;
#40001=EDGE_CURVE ( 'NONE', #41898, #2156, #5660, .T. ) ;
#40023=FACE_OUTER_BOUND ( 'NONE', #22573, .T. ) ;
#40024=ORIENTED_EDGE ( 'NONE', *, *, #46172, .F. ) ;
#40025=AXIS2_PLACEMENT_3D ( 'NONE', #15574, #9914, #10587 ) ;
#40036=CARTESIAN_POINT ( 'NONE',  ( -30.00000000000000000, -12.00000000000000000, -10.20500000000000007 ) ) ;
#40038=ORIENTED_EDGE ( 'NONE', *, *, #45492, .T. ) ;
#40047=EDGE_CURVE ( 'NONE', #40687, #67636, #8012, .T. ) ;
#40059=CARTESIAN_POINT ( 'NONE',  ( 25.50000000000000355, -5.578999999999999737, -20.87900000000000134 ) ) ;
#40060=ORIENTED_EDGE ( 'NONE', *, *, #24408, .F. ) ;
#40066=ORIENTED_EDGE ( 'NONE', *, *, #21383, .T. ) ;
#40071=LINE ( 'NONE', #25232, #14688 ) ;
#40072=DIRECTION ( 'NONE',  ( -0.4285714285711678118, 0.000000000000000000, -0.9035079029053749711 ) ) ;
#40076=LINE ( 'NONE', #8617, #36355 ) ;
#40077=ADVANCED_FACE ( 'NONE', ( #45496 ), #50803, .T. ) ;
#40078=DIRECTION ( 'NONE',  ( 0.000000000000000000, -0.7046037717806115097, 0.7096009616626348659 ) ) ;
#40087=EDGE_CURVE ( 'NONE', #5599, #50768, #39835, .T. ) ;
#40090=EDGE_CURVE ( 'NONE', #33817, #14966, #40663, .T. ) ;
#40093=AXIS2_PLACEMENT_3D ( 'NONE', #33815, #976, #19220 ) ;
#40095=DIRECTION ( 'NONE',  ( -0.000000000000000000, 1.000000000000000000, -0.000000000000000000 ) ) ;
#40106=PRESENTATION_STYLE_ASSIGNMENT (( #7591 ) ) ;
#40109=AXIS2_PLACEMENT_3D ( 'NONE', #46817, #68401, #10740 ) ;
#40121=ADVANCED_FACE ( 'NONE', ( #3086 ), #18274, .T. ) ;
#40131=AXIS2_PLACEMENT_3D ( 'NONE', #27854, #60712, #34168 ) ;
#40135=AXIS2_PLACEMENT_3D ( 'NONE', #34563, #17956, #13702 ) ;
#40139=ORIENTED_EDGE ( 'NONE', *, *, #28891, .F. ) ;
#40141=EDGE_LOOP ( 'NONE', ( #40060, #50600, #1726, #40435, #62710 ) ) ;
#40147=VECTOR ( 'NONE', #17744, 1000.000000000000000 ) ;
#40151=CARTESIAN_POINT ( 'NONE',  ( -13.00000000000000178, -15.50000000000000000, 14.50000000000000000 ) ) ;
#40152=ADVANCED_FACE ( 'NONE', ( #35584 ), #57167, .T. ) ;
#40153=PLANE ( 'NONE',  #48578 ) ;
#40156=CIRCLE ( 'NONE', #23252, 1.620999999999997332 ) ;
#40161=ORIENTED_EDGE ( 'NONE', *, *, #53027, .F. ) ;
#40166=EDGE_CURVE ( 'NONE', #57686, #39654, #35047, .T. ) ;
#40167=DIRECTION ( 'NONE',  ( 0.000000000000000000, 1.000000000000000000, 0.000000000000000000 ) ) ;
#40169=CARTESIAN_POINT ( 'NONE',  ( 11.00000000000000000, -14.04000000000000092, -14.80000000000000071 ) ) ;
#40172=ORIENTED_EDGE ( 'NONE', *, *, #59032, .F. ) ;
#40177=EDGE_CURVE ( 'NONE', #45394, #22980, #57511, .T. ) ;
#40178=LINE ( 'NONE', #19317, #47078 ) ;
#40190=LINE ( 'NONE', #44449, #44398 ) ;
#40193=DIRECTION ( 'NONE',  ( 0.000000000000000000, -0.9921567416492215186, 0.1249999999999996531 ) ) ;
#40197=VECTOR ( 'NONE', #32231, 1000.000000000000000 ) ;
#40206=DIRECTION ( 'NONE',  ( 0.000000000000000000, 1.000000000000000000, 0.000000000000000000 ) ) ;
#40208=ORIENTED_EDGE ( 'NONE', *, *, #19864, .T. ) ;
#40224=EDGE_CURVE ( 'NONE', #44628, #35366, #30998, .T. ) ;
#40244=LINE ( 'NONE', #28591, #30877 ) ;
#40245=ORIENTED_EDGE ( 'NONE', *, *, #12925, .F. ) ;
#40254=VECTOR ( 'NONE', #21792, 1000.000000000000000 ) ;
#40261=CIRCLE ( 'NONE', #62888, 0.5000000000001386669 ) ;
#40271=ORIENTED_EDGE ( 'NONE', *, *, #58286, .F. ) ;
#40279=FACE_OUTER_BOUND ( 'NONE', #48854, .T. ) ;
#40288=CARTESIAN_POINT ( 'NONE',  ( -25.50000000000000355, -15.12100000000000044, 24.12099999999999511 ) ) ;
#40293=AXIS2_PLACEMENT_3D ( 'NONE', #15268, #42481, #35772 ) ;
#40295=ORIENTED_EDGE ( 'NONE', *, *, #20225, .T. ) ;
#40298=LINE ( 'NONE', #61873, #20788 ) ;
#40300=ORIENTED_EDGE ( 'NONE', *, *, #8083, .T. ) ;
#40301=DIRECTION ( 'NONE',  ( 0.000000000000000000, -5.800915303574361727E-12, 1.000000000000000000 ) ) ;
#40303=VECTOR ( 'NONE', #6280, 1000.000000000000000 ) ;
#40305=FACE_OUTER_BOUND ( 'NONE', #36335, .T. ) ;
#40316=CIRCLE ( 'NONE', #12102, 4.500000000000191847 ) ;
#40322=CARTESIAN_POINT ( 'NONE',  ( -11.75000000000000000, -5.000000000000000000, 11.75000000000000000 ) ) ;
#40325=ORIENTED_EDGE ( 'NONE', *, *, #43462, .T. ) ;
#40327=LINE ( 'NONE', #1448, #13765 ) ;
#40330=CARTESIAN_POINT ( 'NONE',  ( 30.00000000000000000, -12.00000000000000000, -12.20000000000000107 ) ) ;
#40340=DIRECTION ( 'NONE',  ( 0.000000000000000000, 0.000000000000000000, 1.000000000000000000 ) ) ;
#40344=CARTESIAN_POINT ( 'NONE',  ( -11.00000000000000000, -5.200000000000001066, 26.59999999999999787 ) ) ;
#40358=ADVANCED_FACE ( 'NONE', ( #1587 ), #6573, .F. ) ;
#40365=ORIENTED_EDGE ( 'NONE', *, *, #20933, .T. ) ;
#40378=ORIENTED_EDGE ( 'NONE', *, *, #66694, .F. ) ;
#40384=DIRECTION ( 'NONE',  ( 1.000000000000000000, 0.000000000000000000, 0.000000000000000000 ) ) ;
#40395=PLANE ( 'NONE',  #27112 ) ;
#40396=ORIENTED_EDGE ( 'NONE', *, *, #10273, .F. ) ;
#40404=DIRECTION ( 'NONE',  ( -1.000000000000000000, 0.000000000000000000, 0.000000000000000000 ) ) ;
#40406=ORIENTED_EDGE ( 'NONE', *, *, #24236, .F. ) ;
#40409=ORIENTED_EDGE ( 'NONE', *, *, #68714, .T. ) ;
#40410=ADVANCED_FACE ( 'NONE', ( #6216 ), #11846, .T. ) ;
#40414=CARTESIAN_POINT ( 'NONE',  ( 30.00000000000000000, -12.00000000000000000, -10.20500000000000007 ) ) ;
#40422=PLANE ( 'NONE',  #58065 ) ;
#40435=ORIENTED_EDGE ( 'NONE', *, *, #10655, .F. ) ;
#40440=DIRECTION ( 'NONE',  ( 0.000000000000000000, 0.7071067811865455743, 0.7071067811865495711 ) ) ;
#40455=DIRECTION ( 'NONE',  ( 0.000000000000000000, 1.000000000000000000, 0.000000000000000000 ) ) ;
#40468=EDGE_LOOP ( 'NONE', ( #18781, #53175, #683, #58257, #68254, #62232 ) ) ;
#40471=FACE_OUTER_BOUND ( 'NONE', #8272, .T. ) ;
#40482=CARTESIAN_POINT ( 'NONE',  ( -28.00000000000000000, -17.00000000000000000, 15.70499999999969809 ) ) ;
#40489=ADVANCED_FACE ( 'NONE', ( #63010 ), #20216, .T. ) ;
#40501=ADVANCED_FACE ( 'NONE', ( #30131 ), #51709, .T. ) ;
#40510=CIRCLE ( 'NONE', #12235, 4.500000000000191847 ) ;
#40516=AXIS2_PLACEMENT_3D ( 'NONE', #39940, #61513, #56232 ) ;
#40522=EDGE_CURVE ( 'NONE', #59443, #47101, #36127, .T. ) ;
#40535=ORIENTED_EDGE ( 'NONE', *, *, #37555, .T. ) ;
#40543=DIRECTION ( 'NONE',  ( 0.000000000000000000, -0.9921567416492215186, 0.1249999999999996531 ) ) ;
#40552=ADVANCED_FACE ( 'NONE', ( #47439 ), #69011, .T. ) ;
#40556=FACE_OUTER_BOUND ( 'NONE', #717, .T. ) ;
#40567=DIRECTION ( 'NONE',  ( 0.000000000000000000, 0.000000000000000000, 1.000000000000000000 ) ) ;
#40569=EDGE_CURVE ( 'NONE', #68865, #56239, #42487, .T. ) ;
#40570=AXIS2_PLACEMENT_3D ( 'NONE', #1954, #55358, #23516 ) ;
#40573=FACE_OUTER_BOUND ( 'NONE', #32766, .T. ) ;
#40580=ORIENTED_EDGE ( 'NONE', *, *, #51431, .T. ) ;
#40592=CIRCLE ( 'NONE', #57554, 4.500000000000190958 ) ;
#40594=LINE ( 'NONE', #29985, #28896 ) ;
#40598=CARTESIAN_POINT ( 'NONE',  ( 30.00000000000000000, -9.487228132326899654, -12.50000000000000000 ) ) ;
#40604=CIRCLE ( 'NONE', #65457, 4.000000000000000888 ) ;
#40609=VERTEX_POINT ( 'NONE', #5380 ) ;
#40612=CARTESIAN_POINT ( 'NONE',  ( -11.50000000000000000, -11.50000000000100009, 19.50000000000103739 ) ) ;
#40619=ORIENTED_EDGE ( 'NONE', *, *, #45337, .F. ) ;
#40621=ADVANCED_FACE ( 'NONE', ( #4667 ), #54154, .F. ) ;
#40622=CARTESIAN_POINT ( 'NONE',  ( -11.00000000000000000, -17.50000000000000000, -26.64999999999900027 ) ) ;
#40632=EDGE_CURVE ( 'NONE', #16696, #6609, #24970, .T. ) ;
#40643=AXIS2_PLACEMENT_3D ( 'NONE', #3054, #68094, #14705 ) ;
#40648=CARTESIAN_POINT ( 'NONE',  ( 30.00000000000000000, -14.04000000000000092, 14.80000000000000071 ) ) ;
#40650=ADVANCED_FACE ( 'NONE', ( #33611 ), #1425, .T. ) ;
#40651=CARTESIAN_POINT ( 'NONE',  ( -25.50000000000000355, -5.578999999999999737, -20.87900000000000134 ) ) ;
#40652=CARTESIAN_POINT ( 'NONE',  ( -17.00000000000000000, -17.50000000000000000, 19.33772233983200195 ) ) ;
#40663=CIRCLE ( 'NONE', #19214, 4.000000000000000888 ) ;
#40668=ORIENTED_EDGE ( 'NONE', *, *, #56944, .F. ) ;
#40672=ADVANCED_FACE ( 'NONE', ( #50213 ), #38913, .F. ) ;
#40673=ORIENTED_EDGE ( 'NONE', *, *, #1537, .F. ) ;
#40687=VERTEX_POINT ( 'NONE', #18026 ) ;
#40691=ORIENTED_EDGE ( 'NONE', *, *, #16554, .F. ) ;
#40705=VERTEX_POINT ( 'NONE', #65784 ) ;
#40709=DIRECTION ( 'NONE',  ( -1.000000000000000000, 0.000000000000000000, 0.000000000000000000 ) ) ;
#40718=LINE ( 'NONE', #55936, #7514 ) ;
#40728=CARTESIAN_POINT ( 'NONE',  ( -15.50000000000000000, -17.50000000000000000, -22.50000000000000000 ) ) ;
#40729=ORIENTED_EDGE ( 'NONE', *, *, #1829, .T. ) ;
#40731=CARTESIAN_POINT ( 'NONE',  ( -11.00000000000000000, -5.200000000000001066, 26.59999999999999432 ) ) ;
#40733=PLANE ( 'NONE',  #38176 ) ;
#40754=VERTEX_POINT ( 'NONE', #7419 ) ;
#40763=CARTESIAN_POINT ( 'NONE',  ( 14.10805890929250062, -5.000000000000000000, -26.25000000000000000 ) ) ;
#40771=EDGE_LOOP ( 'NONE', ( #10915, #6012, #23279, #62950 ) ) ;
#40778=CARTESIAN_POINT ( 'NONE',  ( 11.50000000000000000, -11.70000000000000284, 11.00000000000000000 ) ) ;
#40784=ORIENTED_EDGE ( 'NONE', *, *, #14919, .F. ) ;
#40786=CIRCLE ( 'NONE', #62228, 0.3500000000009988455 ) ;
#40787=DIRECTION ( 'NONE',  ( -1.000000000000000000, 0.000000000000000000, 0.000000000000000000 ) ) ;
#40794=DIRECTION ( 'NONE',  ( -1.000000000000000000, 0.000000000000000000, 0.000000000000000000 ) ) ;
#40802=EDGE_LOOP ( 'NONE', ( #7530, #67120, #63990, #48361 ) ) ;
#40816=CARTESIAN_POINT ( 'NONE',  ( 15.50000000000000000, -0.4000000000000000222, 19.00000000000000355 ) ) ;
#40821=EDGE_LOOP ( 'NONE', ( #11467, #24283, #36580, #8061, #47113, #4161, #67956 ) ) ;
#40824=AXIS2_PLACEMENT_3D ( 'NONE', #17719, #44230, #39617 ) ;
#40827=LINE ( 'NONE', #25631, #63646 ) ;
#40843=ORIENTED_EDGE ( 'NONE', *, *, #56457, .F. ) ;
#40851=VECTOR ( 'NONE', #33588, 1000.000000000000000 ) ;
#40865=EDGE_CURVE ( 'NONE', #41539, #50067, #19086, .T. ) ;
#40868=ORIENTED_EDGE ( 'NONE', *, *, #60765, .T. ) ;
#40869=AXIS2_PLACEMENT_3D ( 'NONE', #41368, #8848, #52339 ) ;
#40871=CYLINDRICAL_SURFACE ( 'NONE', #7971, 0.5000000000001374456 ) ;
#40875=CARTESIAN_POINT ( 'NONE',  ( 15.50000000000000000, -5.000000000000000000, -22.50000000000000000 ) ) ;
#40876=CYLINDRICAL_SURFACE ( 'NONE', #9862, 3.499999999999038547 ) ;
#40880=LINE ( 'NONE', #68818, #51671 ) ;
#40881=ADVANCED_FACE ( 'NONE', ( #41700 ), #7767, .F. ) ;
#40883=CYLINDRICAL_SURFACE ( 'NONE', #50274, 2.250000000000001776 ) ;
#40890=DIRECTION ( 'NONE',  ( 0.000000000000000000, 1.000000000000000000, 0.000000000000000000 ) ) ;
#40892=EDGE_CURVE ( 'NONE', #13557, #41462, #40992, .T. ) ;
#40899=CARTESIAN_POINT ( 'NONE',  ( 11.00000000000000000, -15.97213595500069871, -14.50000000000000000 ) ) ;
#40900=DIRECTION ( 'NONE',  ( -0.8660254037844482555, 0.000000000000000000, -0.4999999999999831801 ) ) ;
#40913=DIRECTION ( 'NONE',  ( 0.000000000000000000, 0.000000000000000000, 1.000000000000000000 ) ) ;
#40914=ORIENTED_EDGE ( 'NONE', *, *, #67508, .T. ) ;
#40915=LINE ( 'NONE', #62129, #5911 ) ;
#40919=LINE ( 'NONE', #19010, #60489 ) ;
#40925=CARTESIAN_POINT ( 'NONE',  ( 30.00000000000000000, -5.599999999999999645, -9.400000000000000355 ) ) ;
#40935=AXIS2_PLACEMENT_3D ( 'NONE', #61919, #24796, #67585 ) ;
#40936=EDGE_LOOP ( 'NONE', ( #20061, #23786, #22644, #2340 ) ) ;
#40939=PLANE ( 'NONE',  #14121 ) ;
#40943=ORIENTED_EDGE ( 'NONE', *, *, #54644, .F. ) ;
#40944=AXIS2_PLACEMENT_3D ( 'NONE', #59962, #16491, #11509 ) ;
#40951=ORIENTED_EDGE ( 'NONE', *, *, #8750, .F. ) ;
#40954=ORIENTED_EDGE ( 'NONE', *, *, #25673, .F. ) ;
#40956=VERTEX_POINT ( 'NONE', #69277 ) ;
#40957=FACE_OUTER_BOUND ( 'NONE', #48279, .T. ) ;
#40958=EDGE_CURVE ( 'NONE', #68720, #25525, #20484, .T. ) ;
#40964=CIRCLE ( 'NONE', #50005, 4.000000000000000888 ) ;
#40973=CARTESIAN_POINT ( 'NONE',  ( 24.00000000000000000, -17.35230188589299871, -15.35019951917099945 ) ) ;
#40975=LINE ( 'NONE', #8093, #39216 ) ;
#40984=CARTESIAN_POINT ( 'NONE',  ( 11.75000000000000000, -5.000000000000000000, -11.75000000000000000 ) ) ;
#40989=VERTEX_POINT ( 'NONE', #32143 ) ;
#40992=LINE ( 'NONE', #46301, #35097 ) ;
#40998=DIRECTION ( 'NONE',  ( 0.000000000000000000, 1.000000000000000000, 0.000000000000000000 ) ) ;
#41001=DIRECTION ( 'NONE',  ( 1.000000000000000000, -0.000000000000000000, -0.000000000000000000 ) ) ;
#41003=ORIENTED_EDGE ( 'NONE', *, *, #40569, .T. ) ;
#41017=DIRECTION ( 'NONE',  ( 1.000000000000000000, 0.000000000000000000, 0.000000000000000000 ) ) ;
#41030=EDGE_CURVE ( 'NONE', #28340, #13228, #36278, .T. ) ;
#41038=FACE_OUTER_BOUND ( 'NONE', #57433, .T. ) ;
#41051=DIRECTION ( 'NONE',  ( 0.000000000000000000, 1.000000000000000000, 0.000000000000000000 ) ) ;
#41054=DIRECTION ( 'NONE',  ( 0.000000000000000000, 1.000000000000000000, 0.000000000000000000 ) ) ;
#41055=CARTESIAN_POINT ( 'NONE',  ( -17.00000000000000000, -15.50000000000000000, -2.000000000000000000 ) ) ;
#41062=CARTESIAN_POINT ( 'NONE',  ( 16.75000000000000000, -0.2038245569916320166, -23.22168783648699986 ) ) ;
#41063=DIRECTION ( 'NONE',  ( 1.000000000000000000, -0.000000000000000000, -0.000000000000000000 ) ) ;
#41064=DIRECTION ( 'NONE',  ( 0.000000000000000000, -0.7084617869623469621, -0.7057491738671168857 ) ) ;
#41067=LINE ( 'NONE', #46373, #56364 ) ;
#41069=EDGE_CURVE ( 'NONE', #7103, #58695, #6311, .T. ) ;
#41071=FACE_OUTER_BOUND ( 'NONE', #38614, .T. ) ;
#41074=DIRECTION ( 'NONE',  ( 0.000000000000000000, 0.000000000000000000, 1.000000000000000000 ) ) ;
#41076=VECTOR ( 'NONE', #18132, 1000.000000000000000 ) ;
#41081=ORIENTED_EDGE ( 'NONE', *, *, #5087, .T. ) ;
#41087=LINE ( 'NONE', #57358, #4509 ) ;
#41092=DIRECTION ( 'NONE',  ( -0.8660254037850496633, 0.000000000000000000, 0.4999999999989417909 ) ) ;
#41094=CARTESIAN_POINT ( 'NONE',  ( 25.50000000000000355, 0.000000000000000000, 22.50000000000000000 ) ) ;
#41095=PLANE ( 'NONE',  #57732 ) ;
#41100=ORIENTED_EDGE ( 'NONE', *, *, #2539, .T. ) ;
#41103=CARTESIAN_POINT ( 'NONE',  ( 16.75000000000000000, -2.500000000000000000, 21.77831216351300014 ) ) ;
#41104=DIRECTION ( 'NONE',  ( 0.000000000000000000, -0.1111111111108840643, -0.9938079899999319178 ) ) ;
#41106=VECTOR ( 'NONE', #19959, 1000.000000000000000 ) ;
#41122=CIRCLE ( 'NONE', #56908, 0.2000000000005261458 ) ;
#41125=ORIENTED_EDGE ( 'NONE', *, *, #15323, .T. ) ;
#41126=VERTEX_POINT ( 'NONE', #33176 ) ;
#41130=AXIS2_PLACEMENT_3D ( 'NONE', #4680, #26248, #41801 ) ;
#41132=CARTESIAN_POINT ( 'NONE',  ( -14.25000000000000000, -2.500000000000000000, -21.77831216351300014 ) ) ;
#41135=DIRECTION ( 'NONE',  ( 1.000000000000000000, 0.000000000000000000, 0.000000000000000000 ) ) ;
#41137=FACE_OUTER_BOUND ( 'NONE', #60118, .T. ) ;
#41138=VERTEX_POINT ( 'NONE', #38158 ) ;
#41141=CARTESIAN_POINT ( 'NONE',  ( -15.50000000000000000, -1.037157890325000054, 22.50000000000000000 ) ) ;
#41148=CARTESIAN_POINT ( 'NONE',  ( 11.50000000000000000, -11.50000000000100009, -15.00000000000084910 ) ) ;
#41149=PLANE ( 'NONE',  #26709 ) ;
#41154=FACE_OUTER_BOUND ( 'NONE', #52985, .T. ) ;
#41162=CIRCLE ( 'NONE', #11828, 0.3499999999999285905 ) ;
#41165=CARTESIAN_POINT ( 'NONE',  ( -13.00000000000000178, -15.50000000000000000, 20.05051025721700242 ) ) ;
#41169=VERTEX_POINT ( 'NONE', #54413 ) ;
#41171=DIRECTION ( 'NONE',  ( 0.000000000000000000, -0.7096009616570518874, -0.7046037717862339012 ) ) ;
#41181=DIRECTION ( 'NONE',  ( 0.4999999999999827360, 0.000000000000000000, -0.8660254037844485886 ) ) ;
#41185=VERTEX_POINT ( 'NONE', #7325 ) ;
#41188=LINE ( 'NONE', #62760, #23688 ) ;
#41193=EDGE_CURVE ( 'NONE', #39751, #57629, #43794, .T. ) ;
#41195=EDGE_CURVE ( 'NONE', #22707, #66744, #65704, .T. ) ;
#41204=EDGE_CURVE ( 'NONE', #67199, #7820, #16953, .T. ) ;
#41208=CARTESIAN_POINT ( 'NONE',  ( 15.50000000000000000, -5.000000000000000000, 22.50000000000000000 ) ) ;
#41216=ORIENTED_EDGE ( 'NONE', *, *, #62333, .T. ) ;
#41217=CARTESIAN_POINT ( 'NONE',  ( 30.00000000000000000, -5.000000000000000000, -27.00000000000000000 ) ) ;
#41218=AXIS2_PLACEMENT_3D ( 'NONE', #25088, #52308, #68575 ) ;
#41230=CARTESIAN_POINT ( 'NONE',  ( -30.00000000000000000, -11.70000000000000284, 12.50000000000000000 ) ) ;
#41238=EDGE_CURVE ( 'NONE', #39654, #44220, #2727, .T. ) ;
#41243=CARTESIAN_POINT ( 'NONE',  ( -30.00000000000000000, -12.00000000000000000, -10.52786404500095863 ) ) ;
#41247=CARTESIAN_POINT ( 'NONE',  ( 14.25000000000000000, -2.500000000000000000, 23.22168783648699986 ) ) ;
#41248=DIRECTION ( 'NONE',  ( 0.000000000000000000, 0.000000000000000000, 1.000000000000000000 ) ) ;
#41250=DIRECTION ( 'NONE',  ( 0.000000000000000000, 0.7071067811865496822, 0.7071067811865454633 ) ) ;
#41252=DIRECTION ( 'NONE',  ( 0.000000000000000000, -0.9921567416492215186, 0.1249999999999996531 ) ) ;
#41256=AXIS2_PLACEMENT_3D ( 'NONE', #36141, #35083, #46400 ) ;
#41265=DIRECTION ( 'NONE',  ( 0.000000000000000000, 1.000000000000000000, 0.000000000000000000 ) ) ;
#41268=AXIS2_PLACEMENT_3D ( 'NONE', #42009, #59669, #37070 ) ;
#41270=CYLINDRICAL_SURFACE ( 'NONE', #65880, 4.000000000000000000 ) ;
#41273=CARTESIAN_POINT ( 'NONE',  ( 11.00000000000000000, -16.28999999999710369, 15.00000000000794920 ) ) ;
#41276=LINE ( 'NONE', #20417, #48054 ) ;
#41277=ORIENTED_EDGE ( 'NONE', *, *, #62587, .F. ) ;
#41284=CARTESIAN_POINT ( 'NONE',  ( -11.75000000000000000, -5.200000000000001066, 26.25000000000000000 ) ) ;
#41285=VECTOR ( 'NONE', #3884, 1000.000000000000000 ) ;
#41287=EDGE_CURVE ( 'NONE', #51206, #27481, #8741, .T. ) ;
#41290=CARTESIAN_POINT ( 'NONE',  ( -25.50000000000000355, -5.200000000000001066, 20.49999999999999645 ) ) ;
#41297=ORIENTED_EDGE ( 'NONE', *, *, #20456, .F. ) ;
#41302=CARTESIAN_POINT ( 'NONE',  ( -30.00000000000000000, -9.200000000000120082, 17.30000000000000071 ) ) ;
#41307=VERTEX_POINT ( 'NONE', #62835 ) ;
#41312=DIRECTION ( 'NONE',  ( 1.000000000000000000, 0.000000000000000000, 0.000000000000000000 ) ) ;
#41313=AXIS2_PLACEMENT_3D ( 'NONE', #52148, #67704, #3016 ) ;
#41315=ORIENTED_EDGE ( 'NONE', *, *, #2569, .F. ) ;
#41327=VECTOR ( 'NONE', #23978, 1000.000000000000000 ) ;
#41330=CARTESIAN_POINT ( 'NONE',  ( -17.00000000000000000, -15.50000000000000000, 19.33772233983200195 ) ) ;
#41332=AXIS2_PLACEMENT_3D ( 'NONE', #47932, #69498, #15760 ) ;
#41336=DIRECTION ( 'NONE',  ( 0.000000000000000000, 0.000000000000000000, 1.000000000000000000 ) ) ;
#41345=DIRECTION ( 'NONE',  ( 0.000000000000000000, 0.7071067811865495711, -0.7071067811865455743 ) ) ;
#41346=DIRECTION ( 'NONE',  ( 0.000000000000000000, 0.000000000000000000, -1.000000000000000000 ) ) ;
#41359=CARTESIAN_POINT ( 'NONE',  ( 30.00000000000000000, -17.50000000000000000, -15.70500000000000007 ) ) ;
#41368=CARTESIAN_POINT ( 'NONE',  ( 30.00000000000000000, -11.70000000000000284, -12.50000000000000000 ) ) ;
#41376=CARTESIAN_POINT ( 'NONE',  ( -16.75000000000000000, -0.2038245569916330158, -21.77831216351300014 ) ) ;
#41389=ORIENTED_EDGE ( 'NONE', *, *, #5304, .F. ) ;
#41393=EDGE_CURVE ( 'NONE', #27989, #33676, #4153, .T. ) ;
#41396=ORIENTED_EDGE ( 'NONE', *, *, #13351, .T. ) ;
#41400=ORIENTED_EDGE ( 'NONE', *, *, #14717, .T. ) ;
#41401=ORIENTED_EDGE ( 'NONE', *, *, #7810, .F. ) ;
#41403=CARTESIAN_POINT ( 'NONE',  ( 30.00000000000000000, -5.599999999999999645, 27.00000000000000000 ) ) ;
#41427=AXIS2_PLACEMENT_3D ( 'NONE', #24578, #67359, #8291 ) ;
#41428=DIRECTION ( 'NONE',  ( -1.000000000000000000, 0.000000000000000000, 0.000000000000000000 ) ) ;
#41452=CARTESIAN_POINT ( 'NONE',  ( -17.24945551514599984, -15.50000000000000000, -25.53140320652400064 ) ) ;
#41462=VERTEX_POINT ( 'NONE', #31384 ) ;
#41467=DIRECTION ( 'NONE',  ( 1.000000000000000000, 0.000000000000000000, 0.000000000000000000 ) ) ;
#41468=EDGE_CURVE ( 'NONE', #33465, #24609, #64585, .T. ) ;
#41474=EDGE_LOOP ( 'NONE', ( #49041, #36721, #22516, #37215 ) ) ;
#41479=LINE ( 'NONE', #25578, #32216 ) ;
#41494=ORIENTED_EDGE ( 'NONE', *, *, #38201, .T. ) ;
#41512=DIRECTION ( 'NONE',  ( 0.000000000000000000, 1.000000000000000000, 0.000000000000000000 ) ) ;
#41519=CYLINDRICAL_SURFACE ( 'NONE', #65617, 3.499999999999999556 ) ;
#41533=CARTESIAN_POINT ( 'NONE',  ( -11.00000000000000000, -12.00000000000000000, 11.03137303340310282 ) ) ;
#41534=CARTESIAN_POINT ( 'NONE',  ( -17.00000000000000000, -16.28999999999999915, 14.50000000000000000 ) ) ;
#41536=CARTESIAN_POINT ( 'NONE',  ( -30.00000000000000000, -9.454754784057099570, 17.53999999999999915 ) ) ;
#41539=VERTEX_POINT ( 'NONE', #32748 ) ;
#41545=LINE ( 'NONE', #63110, #63294 ) ;
#41557=ORIENTED_EDGE ( 'NONE', *, *, #185, .T. ) ;
#41558=VERTEX_POINT ( 'NONE', #49022 ) ;
#41566=VERTEX_POINT ( 'NONE', #38409 ) ;
#41569=CARTESIAN_POINT ( 'NONE',  ( 15.70366306705349757, -0.2717122460102775472, 21.17420925361331641 ) ) ;
#41577=CARTESIAN_POINT ( 'NONE',  ( 30.00000000000000000, -9.200000000000120082, -17.30000000000000071 ) ) ;
#41589=EDGE_CURVE ( 'NONE', #53596, #28131, #39535, .T. ) ;
#41611=CARTESIAN_POINT ( 'NONE',  ( 30.00000000000000000, -13.79999999999979998, -17.30000000000000071 ) ) ;
#41612=DIRECTION ( 'NONE',  ( 0.000000000000000000, 0.000000000000000000, 1.000000000000000000 ) ) ;
#41633=DIRECTION ( 'NONE',  ( 0.000000000000000000, 0.7084617869628681008, 0.7057491738665939707 ) ) ;
#41635=ORIENTED_EDGE ( 'NONE', *, *, #46226, .F. ) ;
#41639=AXIS2_PLACEMENT_3D ( 'NONE', #28211, #1012, #65697 ) ;
#41640=CARTESIAN_POINT ( 'NONE',  ( 11.00000000000000000, -12.00000000000000000, 10.52786404500095863 ) ) ;
#41644=ORIENTED_EDGE ( 'NONE', *, *, #8795, .T. ) ;
#41666=DIRECTION ( 'NONE',  ( 0.000000000000000000, 0.000000000000000000, 1.000000000000000000 ) ) ;
#41667=LINE ( 'NONE', #19739, #27865 ) ;
#41685=LINE ( 'NONE', #9519, #61750 ) ;
#41686=EDGE_CURVE ( 'NONE', #67430, #54079, #2308, .T. ) ;
#41689=VECTOR ( 'NONE', #36655, 1000.000000000000000 ) ;
#41697=DIRECTION ( 'NONE',  ( -0.000000000000000000, 1.000000000000000000, -0.000000000000000000 ) ) ;
#41699=DIRECTION ( 'NONE',  ( 0.000000000000000000, 1.000000000000000000, 0.000000000000000000 ) ) ;
#41700=FACE_OUTER_BOUND ( 'NONE', #35419, .T. ) ;
#41704=CARTESIAN_POINT ( 'NONE',  ( 11.00000000000000000, -11.50000000000100009, 15.00000000000084910 ) ) ;
#41717=DIRECTION ( 'NONE',  ( 0.000000000000000000, 1.000000000000000000, 0.000000000000000000 ) ) ;
#41725=CARTESIAN_POINT ( 'NONE',  ( 25.50000000000000355, -5.578999999999999737, -22.50000000000000000 ) ) ;
#41745=FACE_OUTER_BOUND ( 'NONE', #51032, .T. ) ;
#41747=ORIENTED_EDGE ( 'NONE', *, *, #25673, .T. ) ;
#41749=PLANE ( 'NONE',  #60172 ) ;
#41750=ADVANCED_FACE ( 'NONE', ( #62388 ), #18083, .F. ) ;
#41762=LINE ( 'NONE', #53441, #53880 ) ;
#41765=CARTESIAN_POINT ( 'NONE',  ( 30.00000000000000000, -9.200000000000120082, -17.30000000000000071 ) ) ;
#41769=AXIS2_PLACEMENT_3D ( 'NONE', #3812, #25746, #19707 ) ;
#41771=DIRECTION ( 'NONE',  ( 0.000000000000000000, 0.000000000000000000, -1.000000000000000000 ) ) ;
#41792=ORIENTED_EDGE ( 'NONE', *, *, #28502, .T. ) ;
#41793=CARTESIAN_POINT ( 'NONE',  ( 24.00000000000000000, -15.50000000000000000, -14.50000000000000000 ) ) ;
#41799=CIRCLE ( 'NONE', #11308, 0.3499999999999611200 ) ;
#41801=DIRECTION ( 'NONE',  ( 0.000000000000000000, -1.000000000000000000, 0.000000000000000000 ) ) ;
#41808=DIRECTION ( 'NONE',  ( 0.000000000000000000, -1.000000000000000000, 0.000000000000000000 ) ) ;
#41809=CARTESIAN_POINT ( 'NONE',  ( 22.14589803375000088, -15.50000000000000000, -21.50000000000000000 ) ) ;
#41812=CARTESIAN_POINT ( 'NONE',  ( 29.50000000000000355, -12.00000000000000000, 10.69999999999999929 ) ) ;
#41813=LINE ( 'NONE', #4362, #52554 ) ;
#41830=AXIS2_PLACEMENT_3D ( 'NONE', #31373, #4141, #63170 ) ;
#41832=VERTEX_POINT ( 'NONE', #58858 ) ;
#41838=EDGE_CURVE ( 'NONE', #22707, #49327, #69111, .T. ) ;
#41841=ORIENTED_EDGE ( 'NONE', *, *, #67100, .F. ) ;
#41845=CARTESIAN_POINT ( 'NONE',  ( 30.00000000000000000, -5.200000000000001066, 9.400000000000000355 ) ) ;
#41850=CIRCLE ( 'NONE', #21511, 4.000000000000001776 ) ;
#41859=ADVANCED_FACE ( 'NONE', ( #15375 ), #25275, .F. ) ;
#41864=CARTESIAN_POINT ( 'NONE',  ( -11.00000000000000000, -16.28999999999999915, 14.50000000000000000 ) ) ;
#41887=VECTOR ( 'NONE', #5473, 1000.000000000000114 ) ;
#41898=VERTEX_POINT ( 'NONE', #56625 ) ;
#41907=EDGE_CURVE ( 'NONE', #32441, #56741, #67936, .T. ) ;
#41908=DIRECTION ( 'NONE',  ( 0.000000000000000000, 1.000000000000000000, 0.000000000000000000 ) ) ;
#41911=VERTEX_POINT ( 'NONE', #2876 ) ;
#41912=VERTEX_POINT ( 'NONE', #8881 ) ;
#41913=EDGE_CURVE ( 'NONE', #62767, #25535, #2184, .T. ) ;
#41914=CARTESIAN_POINT ( 'NONE',  ( 30.00000000000000000, -16.28999999999710369, -15.00000000000794920 ) ) ;
#41915=CARTESIAN_POINT ( 'NONE',  ( 15.50000000000000000, -0.2000000000000000111, -19.19999999702029925 ) ) ;
#41930=VERTEX_POINT ( 'NONE', #14188 ) ;
#41931=ADVANCED_FACE ( 'NONE', ( #24092 ), #19839, .F. ) ;
#41942=EDGE_CURVE ( 'NONE', #19212, #35877, #19141, .T. ) ;
#41948=CARTESIAN_POINT ( 'NONE',  ( -29.50000000000000355, -12.00000000000000000, 11.03137303340310282 ) ) ;
#41951=CARTESIAN_POINT ( 'NONE',  ( 23.48000000000000043, -15.50000000000000000, -26.00000000000000355 ) ) ;
#41962=DIRECTION ( 'NONE',  ( 1.000000000000000000, -0.000000000000000000, -0.000000000000000000 ) ) ;
#41978=CARTESIAN_POINT ( 'NONE',  ( -14.45366306705349757, -0.2717122460102549542, 23.33927276307431242 ) ) ;
#41985=CARTESIAN_POINT ( 'NONE',  ( 16.75000000000000000, -2.500000000000000000, 21.77831216351300014 ) ) ;
#42008=ADVANCED_FACE ( 'NONE', ( #9953 ), #37515, .F. ) ;
#42009=CARTESIAN_POINT ( 'NONE',  ( -29.50000000000000355, -11.50000000000100009, -15.00000000000084910 ) ) ;
#42011=ORIENTED_EDGE ( 'NONE', *, *, #30659, .F. ) ;
#42013=CARTESIAN_POINT ( 'NONE',  ( -25.50000000000000355, -5.200000000000001066, 22.50000000000000000 ) ) ;
#42026=CARTESIAN_POINT ( 'NONE',  ( -30.00000000000000000, -11.50000000000100009, -15.00000000000084910 ) ) ;
#42031=AXIS2_PLACEMENT_3D ( 'NONE', #61904, #56598, #33974 ) ;
#42034=DIRECTION ( 'NONE',  ( -1.000000000000000000, 0.000000000000000000, 0.000000000000000000 ) ) ;
#42035=AXIS2_PLACEMENT_3D ( 'NONE', #60675, #594, #12565 ) ;
#42048=VECTOR ( 'NONE', #61065, 1000.000000000000000 ) ;
#42051=CARTESIAN_POINT ( 'NONE',  ( 25.50000000000000355, -5.200000000000001066, -22.50000000000000000 ) ) ;
#42060=DIRECTION ( 'NONE',  ( 0.000000000000000000, 1.000000000000000000, 0.000000000000000000 ) ) ;
#42071=ORIENTED_EDGE ( 'NONE', *, *, #60603, .T. ) ;
#42072=VECTOR ( 'NONE', #38389, 1000.000000000000000 ) ;
#42081=AXIS2_PLACEMENT_3D ( 'NONE', #10269, #32544, #38531 ) ;
#42089=EDGE_CURVE ( 'NONE', #47121, #11595, #56557, .T. ) ;
#42090=EDGE_CURVE ( 'NONE', #62566, #5332, #1204, .T. ) ;
#42096=AXIS2_PLACEMENT_3D ( 'NONE', #42305, #14744, #36304 ) ;
#42099=CARTESIAN_POINT ( 'NONE',  ( -11.50000000000000000, -11.70000000000012008, -10.70000000000011831 ) ) ;
#42110=FACE_BOUND ( 'NONE', #62980, .T. ) ;
#42112=LINE ( 'NONE', #14904, #48637 ) ;
#42113=DIRECTION ( 'NONE',  ( 0.000000000000000000, 0.000000000000000000, 1.000000000000000000 ) ) ;
#42122=FACE_OUTER_BOUND ( 'NONE', #9732, .T. ) ;
#42126=EDGE_CURVE ( 'NONE', #22030, #13975, #32203, .T. ) ;
#42135=DIRECTION ( 'NONE',  ( 1.000000000000000000, 0.000000000000000000, 0.000000000000000000 ) ) ;
#42143=VECTOR ( 'NONE', #36049, 1000.000000000000000 ) ;
#42146=DIRECTION ( 'NONE',  ( 0.000000000000000000, 0.000000000000000000, 1.000000000000000000 ) ) ;
#42147=AXIS2_PLACEMENT_3D ( 'NONE', #42316, #63896, #53990 ) ;
#42157=ORIENTED_EDGE ( 'NONE', *, *, #9285, .T. ) ;
#42164=VERTEX_POINT ( 'NONE', #7043 ) ;
#42166=EDGE_LOOP ( 'NONE', ( #46428, #52846 ) ) ;
#42172=DIRECTION ( 'NONE',  ( 0.8660254037844482555, 0.000000000000000000, 0.4999999999999831801 ) ) ;
#42180=EDGE_CURVE ( 'NONE', #8072, #51926, #61128, .T. ) ;
#42185=FACE_OUTER_BOUND ( 'NONE', #10564, .T. ) ;
#42188=ORIENTED_EDGE ( 'NONE', *, *, #50946, .F. ) ;
#42190=EDGE_LOOP ( 'NONE', ( #49635, #13338, #40943, #50009 ) ) ;
#42191=VECTOR ( 'NONE', #49530, 1000.000000000000000 ) ;
#42199=DIRECTION ( 'NONE',  ( 0.000000000000000000, 0.000000000000000000, 1.000000000000000000 ) ) ;
#42206=AXIS2_PLACEMENT_3D ( 'NONE', #27306, #48519, #65812 ) ;
#42208=ORIENTED_EDGE ( 'NONE', *, *, #13666, .F. ) ;
#42228=ORIENTED_EDGE ( 'NONE', *, *, #51825, .T. ) ;
#42236=VERTEX_POINT ( 'NONE', #32563 ) ;
#42238=ORIENTED_EDGE ( 'NONE', *, *, #41393, .T. ) ;
#42240=CARTESIAN_POINT ( 'NONE',  ( -11.50000000000000000, -15.46862696659690073, -14.50000000000000000 ) ) ;
#42250=ORIENTED_EDGE ( 'NONE', *, *, #62662, .T. ) ;
#42252=CIRCLE ( 'NONE', #5014, 3.300000002979700753 ) ;
#42254=DIRECTION ( 'NONE',  ( 0.000000000000000000, 0.000000000000000000, -1.000000000000000000 ) ) ;
#42264=VERTEX_POINT ( 'NONE', #27936 ) ;
#42273=FACE_OUTER_BOUND ( 'NONE', #68160, .T. ) ;
#42283=VECTOR ( 'NONE', #61692, 1000.000000000000000 ) ;
#42285=CARTESIAN_POINT ( 'NONE',  ( 29.25000000000000000, -5.000000000000000000, 26.25000000000000000 ) ) ;
#42286=DIRECTION ( 'NONE',  ( 0.9583148474998867128, 0.000000000000000000, -0.2857142857143631365 ) ) ;
#42294=EDGE_CURVE ( 'NONE', #29870, #32597, #14831, .T. ) ;
#42297=VERTEX_POINT ( 'NONE', #1745 ) ;
#42301=ADVANCED_FACE ( 'NONE', ( #55158 ), #23319, .T. ) ;
#42305=CARTESIAN_POINT ( 'NONE',  ( 15.50000000000000000, -5.000000000000000000, -22.50000000000000000 ) ) ;
#42307=VECTOR ( 'NONE', #60768, 1000.000000000000000 ) ;
#42316=CARTESIAN_POINT ( 'NONE',  ( -23.48000000000000043, -15.50000000000000000, -26.00000000000000355 ) ) ;
#42322=CARTESIAN_POINT ( 'NONE',  ( 11.75000000000000000, -5.200000000000001066, 26.25000000000000000 ) ) ;
#42324=ORIENTED_EDGE ( 'NONE', *, *, #38445, .F. ) ;
#42326=DIRECTION ( 'NONE',  ( 1.000000000000000000, 0.000000000000000000, 0.000000000000000000 ) ) ;
#42334=DIRECTION ( 'NONE',  ( 0.000000000000000000, 1.000000000000000000, 0.000000000000000000 ) ) ;
#42340=DIRECTION ( 'NONE',  ( 0.000000000000000000, -1.000000000000000000, 0.000000000000000000 ) ) ;
#42341=DIRECTION ( 'NONE',  ( 0.000000000000000000, 0.7057491738665943037, -0.7084617869628675457 ) ) ;
#42343=AXIS2_PLACEMENT_3D ( 'NONE', #1056, #60086, #6354 ) ;
#42354=CIRCLE ( 'NONE', #24274, 4.000000000000000888 ) ;
#42359=EDGE_CURVE ( 'NONE', #32779, #38222, #29499, .T. ) ;
#42368=DIRECTION ( 'NONE',  ( 0.000000000000000000, 0.000000000000000000, 1.000000000000000000 ) ) ;
#42369=DIRECTION ( 'NONE',  ( 0.000000000000000000, -0.9921567416492215186, -0.1249999999999996531 ) ) ;
#42382=DIRECTION ( 'NONE',  ( -0.000000000000000000, 1.000000000000000000, -0.000000000000000000 ) ) ;
#42386=CARTESIAN_POINT ( 'NONE',  ( 11.50000000000000000, -12.00000000000000000, 11.00000000000000000 ) ) ;
#42390=VECTOR ( 'NONE', #15415, 1000.000000000000000 ) ;
#42401=DIRECTION ( 'NONE',  ( 0.000000000000000000, 0.000000000000000000, 1.000000000000000000 ) ) ;
#42415=CARTESIAN_POINT ( 'NONE',  ( 11.00000000000000000, -17.14999999999999858, -27.00000000000000000 ) ) ;
#42420=EDGE_CURVE ( 'NONE', #63841, #46765, #22029, .T. ) ;
#42421=CYLINDRICAL_SURFACE ( 'NONE', #3946, 4.500000000000189182 ) ;
#42425=CARTESIAN_POINT ( 'NONE',  ( -11.75000000000000000, -5.200000000000001066, -26.25000000000000000 ) ) ;
#42429=LINE ( 'NONE', #57990, #22272 ) ;
#42434=LINE ( 'NONE', #52353, #58118 ) ;
#42437=DIRECTION ( 'NONE',  ( 0.000000000000000000, 0.000000000000000000, -1.000000000000000000 ) ) ;
#42442=EDGE_CURVE ( 'NONE', #48624, #35877, #26641, .T. ) ;
#42448=ORIENTED_EDGE ( 'NONE', *, *, #24906, .F. ) ;
#42454=VERTEX_POINT ( 'NONE', #22716 ) ;
#42457=CARTESIAN_POINT ( 'NONE',  ( 30.00000000000000000, -11.70000000000000284, -12.50000000000000000 ) ) ;
#42468=ORIENTED_EDGE ( 'NONE', *, *, #50026, .F. ) ;
#42476=CARTESIAN_POINT ( 'NONE',  ( 17.00000000000000000, -17.50000000000000000, -19.33772233983200195 ) ) ;
#42481=DIRECTION ( 'NONE',  ( -1.000000000000000000, 0.000000000000000000, 0.000000000000000000 ) ) ;
#42485=CARTESIAN_POINT ( 'NONE',  ( -16.74999999999999289, -0.3152037684892574076, 22.74589050208021490 ) ) ;
#42487=LINE ( 'NONE', #401, #9125 ) ;
#42513=ORIENTED_EDGE ( 'NONE', *, *, #33074, .T. ) ;
#42518=DIRECTION ( 'NONE',  ( -1.000000000000000000, 0.000000000000000000, 0.000000000000000000 ) ) ;
#42521=ORIENTED_EDGE ( 'NONE', *, *, #759, .F. ) ;
#42530=TOROIDAL_SURFACE ( 'NONE', #50441, 3.299999999999470024, 0.2000000000005275058 ) ;
#42531=ORIENTED_EDGE ( 'NONE', *, *, #60245, .T. ) ;
#42534=CARTESIAN_POINT ( 'NONE',  ( 25.50000000000000355, 0.000000000000000000, -24.12099999999999866 ) ) ;
#42539=ORIENTED_EDGE ( 'NONE', *, *, #27975, .F. ) ;
#42549=DIRECTION ( 'NONE',  ( 0.000000000000000000, 0.000000000000000000, -1.000000000000000000 ) ) ;
#42562=ORIENTED_EDGE ( 'NONE', *, *, #50200, .T. ) ;
#42565=AXIS2_PLACEMENT_3D ( 'NONE', #11663, #55511, #49170 ) ;
#42566=PLANE ( 'NONE',  #55818 ) ;
#42568=LINE ( 'NONE', #47181, #67485 ) ;
#42576=CARTESIAN_POINT ( 'NONE',  ( 25.50000000000000355, -5.200000000000001066, -22.50000000000000000 ) ) ;
#42577=DIRECTION ( 'NONE',  ( 0.000000000000000000, 0.000000000000000000, -1.000000000000000000 ) ) ;
#42579=AXIS2_PLACEMENT_3D ( 'NONE', #16578, #15876, #27873 ) ;
#42585=CARTESIAN_POINT ( 'NONE',  ( 30.00000000000000000, -17.35230188589299871, 15.35019951917099945 ) ) ;
#42587=AXIS2_PLACEMENT_3D ( 'NONE', #26138, #58662, #8816 ) ;
#42597=DIRECTION ( 'NONE',  ( 0.8660254037844482555, 0.000000000000000000, 0.4999999999999831801 ) ) ;
#42599=CARTESIAN_POINT ( 'NONE',  ( 30.00000000000000000, -11.50000000000000000, 11.00000000000000000 ) ) ;
#42600=CARTESIAN_POINT ( 'NONE',  ( -25.50000000000000355, -15.12100000000000044, 20.87900000000000134 ) ) ;
#42602=VECTOR ( 'NONE', #64228, 1000.000000000000000 ) ;
#42607=ORIENTED_EDGE ( 'NONE', *, *, #27582, .F. ) ;
#42608=ORIENTED_EDGE ( 'NONE', *, *, #52734, .T. ) ;
#42614=VERTEX_POINT ( 'NONE', #68985 ) ;
#42622=CARTESIAN_POINT ( 'NONE',  ( -11.00000000000000000, -12.00000000000000000, 12.20000000000000107 ) ) ;
#42625=DIRECTION ( 'NONE',  ( 0.000000000000000000, -0.8206518066484758123, -0.5714285714283042772 ) ) ;
#42636=ORIENTED_EDGE ( 'NONE', *, *, #18191, .T. ) ;
#42640=PRODUCT_DEFINITION_FORMATION_WITH_SPECIFIED_SOURCE ( 'ANY', '', #44806, .NOT_KNOWN. ) ;
#42645=CARTESIAN_POINT ( 'NONE',  ( 29.50000000000000355, -12.00000000000000000, 10.69999999999999929 ) ) ;
#42651=FACE_OUTER_BOUND ( 'NONE', #68778, .T. ) ;
#42654=LINE ( 'NONE', #14741, #28888 ) ;
#42660=DIRECTION ( 'NONE',  ( 0.000000000000000000, -1.000000000000000000, 0.000000000000000000 ) ) ;
#42664=DIRECTION ( 'NONE',  ( 0.7142857142857395036, 0.000000000000000000, 0.6998542122237394469 ) ) ;
#42668=CARTESIAN_POINT ( 'NONE',  ( 28.00000000000000000, -16.28999999999710369, -15.00000000000794920 ) ) ;
#42672=ORIENTED_EDGE ( 'NONE', *, *, #26809, .F. ) ;
#42680=CARTESIAN_POINT ( 'NONE',  ( -30.00000000000000000, -10.85999999999999943, 9.000000000000001776 ) ) ;
#42681=ORIENTED_EDGE ( 'NONE', *, *, #23716, .T. ) ;
#42693=ORIENTED_EDGE ( 'NONE', *, *, #1486, .F. ) ;
#42694=CARTESIAN_POINT ( 'NONE',  ( 23.75054448485400016, -15.50000000000000000, -25.53140320652400064 ) ) ;
#42696=VECTOR ( 'NONE', #21044, 1000.000000000000000 ) ;
#42698=CARTESIAN_POINT ( 'NONE',  ( 25.50000000000000355, -15.50000000000000000, -22.50000000000000000 ) ) ;
#42700=ORIENTED_EDGE ( 'NONE', *, *, #37463, .T. ) ;
#42714=VERTEX_POINT ( 'NONE', #48823 ) ;
#42716=CARTESIAN_POINT ( 'NONE',  ( -15.50000000000000000, -5.000000000000000000, -26.00000000000000000 ) ) ;
#42724=ORIENTED_EDGE ( 'NONE', *, *, #36692, .T. ) ;
#42725=EDGE_CURVE ( 'NONE', #32135, #64214, #21648, .T. ) ;
#42738=DIRECTION ( 'NONE',  ( -1.000000000000000000, 0.000000000000000000, 0.000000000000000000 ) ) ;
#42739=CIRCLE ( 'NONE', #43895, 4.500000000000190958 ) ;
#42741=ORIENTED_EDGE ( 'NONE', *, *, #53243, .F. ) ;
#42754=DIRECTION ( 'NONE',  ( -1.000000000000000000, 0.000000000000000000, 0.000000000000000000 ) ) ;
#42757=CARTESIAN_POINT ( 'NONE',  ( -11.00000000000000000, -8.959999999999999076, -12.95475478405700009 ) ) ;
#42758=EDGE_CURVE ( 'NONE', #7139, #41138, #22796, .T. ) ;
#42759=CIRCLE ( 'NONE', #22427, 4.000000000000000000 ) ;
#42762=ORIENTED_EDGE ( 'NONE', *, *, #31422, .T. ) ;
#42774=ORIENTED_EDGE ( 'NONE', *, *, #46633, .T. ) ;
#42791=ORIENTED_EDGE ( 'NONE', *, *, #33247, .T. ) ;
#42793=VECTOR ( 'NONE', #19153, 1000.000000000000000 ) ;
#42796=DIRECTION ( 'NONE',  ( 0.000000000000000000, -0.1249999999999996531, 0.9921567416492215186 ) ) ;
#42801=CYLINDRICAL_SURFACE ( 'NONE', #56071, 2.250000000000001776 ) ;
#42802=EDGE_CURVE ( 'NONE', #30786, #52350, #50186, .T. ) ;
#42811=PLANE ( 'NONE',  #30059 ) ;
#42822=LINE ( 'NONE', #42476, #54170 ) ;
#42832=EDGE_LOOP ( 'NONE', ( #32080, #51902, #17349, #4109 ) ) ;
#42835=CARTESIAN_POINT ( 'NONE',  ( 30.00000000000000000, -11.50000000000100009, 10.50000000000065903 ) ) ;
#42844=ORIENTED_EDGE ( 'NONE', *, *, #10257, .T. ) ;
#42846=CARTESIAN_POINT ( 'NONE',  ( -13.00000000000000178, -17.00000000000000000, -15.70499999999969809 ) ) ;
#42853=CYLINDRICAL_SURFACE ( 'NONE', #29513, 0.4000000000000617506 ) ;
#42854=VERTEX_POINT ( 'NONE', #33916 ) ;
#42862=CARTESIAN_POINT ( 'NONE',  ( 29.25000000000000000, -5.000000000000000000, 60.00000000000000000 ) ) ;
#42874=ORIENTED_EDGE ( 'NONE', *, *, #27582, .T. ) ;
#42875=ORIENTED_EDGE ( 'NONE', *, *, #65392, .T. ) ;
#42905=EDGE_LOOP ( 'NONE', ( #30270, #52596, #32008, #14245 ) ) ;
#42912=FACE_OUTER_BOUND ( 'NONE', #29863, .T. ) ;
#42914=AXIS2_PLACEMENT_3D ( 'NONE', #45459, #7635, #62415 ) ;
#42915=CARTESIAN_POINT ( 'NONE',  ( 25.50000000000000355, -5.578999999999999737, -24.12099999999999511 ) ) ;
#42916=ORIENTED_EDGE ( 'NONE', *, *, #47941, .F. ) ;
#42918=DIRECTION ( 'NONE',  ( 0.000000000000000000, 0.000000000000000000, -1.000000000000000000 ) ) ;
#42927=EDGE_CURVE ( 'NONE', #68445, #44549, #60214, .T. ) ;
#42938=CARTESIAN_POINT ( 'NONE',  ( -19.00000000000000000, -5.000000000000000000, -22.50000000000000000 ) ) ;
#42946=FACE_OUTER_BOUND ( 'NONE', #19429, .T. ) ;
#42956=EDGE_CURVE ( 'NONE', #32328, #36815, #51596, .T. ) ;
#42957=EDGE_LOOP ( 'NONE', ( #57913, #3355, #27205, #23554 ) ) ;
#42958=ORIENTED_EDGE ( 'NONE', *, *, #56682, .F. ) ;
#42971=ORIENTED_EDGE ( 'NONE', *, *, #27070, .F. ) ;
#42974=EDGE_CURVE ( 'NONE', #32181, #57411, #8436, .T. ) ;
#42984=VECTOR ( 'NONE', #24452, 1000.000000000000000 ) ;
#42994=LINE ( 'NONE', #22485, #2623 ) ;
#43013=DIRECTION ( 'NONE',  ( 0.000000000000000000, 0.000000000000000000, 1.000000000000000000 ) ) ;
#43018=CARTESIAN_POINT ( 'NONE',  ( 25.49999999999869971, -17.50000000000000000, 22.50000000000000000 ) ) ;
#43020=CARTESIAN_POINT ( 'NONE',  ( 15.50000000000000000, -2.500000000000000000, -23.94337567297399971 ) ) ;
#43022=ORIENTED_EDGE ( 'NONE', *, *, #6171, .T. ) ;
#43032=DIRECTION ( 'NONE',  ( 0.000000000000000000, -1.000000000000000000, 0.000000000000000000 ) ) ;
#43036=ORIENTED_EDGE ( 'NONE', *, *, #10471, .T. ) ;
#43038=AXIS2_PLACEMENT_3D ( 'NONE', #50814, #56135, #29595 ) ;
#43051=AXIS2_PLACEMENT_3D ( 'NONE', #20934, #25199, #68695 ) ;
#43053=CARTESIAN_POINT ( 'NONE',  ( -11.00000000000000000, -10.85999999999999943, 9.000000000000001776 ) ) ;
#43054=VECTOR ( 'NONE', #19750, 1000.000000000000000 ) ;
#43060=CARTESIAN_POINT ( 'NONE',  ( 14.05000000000000249, -0.2000000000000000111, -22.50000000000000000 ) ) ;
#43071=DIRECTION ( 'NONE',  ( -1.000000000000000000, 0.000000000000000000, 0.000000000000000000 ) ) ;
#43074=ORIENTED_EDGE ( 'NONE', *, *, #46233, .T. ) ;
#43077=DIRECTION ( 'NONE',  ( 0.000000000000000000, 0.000000000000000000, 1.000000000000000000 ) ) ;
#43082=CARTESIAN_POINT ( 'NONE',  ( 30.00000000000000000, -10.85999999999999943, -9.350000000000269651 ) ) ;
#43083=DIRECTION ( 'NONE',  ( 1.000000000000000000, 0.000000000000000000, 0.000000000000000000 ) ) ;
#43090=ORIENTED_EDGE ( 'NONE', *, *, #54793, .F. ) ;
#43111=DIRECTION ( 'NONE',  ( 0.000000000000000000, 0.000000000000000000, 1.000000000000000000 ) ) ;
#43117=CARTESIAN_POINT ( 'NONE',  ( -29.50000000000000355, -11.50000000000000000, 11.00000000000000000 ) ) ;
#43123=DIRECTION ( 'NONE',  ( 1.000000000000000000, -0.000000000000000000, -0.000000000000000000 ) ) ;
#43126=VERTEX_POINT ( 'NONE', #66375 ) ;
#43130=EDGE_LOOP ( 'NONE', ( #943, #37821, #28156, #53245 ) ) ;
#43143=DIRECTION ( 'NONE',  ( 0.000000000000000000, 0.000000000000000000, 1.000000000000000000 ) ) ;
#43145=ADVANCED_FACE ( 'NONE', ( #66710 ), #996, .F. ) ;
#43148=AXIS2_PLACEMENT_3D ( 'NONE', #18661, #7004, #1373 ) ;
#43169=CYLINDRICAL_SURFACE ( 'NONE', #15246, 4.000000000000000000 ) ;
#43170=ORIENTED_EDGE ( 'NONE', *, *, #32352, .F. ) ;
#43178=EDGE_CURVE ( 'NONE', #24440, #41462, #49761, .T. ) ;
#43181=CARTESIAN_POINT ( 'NONE',  ( -24.00000000000000000, -16.28999999999999915, -14.50000000000000000 ) ) ;
#43182=VECTOR ( 'NONE', #58995, 1000.000000000000000 ) ;
#43191=DIRECTION ( 'NONE',  ( 0.000000000000000000, 0.000000000000000000, 1.000000000000000000 ) ) ;
#43192=ADVANCED_FACE ( 'NONE', ( #1328, #39152 ), #45481, .T. ) ;
#43195=EDGE_CURVE ( 'NONE', #55585, #34045, #2361, .T. ) ;
#43199=DIRECTION ( 'NONE',  ( 1.000000000000000000, -0.000000000000000000, -0.000000000000000000 ) ) ;
#43200=ORIENTED_EDGE ( 'NONE', *, *, #52564, .F. ) ;
#43201=EDGE_LOOP ( 'NONE', ( #45803, #14651, #7647, #8791 ) ) ;
#43202=DIRECTION ( 'NONE',  ( -0.000000000000000000, 1.000000000000000000, -0.000000000000000000 ) ) ;
#43204=CYLINDRICAL_SURFACE ( 'NONE', #42206, 0.5000000000079367624 ) ;
#43206=ADVANCED_FACE ( 'NONE', ( #18615 ), #35215, .F. ) ;
#43234=EDGE_LOOP ( 'NONE', ( #53044, #62430, #38286, #38598 ) ) ;
#43238=EDGE_LOOP ( 'NONE', ( #49243, #44477, #63501, #26227 ) ) ;
#43248=CARTESIAN_POINT ( 'NONE',  ( 15.91242688423647955, -0.3152598339557988183, 23.70526090033903799 ) ) ;
#43253=CARTESIAN_POINT ( 'NONE',  ( -29.50000000000000355, -11.50000000000000000, -11.00000000000000000 ) ) ;
#43256=DIRECTION ( 'NONE',  ( 0.000000000000000000, -1.000000000000000000, 0.000000000000000000 ) ) ;
#43267=ORIENTED_EDGE ( 'NONE', *, *, #54492, .T. ) ;
#43269=CARTESIAN_POINT ( 'NONE',  ( -30.00000000000000000, -5.000000000000000000, -27.00000000000000000 ) ) ;
#43271=ADVANCED_FACE ( 'NONE', ( #30292 ), #40883, .F. ) ;
#43277=EDGE_CURVE ( 'NONE', #29771, #30686, #22031, .T. ) ;
#43283=DIRECTION ( 'NONE',  ( 0.000000000000000000, -1.000000000000000000, 0.000000000000000000 ) ) ;
#43304=EDGE_LOOP ( 'NONE', ( #53288, #37898, #67238, #22828 ) ) ;
#43308=CARTESIAN_POINT ( 'NONE',  ( -29.50000000000000355, -12.00000000000000000, -11.00000000000000000 ) ) ;
#43313=ORIENTED_EDGE ( 'NONE', *, *, #32325, .T. ) ;
#43314=DIRECTION ( 'NONE',  ( 0.000000000000000000, 0.000000000000000000, 1.000000000000000000 ) ) ;
#43321=LINE ( 'NONE', #44689, #26179 ) ;
#43327=ORIENTED_EDGE ( 'NONE', *, *, #3664, .T. ) ;
#43354=CARTESIAN_POINT ( 'NONE',  ( -13.00000000000000178, -16.64230188589299786, -14.64519951917100116 ) ) ;
#43355=LINE ( 'NONE', #58935, #9581 ) ;
#43363=ORIENTED_EDGE ( 'NONE', *, *, #63155, .T. ) ;
#43366=DIRECTION ( 'NONE',  ( 0.000000000000000000, -1.000000000000000000, 0.000000000000000000 ) ) ;
#43372=DIRECTION ( 'NONE',  ( 1.000000000000000000, 0.000000000000000000, 0.000000000000000000 ) ) ;
#43374=ORIENTED_EDGE ( 'NONE', *, *, #20933, .F. ) ;
#43383=CARTESIAN_POINT ( 'NONE',  ( 14.25000000000000000, -2.500000000000000000, 23.22168783648699986 ) ) ;
#43387=AXIS2_PLACEMENT_3D ( 'NONE', #41704, #53034, #47712 ) ;
#43394=DIRECTION ( 'NONE',  ( 0.000000000000000000, 1.000000000000000000, 0.000000000000000000 ) ) ;
#43401=EDGE_CURVE ( 'NONE', #12841, #5665, #65523, .T. ) ;
#43405=EDGE_CURVE ( 'NONE', #17638, #4595, #55943, .T. ) ;
#43409=EDGE_LOOP ( 'NONE', ( #44001, #52603, #557, #55466, #8849, #39382, #32349, #39605, #28539, #42681, #4583, #18885, #65901, #67701, #52191, #10570, #68332, #56958 ) ) ;
#43412=ORIENTED_EDGE ( 'NONE', *, *, #51003, .T. ) ;
#43417=CYLINDRICAL_SURFACE ( 'NONE', #22336, 0.3500000000009988455 ) ;
#43423=CARTESIAN_POINT ( 'NONE',  ( -17.00000000000000000, -17.50000000000000000, 15.70500000000000007 ) ) ;
#43429=FACE_OUTER_BOUND ( 'NONE', #34142, .T. ) ;
#43431=ORIENTED_EDGE ( 'NONE', *, *, #63833, .F. ) ;
#43432=DIRECTION ( 'NONE',  ( 0.000000000000000000, 0.000000000000000000, 1.000000000000000000 ) ) ;
#43438=DIRECTION ( 'NONE',  ( 0.000000000000000000, 1.000000000000000000, 0.000000000000000000 ) ) ;
#43439=DIRECTION ( 'NONE',  ( 0.000000000000000000, -0.1111111111108840643, -0.9938079899999319178 ) ) ;
#43445=EDGE_CURVE ( 'NONE', #64218, #1941, #16375, .T. ) ;
#43448=ORIENTED_EDGE ( 'NONE', *, *, #15531, .T. ) ;
#43458=ORIENTED_EDGE ( 'NONE', *, *, #53543, .F. ) ;
#43462=EDGE_CURVE ( 'NONE', #41832, #13102, #44620, .T. ) ;
#43465=LINE ( 'NONE', #342, #37203 ) ;
#43470=LINE ( 'NONE', #49131, #13106 ) ;
#43473=ORIENTED_EDGE ( 'NONE', *, *, #22390, .T. ) ;
#43478=DIRECTION ( 'NONE',  ( 0.000000000000000000, -1.000000000000000000, 0.000000000000000000 ) ) ;
#43484=ORIENTED_EDGE ( 'NONE', *, *, #11857, .F. ) ;
#43490=ORIENTED_EDGE ( 'NONE', *, *, #60447, .F. ) ;
#43495=DIRECTION ( 'NONE',  ( 0.000000000000000000, -1.000000000000000000, 0.000000000000000000 ) ) ;
#43497=ORIENTED_EDGE ( 'NONE', *, *, #30936, .T. ) ;
#43499=VERTEX_POINT ( 'NONE', #34715 ) ;
#43500=CARTESIAN_POINT ( 'NONE',  ( 30.00000000000000000, -15.97213595500069871, 14.50000000000000000 ) ) ;
#43501=VECTOR ( 'NONE', #52624, 1000.000000000000000 ) ;
#43502=CIRCLE ( 'NONE', #2863, 4.000000000000000000 ) ;
#43511=ORIENTED_EDGE ( 'NONE', *, *, #156, .T. ) ;
#43515=DIRECTION ( 'NONE',  ( -1.000000000000000000, 0.000000000000000000, 0.000000000000000000 ) ) ;
#43516=VERTEX_POINT ( 'NONE', #50285 ) ;
#43524=ORIENTED_EDGE ( 'NONE', *, *, #42956, .F. ) ;
#43533=TOROIDAL_SURFACE ( 'NONE', #4188, 3.299999999999474909, 0.2000000000005234813 ) ;
#43537=EDGE_CURVE ( 'NONE', #51205, #35164, #48022, .T. ) ;
#43538=VECTOR ( 'NONE', #8387, 1000.000000000000000 ) ;
#43541=DIRECTION ( 'NONE',  ( -1.000000000000000000, 0.000000000000000000, 0.000000000000000000 ) ) ;
#43542=EDGE_LOOP ( 'NONE', ( #14611, #4205, #4254, #31649 ) ) ;
#43543=EDGE_CURVE ( 'NONE', #35617, #7006, #56292, .T. ) ;
#43548=ORIENTED_EDGE ( 'NONE', *, *, #16730, .T. ) ;
#43570=CARTESIAN_POINT ( 'NONE',  ( -29.50000000000000355, -11.70000000000000284, -11.00000000000000000 ) ) ;
#43574=VERTEX_POINT ( 'NONE', #62635 ) ;
#43580=ADVANCED_FACE ( 'NONE', ( #35767, #63355 ), #30819, .T. ) ;
#43583=CARTESIAN_POINT ( 'NONE',  ( -11.50000000000000000, -12.00000000000000000, 11.00000000000000000 ) ) ;
#43584=ORIENTED_EDGE ( 'NONE', *, *, #50264, .F. ) ;
#43590=VERTEX_POINT ( 'NONE', #58037 ) ;
#43591=ORIENTED_EDGE ( 'NONE', *, *, #5561, .T. ) ;
#43603=VERTEX_POINT ( 'NONE', #52763 ) ;
#43608=DIRECTION ( 'NONE',  ( 1.000000000000000000, -0.000000000000000000, -0.000000000000000000 ) ) ;
#43615=ADVANCED_FACE ( 'NONE', ( #68662 ), #20207, .T. ) ;
#43618=ORIENTED_EDGE ( 'NONE', *, *, #17321, .F. ) ;
#43620=LINE ( 'NONE', #27701, #14416 ) ;
#43623=CIRCLE ( 'NONE', #56030, 3.499999999999999556 ) ;
#43626=EDGE_CURVE ( 'NONE', #52249, #55561, #37531, .T. ) ;
#43627=DIRECTION ( 'NONE',  ( -1.000000000000000000, 0.000000000000000000, 0.000000000000000000 ) ) ;
#43652=EDGE_LOOP ( 'NONE', ( #2423, #53785, #37072, #14957 ) ) ;
#43659=( LENGTH_UNIT ( ) NAMED_UNIT ( * ) SI_UNIT ( .MILLI., .METRE. ) );
#43661=AXIS2_PLACEMENT_3D ( 'NONE', #58762, #69727, #22330 ) ;
#43672=AXIS2_PLACEMENT_3D ( 'NONE', #22291, #38877, #6369 ) ;
#43673=CARTESIAN_POINT ( 'NONE',  ( 11.50000000000000000, -11.50000000000000000, 15.00000000000000000 ) ) ;
#43678=FACE_OUTER_BOUND ( 'NONE', #56243, .T. ) ;
#43685=CARTESIAN_POINT ( 'NONE',  ( 25.50000000000000355, 0.000000000000000000, -22.50000000000000000 ) ) ;
#43686=ADVANCED_FACE ( 'NONE', ( #37876 ), #6388, .F. ) ;
#43687=ORIENTED_EDGE ( 'NONE', *, *, #23329, .T. ) ;
#43688=LINE ( 'NONE', #3850, #47291 ) ;
#43689=CARTESIAN_POINT ( 'NONE',  ( 30.00000000000000000, -12.00000000000000000, -11.03137303340310282 ) ) ;
#43693=LINE ( 'NONE', #54654, #60659 ) ;
#43697=EDGE_CURVE ( 'NONE', #35777, #22939, #11001, .T. ) ;
#43701=DIRECTION ( 'NONE',  ( -1.000000000000000000, 0.000000000000000000, 0.000000000000000000 ) ) ;
#43703=CARTESIAN_POINT ( 'NONE',  ( -11.00000000000000000, -17.35230188589299871, -15.35019951917099945 ) ) ;
#43705=VECTOR ( 'NONE', #24351, 1000.000000000000000 ) ;
#43712=CARTESIAN_POINT ( 'NONE',  ( -18.85410196625000268, -17.50000000000000000, 21.50000000000000000 ) ) ;
#43714=DIRECTION ( 'NONE',  ( -0.000000000000000000, 1.000000000000000000, -0.000000000000000000 ) ) ;
#43718=DIRECTION ( 'NONE',  ( 0.000000000000000000, 1.000000000000000000, 0.000000000000000000 ) ) ;
#43719=DIRECTION ( 'NONE',  ( 1.000000000000000000, -0.000000000000000000, -0.000000000000000000 ) ) ;
#43727=DIRECTION ( 'NONE',  ( -0.000000000000000000, 1.000000000000000000, -0.000000000000000000 ) ) ;
#43728=ORIENTED_EDGE ( 'NONE', *, *, #67406, .F. ) ;
#43732=LINE ( 'NONE', #37733, #63909 ) ;
#43759=ADVANCED_FACE ( 'NONE', ( #60120 ), #12353, .F. ) ;
#43768=ADVANCED_FACE ( 'NONE', ( #66119 ), #7059, .T. ) ;
#43770=VECTOR ( 'NONE', #9787, 1000.000000000000000 ) ;
#43774=ORIENTED_EDGE ( 'NONE', *, *, #50829, .T. ) ;
#43779=CARTESIAN_POINT ( 'NONE',  ( -30.00000000000000000, -11.50000000000000000, -15.00000000000000000 ) ) ;
#43782=FACE_OUTER_BOUND ( 'NONE', #27907, .T. ) ;
#43788=AXIS2_PLACEMENT_3D ( 'NONE', #50994, #62297, #56993 ) ;
#43793=CARTESIAN_POINT ( 'NONE',  ( -15.08565937784311473, -0.3156604612129270127, 21.29584399676446083 ) ) ;
#43794=LINE ( 'NONE', #22912, #30471 ) ;
#43823=VERTEX_POINT ( 'NONE', #23337 ) ;
#43825=DIRECTION ( 'NONE',  ( 0.000000000000000000, 0.000000000000000000, 1.000000000000000000 ) ) ;
#43837=DIRECTION ( 'NONE',  ( -0.3479852726768748461, 0.000000000000000000, -0.9375000000000006661 ) ) ;
#43842=DIRECTION ( 'NONE',  ( 0.000000000000000000, -0.7071067811865454633, -0.7071067811865496822 ) ) ;
#43843=EDGE_CURVE ( 'NONE', #67429, #26513, #66465, .T. ) ;
#43847=CARTESIAN_POINT ( 'NONE',  ( 11.50000000000000000, -11.50000000000000000, 11.00000000000000000 ) ) ;
#43859=CARTESIAN_POINT ( 'NONE',  ( -11.00000000000000000, -11.50000000000100009, 10.50000000000065903 ) ) ;
#43870=EDGE_LOOP ( 'NONE', ( #69640, #48192, #12207, #47213 ) ) ;
#43876=DIRECTION ( 'NONE',  ( 0.000000000000000000, -0.1111111111108840643, -0.9938079899999319178 ) ) ;
#43882=VERTEX_POINT ( 'NONE', #46289 ) ;
#43885=PLANE ( 'NONE',  #3752 ) ;
#43887=VECTOR ( 'NONE', #17126, 1000.000000000000000 ) ;
#43889=CARTESIAN_POINT ( 'NONE',  ( -11.00000000000000000, -17.50000000000000000, -26.64999999999999858 ) ) ;
#43892=CARTESIAN_POINT ( 'NONE',  ( 30.00000000000000000, -14.04000000000000092, 14.80000000000000071 ) ) ;
#43895=AXIS2_PLACEMENT_3D ( 'NONE', #63035, #18479, #67291 ) ;
#43898=FACE_BOUND ( 'NONE', #30347, .T. ) ;
#43904=DIRECTION ( 'NONE',  ( 0.000000000000000000, -1.000000000000000000, 0.000000000000000000 ) ) ;
#43918=CARTESIAN_POINT ( 'NONE',  ( 11.00000000000000000, -14.04000000000000092, 17.04524521594300523 ) ) ;
#43930=ORIENTED_EDGE ( 'NONE', *, *, #38033, .T. ) ;
#43953=EDGE_LOOP ( 'NONE', ( #14735, #68799, #46223, #58181 ) ) ;
#43955=CARTESIAN_POINT ( 'NONE',  ( -11.75000000000000000, -5.000000000000000000, 60.00000000000000000 ) ) ;
#43976=DIRECTION ( 'NONE',  ( 0.000000000000000000, 0.000000000000000000, -1.000000000000000000 ) ) ;
#43977=VECTOR ( 'NONE', #48106, 1000.000000000000000 ) ;
#43983=ORIENTED_EDGE ( 'NONE', *, *, #38372, .F. ) ;
#43985=EDGE_CURVE ( 'NONE', #5159, #45736, #22224, .T. ) ;
#43995=AXIS2_PLACEMENT_3D ( 'NONE', #50557, #2115, #3868 ) ;
#44001=ORIENTED_EDGE ( 'NONE', *, *, #31127, .T. ) ;
#44002=VECTOR ( 'NONE', #57270, 1000.000000000000000 ) ;
#44004=DIRECTION ( 'NONE',  ( 0.000000000000000000, 0.000000000000000000, 1.000000000000000000 ) ) ;
#44011=ORIENTED_EDGE ( 'NONE', *, *, #38391, .F. ) ;
#44017=ORIENTED_EDGE ( 'NONE', *, *, #10332, .F. ) ;
#44020=CARTESIAN_POINT ( 'NONE',  ( -22.14589803375000088, -17.50000000000000000, 21.50000000000000000 ) ) ;
#44031=VECTOR ( 'NONE', #5122, 1000.000000000000000 ) ;
#44043=DIRECTION ( 'NONE',  ( 0.000000000000000000, 0.000000000000000000, 1.000000000000000000 ) ) ;
#44045=CARTESIAN_POINT ( 'NONE',  ( 13.00000000000000178, -15.50000000000000000, 2.000000000000000000 ) ) ;
#44046=AXIS2_PLACEMENT_3D ( 'NONE', #62470, #29957, #40567 ) ;
#44051=ORIENTED_EDGE ( 'NONE', *, *, #40047, .T. ) ;
#44052=AXIS2_PLACEMENT_3D ( 'NONE', #28308, #50582, #33954 ) ;
#44054=VERTEX_POINT ( 'NONE', #21866 ) ;
#44061=LINE ( 'NONE', #22844, #51062 ) ;
#44063=ORIENTED_EDGE ( 'NONE', *, *, #10123, .T. ) ;
#44064=CARTESIAN_POINT ( 'NONE',  ( 15.50000000000129852, -15.50000000000000000, -22.50000000000000000 ) ) ;
#44065=VERTEX_POINT ( 'NONE', #42386 ) ;
#44069=ORIENTED_EDGE ( 'NONE', *, *, #21117, .F. ) ;
#44070=DIRECTION ( 'NONE',  ( 0.000000000000000000, 0.000000000000000000, -1.000000000000000000 ) ) ;
#44074=CIRCLE ( 'NONE', #11317, 4.000000000000000888 ) ;
#44085=ORIENTED_EDGE ( 'NONE', *, *, #48658, .T. ) ;
#44087=CIRCLE ( 'NONE', #3466, 1.620999999999997332 ) ;
#44093=DIRECTION ( 'NONE',  ( -1.000000000000000000, 0.000000000000000000, 0.000000000000000000 ) ) ;
#44098=CARTESIAN_POINT ( 'NONE',  ( 28.00000000000000000, -17.50000000000000000, -15.70500000000000007 ) ) ;
#44100=EDGE_CURVE ( 'NONE', #23076, #67807, #33848, .T. ) ;
#44110=DIRECTION ( 'NONE',  ( 0.000000000000000000, 1.000000000000000000, 0.000000000000000000 ) ) ;
#44120=CARTESIAN_POINT ( 'NONE',  ( 15.50000000000000000, 998.9628421096749662, -22.50000000000000000 ) ) ;
#44128=DIRECTION ( 'NONE',  ( 0.000000000000000000, 0.000000000000000000, 1.000000000000000000 ) ) ;
#44141=ADVANCED_FACE ( 'NONE', ( #28542 ), #50116, .F. ) ;
#44147=EDGE_CURVE ( 'NONE', #4772, #12650, #55875, .T. ) ;
#44149=EDGE_CURVE ( 'NONE', #42714, #67332, #49774, .T. ) ;
#44160=DIRECTION ( 'NONE',  ( 1.000000000000000000, -0.000000000000000000, -0.000000000000000000 ) ) ;
#44163=DIRECTION ( 'NONE',  ( 1.000000000000000000, -0.000000000000000000, -0.000000000000000000 ) ) ;
#44167=DIRECTION ( 'NONE',  ( 1.000000000000000000, -0.000000000000000000, -0.000000000000000000 ) ) ;
#44169=VERTEX_POINT ( 'NONE', #41247 ) ;
#44174=CARTESIAN_POINT ( 'NONE',  ( -16.75000000000000000, -2.500000000000000000, -23.22168783648699986 ) ) ;
#44193=CLOSED_SHELL ( 'NONE', ( #12372, #839, #54601, #58039, #28615, #27498, #58280, #55034, #44141, #53584, #66534, #49945, #35256, #29638, #37224, #44472, #8169, #24078, #20285, #55928, #64469, #9370, #30036, #30165, #62520, #1859, #36317, #69523, #21665, #3525, #34089, #9043, #68688, #43145, #69687, #11819, #27111, #9201, #15545, #32829, #48392, #33627, #40152, #23336, #28363, #25667, #48803, #46739, #37834, #16841, #67940, #38332, #42008, #59994, #3119, #28745, #31891, #46567, #59521, #6176, #57117, #37616, #12595, #18130, #21097, #46140, #18315, #66986, #58428, #12292, #50000, #14878, #47504, #64924, #53194, #59489, #46300, #62802, #22205, #40121, #56842, #32992, #55126, #54823, #53152, #35038, #3461, #6674, #5532, #35283, #30350, #11504, #20503, #4390, #61042, #40501, #12179, #59205, #53274, #36163, #31055, #49825, #48135, #37557, #50339, #20719, #17028, #14081, #9293, #16276, #919, #36365, #66780, #17490, #69457, #51694, #12072, #10096, #38026, #48418, #43615, #20217, #19349, #49137, #29380, #43206, #60112, #16943, #39603, #50053, #53267, #40650, #9051, #20501, #2464, #892, #21162, #68832, #39813, #40410, #52343, #60685, #33766, #15999, #18375, #20698, #25061, #1247, #12847, #25067, #59601, #34687, #5448, #8339, #26761, #27501, #12344, #13320, #20303, #52889, #359, #20646, #60239, #47189, #68838, #13325, #40358, #14707, #47369, #46717, #2980, #23437, #60512, #31823, #21038, #67374, #32307, #60069, #12171, #38540, #9109, #47985, #59196, #36969, #18928, #68117, #60040, #44616, #50384, #46432, #37115, #26236, #49447, #15813, #11864, #68826, #19216, #1135, #15635, #21571, #40881, #52852, #1069, #15023, #21899, #20706, #39644, #59481, #48873, #49481, #25973, #53537, #37642, #34437, #16732, #60149, #36420, #35420, #12154, #19, #3935, #25010, #1032, #34950, #48268, #17249, #48839, #52476, #13451, #37979, #47722, #68075, #12075, #31546, #8707, #67421, #8708, #47448, #55580, #27340, #36452, #4349, #27190, #21130, #40489, #24467, #67601, #8284, #54394, #64853, #1227, #15191, #54886, #49213, #50739, #34377, #58942, #6027, #45250, #10579, #62555, #66275, #31582, #31202, #48794, #775, #3530, #63693, #44706, #39475, #43759, #7988, #2631, #5038, #40621, #43686, #25854, #42301, #44577, #12588, #65409, #31957, #14238, #12856, #57758, #16877, #2246, #68769, #13735, #31203, #14569, #9306, #26226, #48738, #68684, #39688, #34110, #51359, #41931, #35971, #50340, #59643, #51222, #7556, #31598, #38357, #8471, #21382, #18859, #65961, #45103, #17813, #2996, #5521, #28654, #8839, #5196, #54462, #43768, #47080, #31061, #4020, #48887, #35428, #57695, #22700, #49430, #43192, #50399, #822, #66881, #68918, #43580, #39048, #507, #2414, #16503, #5953, #24460, #41859, #48574, #69889, #61238, #47247, #40552, #7902, #41750, #54873, #64194, #32028, #43271, #33240, #51130, #24812, #23676, #3604, #15096, #6088, #58203, #19278, #54887, #8025, #64866, #10725, #13131, #49238, #34240, #15971, #40672, #11132, #5628, #7264, #18949, #24616, #38918, #24270, #68704, #65238, #65285, #32908, #10717, #9859, #45896, #21575, #45890, #11952, #66188, #51375, #33069, #31001, #19928, #55664, #4119, #12200, #3041, #40077 ) ) ;
#44194=DIRECTION ( 'NONE',  ( 1.000000000000000000, 0.000000000000000000, 0.000000000000000000 ) ) ;
#44198=CIRCLE ( 'NONE', #43051, 3.299999999999473577 ) ;
#44202=ORIENTED_EDGE ( 'NONE', *, *, #33074, .F. ) ;
#44216=EDGE_LOOP ( 'NONE', ( #57491, #21, #18113, #21474 ) ) ;
#44217=CIRCLE ( 'NONE', #23926, 4.500000000000191847 ) ;
#44220=VERTEX_POINT ( 'NONE', #14395 ) ;
#44230=DIRECTION ( 'NONE',  ( -1.000000000000000000, 0.000000000000000000, 0.000000000000000000 ) ) ;
#44232=VERTEX_POINT ( 'NONE', #8733 ) ;
#44241=CARTESIAN_POINT ( 'NONE',  ( -30.00000000000000000, -5.599999999999999645, 27.00000000000000000 ) ) ;
#44274=VECTOR ( 'NONE', #37756, 1000.000000000000000 ) ;
#44275=CARTESIAN_POINT ( 'NONE',  ( 16.54633693294649532, -0.2717122460102548986, 23.33927276307431598 ) ) ;
#44277=LINE ( 'NONE', #18436, #9037 ) ;
#44278=CIRCLE ( 'NONE', #1389, 4.000000000000000000 ) ;
#44285=LINE ( 'NONE', #28376, #31410 ) ;
#44290=AXIS2_PLACEMENT_3D ( 'NONE', #55987, #67996, #24858 ) ;
#44297=DIRECTION ( 'NONE',  ( 1.000000000000000000, 0.000000000000000000, 0.000000000000000000 ) ) ;
#44300=CIRCLE ( 'NONE', #48828, 0.3500000000002719824 ) ;
#44301=DIRECTION ( 'NONE',  ( 0.000000000000000000, 0.000000000000000000, 1.000000000000000000 ) ) ;
#44304=DIRECTION ( 'NONE',  ( 0.000000000000000000, 0.000000000000000000, -1.000000000000000000 ) ) ;
#44320=EDGE_CURVE ( 'NONE', #48682, #14923, #47962, .T. ) ;
#44330=DIRECTION ( 'NONE',  ( 0.000000000000000000, 0.000000000000000000, -1.000000000000000000 ) ) ;
#44335=EDGE_LOOP ( 'NONE', ( #42513, #33522, #22358, #40365 ) ) ;
#44340=CARTESIAN_POINT ( 'NONE',  ( 11.00000000000000000, -5.599999999999379696, -26.60000000000059828 ) ) ;
#44355=CARTESIAN_POINT ( 'NONE',  ( -11.50000000000000000, -12.00000000000000000, -11.03137303340310282 ) ) ;
#44356=CONICAL_SURFACE ( 'NONE', #19537, 2.000000000000001776, 0.7853981633974503884 ) ;
#44359=CARTESIAN_POINT ( 'NONE',  ( 30.00000000000000000, -16.28999999999710369, 15.00000000000794920 ) ) ;
#44371=VERTEX_POINT ( 'NONE', #16130 ) ;
#44374=AXIS2_PLACEMENT_3D ( 'NONE', #37492, #32182, #26889 ) ;
#44387=EDGE_CURVE ( 'NONE', #34666, #19227, #16829, .T. ) ;
#44388=CARTESIAN_POINT ( 'NONE',  ( -29.25000000000000000, -5.000000000000000000, 11.75000000000000000 ) ) ;
#44394=VERTEX_POINT ( 'NONE', #43703 ) ;
#44396=VECTOR ( 'NONE', #17227, 1000.000000000000000 ) ;
#44398=VECTOR ( 'NONE', #12961, 1000.000000000000000 ) ;
#44399=ORIENTED_EDGE ( 'NONE', *, *, #13805, .T. ) ;
#44415=CARTESIAN_POINT ( 'NONE',  ( -11.00000000000000000, -16.28999999999999915, 14.50000000000000000 ) ) ;
#44417=FACE_OUTER_BOUND ( 'NONE', #68317, .T. ) ;
#44421=ORIENTED_EDGE ( 'NONE', *, *, #17948, .T. ) ;
#44429=PLANE ( 'NONE',  #28153 ) ;
#44434=CARTESIAN_POINT ( 'NONE',  ( 28.00000000000000000, -15.50000000000000000, 14.50000000000000000 ) ) ;
#44435=CARTESIAN_POINT ( 'NONE',  ( 15.50000000000000000, -5.000000000000000000, 22.50000000000000000 ) ) ;
#44449=CARTESIAN_POINT ( 'NONE',  ( -25.50000000000000355, -5.578999999999999737, 24.12099999999999866 ) ) ;
#44470=CARTESIAN_POINT ( 'NONE',  ( 30.00000000000000000, -12.00000000000000000, -12.20000000000000107 ) ) ;
#44471=DIRECTION ( 'NONE',  ( 1.000000000000000000, 0.000000000000000000, 0.000000000000000000 ) ) ;
#44472=ADVANCED_FACE ( 'NONE', ( #38730 ), #62688, .F. ) ;
#44473=CARTESIAN_POINT ( 'NONE',  ( 11.50000000000000000, -11.50000000000000000, 15.00000000000000000 ) ) ;
#44477=ORIENTED_EDGE ( 'NONE', *, *, #23874, .F. ) ;
#44478=CYLINDRICAL_SURFACE ( 'NONE', #60743, 3.499999999999999556 ) ;
#44484=EDGE_CURVE ( 'NONE', #38571, #19166, #63094, .T. ) ;
#44506=DIRECTION ( 'NONE',  ( 1.000000000000000000, 0.000000000000000000, 0.000000000000000000 ) ) ;
#44512=ORIENTED_EDGE ( 'NONE', *, *, #46913, .F. ) ;
#44514=CYLINDRICAL_SURFACE ( 'NONE', #43672, 3.499999999999055866 ) ;
#44515=CARTESIAN_POINT ( 'NONE',  ( -11.00000000000000000, -11.70000000000000284, 12.50000000000000000 ) ) ;
#44520=AXIS2_PLACEMENT_3D ( 'NONE', #15904, #47726, #68949 ) ;
#44525=EDGE_CURVE ( 'NONE', #46957, #39153, #62377, .T. ) ;
#44531=DIRECTION ( 'NONE',  ( 1.000000000000000000, -0.000000000000000000, -0.000000000000000000 ) ) ;
#44533=EDGE_CURVE ( 'NONE', #41138, #64942, #46886, .T. ) ;
#44537=CARTESIAN_POINT ( 'NONE',  ( -17.51999999999999957, -15.50000000000000000, 26.00000000000000355 ) ) ;
#44543=DIRECTION ( 'NONE',  ( -0.9583148474998870459, 0.000000000000000000, 0.2857142857143623593 ) ) ;
#44545=VECTOR ( 'NONE', #67305, 1000.000000000000000 ) ;
#44549=VERTEX_POINT ( 'NONE', #62028 ) ;
#44551=CARTESIAN_POINT ( 'NONE',  ( 18.85410196625000268, -15.50000000000000000, 21.50000000000000000 ) ) ;
#44559=DIRECTION ( 'NONE',  ( 0.000000000000000000, 0.7057491738665943037, -0.7084617869628675457 ) ) ;
#44569=CARTESIAN_POINT ( 'NONE',  ( 17.24945551514599984, -15.50000000000000000, 25.53140320652400064 ) ) ;
#44573=CARTESIAN_POINT ( 'NONE',  ( 30.00000000000000000, -10.85999999999999943, 9.350000000000269651 ) ) ;
#44577=ADVANCED_FACE ( 'NONE', ( #40471 ), #34805, .T. ) ;
#44578=FACE_OUTER_BOUND ( 'NONE', #46805, .T. ) ;
#44584=VERTEX_POINT ( 'NONE', #19254 ) ;
#44587=VECTOR ( 'NONE', #45947, 1000.000000000000000 ) ;
#44589=CIRCLE ( 'NONE', #35725, 4.500000000000191847 ) ;
#44596=CARTESIAN_POINT ( 'NONE',  ( 16.33565937784172917, -0.3156604612126716614, -21.53909249377372959 ) ) ;
#44601=EDGE_LOOP ( 'NONE', ( #53775, #63320, #35234, #19453 ) ) ;
#44612=DIRECTION ( 'NONE',  ( 0.000000000000000000, 0.000000000000000000, 1.000000000000000000 ) ) ;
#44613=EDGE_CURVE ( 'NONE', #18754, #63213, #52135, .T. ) ;
#44615=DIRECTION ( 'NONE',  ( -1.000000000000000000, 0.000000000000000000, 0.000000000000000000 ) ) ;
#44616=ADVANCED_FACE ( 'NONE', ( #62734 ), #25265, .F. ) ;
#44619=CARTESIAN_POINT ( 'NONE',  ( 29.50000000000000355, -15.46862696659690073, -14.50000000000000000 ) ) ;
#44620=LINE ( 'NONE', #66207, #11855 ) ;
#44628=VERTEX_POINT ( 'NONE', #25976 ) ;
#44631=DIRECTION ( 'NONE',  ( 0.000000000000000000, 0.000000000000000000, 1.000000000000000000 ) ) ;
#44636=PLANE ( 'NONE',  #15003 ) ;
#44639=DIRECTION ( 'NONE',  ( 1.000000000000000000, -0.000000000000000000, -0.000000000000000000 ) ) ;
#44645=VECTOR ( 'NONE', #7537, 1000.000000000000000 ) ;
#44652=EDGE_LOOP ( 'NONE', ( #13773, #53001, #43448, #5717, #51713, #62397, #64460, #24861 ) ) ;
#44657=LINE ( 'NONE', #56329, #24003 ) ;
#44662=PLANE ( 'NONE',  #33365 ) ;
#44668=CARTESIAN_POINT ( 'NONE',  ( 11.50000000000000000, -15.46862696659690073, -14.50000000000000000 ) ) ;
#44673=ORIENTED_EDGE ( 'NONE', *, *, #42126, .F. ) ;
#44674=AXIS2_PLACEMENT_3D ( 'NONE', #12870, #40095, #34436 ) ;
#44675=ORIENTED_EDGE ( 'NONE', *, *, #45537, .T. ) ;
#44676=CARTESIAN_POINT ( 'NONE',  ( -28.00000000000000000, -16.64230188589299786, -14.64519951917100116 ) ) ;
#44689=CARTESIAN_POINT ( 'NONE',  ( 28.00000000000000000, -15.50000000000000000, -14.49999999999999645 ) ) ;
#44698=LINE ( 'NONE', #55672, #2219 ) ;
#44706=ADVANCED_FACE ( 'NONE', ( #10404 ), #54241, .F. ) ;
#44719=ORIENTED_EDGE ( 'NONE', *, *, #2425, .F. ) ;
#44725=DIRECTION ( 'NONE',  ( 0.000000000000000000, -0.7096009616570518874, 0.7046037717862339012 ) ) ;
#44745=VECTOR ( 'NONE', #29651, 1000.000000000000000 ) ;
#44747=ORIENTED_EDGE ( 'NONE', *, *, #47720, .F. ) ;
#44748=ORIENTED_EDGE ( 'NONE', *, *, #36692, .F. ) ;
#44756=ORIENTED_EDGE ( 'NONE', *, *, #1630, .T. ) ;
#44757=DIRECTION ( 'NONE',  ( -0.4998444328988824181, 0.000000000000000000, 0.8661152018640445593 ) ) ;
#44765=DIRECTION ( 'NONE',  ( 0.000000000000000000, -5.800915303574361727E-12, 1.000000000000000000 ) ) ;
#44772=AXIS2_PLACEMENT_3D ( 'NONE', #50454, #29924, #18258 ) ;
#44777=CARTESIAN_POINT ( 'NONE',  ( -25.50000000000000355, -5.578999999999999737, 20.87899999999999778 ) ) ;
#44781=CARTESIAN_POINT ( 'NONE',  ( 14.25000000000000178, -0.2714405302574884327, 22.98746066354537732 ) ) ;
#44783=DIRECTION ( 'NONE',  ( 0.000000000000000000, 1.000000000000000000, 0.000000000000000000 ) ) ;
#44800=ORIENTED_EDGE ( 'NONE', *, *, #3055, .F. ) ;
#44801=DIRECTION ( 'NONE',  ( -1.000000000000000000, 0.000000000000000000, 0.000000000000000000 ) ) ;
#44806=PRODUCT ( 'SAWC-0630-60S_wagen', 'SAWC-0630-60S_wagen', '', ( #3825 ) ) ;
#44809=CARTESIAN_POINT ( 'NONE',  ( -15.50000000000000000, -5.000000000000000000, 22.50000000000000000 ) ) ;
#44823=FACE_OUTER_BOUND ( 'NONE', #40936, .T. ) ;
#44825=STYLED_ITEM ( 'NONE', ( #40106 ), #20823 ) ;
#44834=EDGE_LOOP ( 'NONE', ( #21006, #17058, #37561, #42448 ) ) ;
#44849=DIRECTION ( 'NONE',  ( 1.000000000000000000, 0.000000000000000000, 0.000000000000000000 ) ) ;
#44860=DIRECTION ( 'NONE',  ( 0.000000000000000000, 0.000000000000000000, -1.000000000000000000 ) ) ;
#44870=EDGE_CURVE ( 'NONE', #42714, #20373, #20486, .T. ) ;
#44887=DIRECTION ( 'NONE',  ( 0.000000000000000000, 0.000000000000000000, 1.000000000000000000 ) ) ;
#44888=DIRECTION ( 'NONE',  ( 0.000000000000000000, 1.000000000000000000, 0.000000000000000000 ) ) ;
#44889=CARTESIAN_POINT ( 'NONE',  ( 29.50000000000000355, -11.50000000000000000, 15.00000000000000000 ) ) ;
#44897=PLANE ( 'NONE',  #68841 ) ;
#44906=CARTESIAN_POINT ( 'NONE',  ( -11.00000000000000000, -9.199999999999999289, -12.69999999999986073 ) ) ;
#44913=ORIENTED_EDGE ( 'NONE', *, *, #13001, .T. ) ;
#44920=ORIENTED_EDGE ( 'NONE', *, *, #11910, .T. ) ;
#44925=EDGE_CURVE ( 'NONE', #1191, #24869, #14186, .T. ) ;
#44928=ORIENTED_EDGE ( 'NONE', *, *, #62161, .F. ) ;
#44930=FACE_OUTER_BOUND ( 'NONE', #20545, .T. ) ;
#44936=CIRCLE ( 'NONE', #50596, 4.500000000000190958 ) ;
#44946=ORIENTED_EDGE ( 'NONE', *, *, #59084, .F. ) ;
#44957=DIRECTION ( 'NONE',  ( 0.000000000000000000, 0.000000000000000000, 1.000000000000000000 ) ) ;
#44968=ORIENTED_EDGE ( 'NONE', *, *, #57423, .F. ) ;
#44975=FACE_OUTER_BOUND ( 'NONE', #6914, .T. ) ;
#44976=EDGE_CURVE ( 'NONE', #50067, #39463, #48061, .T. ) ;
#44977=ORIENTED_EDGE ( 'NONE', *, *, #42956, .T. ) ;
#44984=CARTESIAN_POINT ( 'NONE',  ( 11.00000000000000000, -11.50000000000100009, -15.00000000000084910 ) ) ;
#44985=CARTESIAN_POINT ( 'NONE',  ( 11.00000000000000000, -15.46862696659690073, 14.50000000000000000 ) ) ;
#44989=CARTESIAN_POINT ( 'NONE',  ( 25.50000000000000355, -5.578999999999999737, 22.50000000000000000 ) ) ;
#44999=DIRECTION ( 'NONE',  ( 0.000000000000000000, 0.000000000000000000, 1.000000000000000000 ) ) ;
#45003=DIRECTION ( 'NONE',  ( 0.000000000000000000, 1.000000000000000000, 0.000000000000000000 ) ) ;
#45007=AXIS2_PLACEMENT_3D ( 'NONE', #24483, #53371, #62643 ) ;
#45010=LINE ( 'NONE', #62321, #33878 ) ;
#45012=CARTESIAN_POINT ( 'NONE',  ( -11.00000000000000000, -5.599999999999999645, 9.000000000000001776 ) ) ;
#45019=EDGE_CURVE ( 'NONE', #10292, #69139, #54072, .T. ) ;
#45021=LINE ( 'NONE', #39715, #37871 ) ;
#45029=ORIENTED_EDGE ( 'NONE', *, *, #40522, .T. ) ;
#45031=FACE_OUTER_BOUND ( 'NONE', #6367, .T. ) ;
#45032=ORIENTED_EDGE ( 'NONE', *, *, #59154, .F. ) ;
#45035=AXIS2_PLACEMENT_3D ( 'NONE', #22441, #21394, #48967 ) ;
#45038=DIRECTION ( 'NONE',  ( 0.000000000000000000, 1.000000000000000000, 1.500535806722250850E-12 ) ) ;
#45039=ORIENTED_EDGE ( 'NONE', *, *, #11008, .T. ) ;
#45045=ORIENTED_EDGE ( 'NONE', *, *, #39226, .F. ) ;
#45046=ORIENTED_EDGE ( 'NONE', *, *, #11263, .T. ) ;
#45051=DIRECTION ( 'NONE',  ( 0.8660254037844482555, 0.000000000000000000, -0.4999999999999831801 ) ) ;
#45055=VECTOR ( 'NONE', #21499, 1000.000000000000000 ) ;
#45066=EDGE_CURVE ( 'NONE', #30786, #9070, #28554, .T. ) ;
#45068=DIRECTION ( 'NONE',  ( 0.000000000000000000, 0.000000000000000000, 1.000000000000000000 ) ) ;
#45081=FACE_OUTER_BOUND ( 'NONE', #15125, .T. ) ;
#45085=ORIENTED_EDGE ( 'NONE', *, *, #33948, .T. ) ;
#45094=AXIS2_PLACEMENT_3D ( 'NONE', #29319, #35675, #67865 ) ;
#45099=ORIENTED_EDGE ( 'NONE', *, *, #56919, .T. ) ;
#45101=DIRECTION ( 'NONE',  ( -1.000000000000000000, 0.000000000000000000, 0.000000000000000000 ) ) ;
#45103=ADVANCED_FACE ( 'NONE', ( #66731, #61786 ), #66396, .F. ) ;
#45107=CARTESIAN_POINT ( 'NONE',  ( -15.50000000000000000, -5.000000000000000000, 22.50000000000000000 ) ) ;
#45121=AXIS2_PLACEMENT_3D ( 'NONE', #69145, #5843, #43314 ) ;
#45125=CARTESIAN_POINT ( 'NONE',  ( 14.25000000000000000, -2.500000000000000000, -23.22168783648699986 ) ) ;
#45126=DIRECTION ( 'NONE',  ( 0.000000000000000000, 0.000000000000000000, -1.000000000000000000 ) ) ;
#45129=VECTOR ( 'NONE', #11258, 1000.000000000000000 ) ;
#45132=DIRECTION ( 'NONE',  ( 0.000000000000000000, -1.000000000000000000, 0.000000000000000000 ) ) ;
#45133=ORIENTED_EDGE ( 'NONE', *, *, #23994, .F. ) ;
#45142=EDGE_CURVE ( 'NONE', #41898, #37433, #34894, .T. ) ;
#45143=VECTOR ( 'NONE', #38248, 999.9999999999998863 ) ;
#45152=DIRECTION ( 'NONE',  ( 0.000000000000000000, -1.000000000000000000, 0.000000000000000000 ) ) ;
#45156=CYLINDRICAL_SURFACE ( 'NONE', #1590, 0.2999999999998732569 ) ;
#45157=DIRECTION ( 'NONE',  ( 0.000000000000000000, -1.000000000000000000, 0.000000000000000000 ) ) ;
#45161=DIRECTION ( 'NONE',  ( 0.000000000000000000, 1.000000000000000000, 0.000000000000000000 ) ) ;
#45176=VECTOR ( 'NONE', #52372, 1000.000000000000000 ) ;
#45183=DIRECTION ( 'NONE',  ( -1.000000000000000000, 0.000000000000000000, 0.000000000000000000 ) ) ;
#45195=ORIENTED_EDGE ( 'NONE', *, *, #16790, .F. ) ;
#45206=ORIENTED_EDGE ( 'NONE', *, *, #32565, .T. ) ;
#45210=DIRECTION ( 'NONE',  ( 1.000000000000000000, -0.000000000000000000, -0.000000000000000000 ) ) ;
#45217=CARTESIAN_POINT ( 'NONE',  ( 11.50000000000000000, -12.00000000000000000, 11.00000000000000000 ) ) ;
#45230=CARTESIAN_POINT ( 'NONE',  ( -15.50000000000000000, -5.000000000000000000, -22.50000000000000000 ) ) ;
#45236=AXIS2_PLACEMENT_3D ( 'NONE', #47763, #69331, #15249 ) ;
#45237=DIRECTION ( 'NONE',  ( -0.000000000000000000, 1.000000000000000000, -0.000000000000000000 ) ) ;
#45250=ADVANCED_FACE ( 'NONE', ( #25723 ), #62837, .F. ) ;
#45253=FACE_OUTER_BOUND ( 'NONE', #23135, .T. ) ;
#45262=DIRECTION ( 'NONE',  ( 0.000000000000000000, 1.000000000000000000, 0.000000000000000000 ) ) ;
#45267=CYLINDRICAL_SURFACE ( 'NONE', #40824, 0.3500000000002719824 ) ;
#45269=PLANE ( 'NONE',  #30369 ) ;
#45273=FACE_OUTER_BOUND ( 'NONE', #44335, .T. ) ;
#45279=ORIENTED_EDGE ( 'NONE', *, *, #3754, .T. ) ;
#45282=DIRECTION ( 'NONE',  ( -1.000000000000000000, 0.000000000000000000, 0.000000000000000000 ) ) ;
#45284=EDGE_CURVE ( 'NONE', #37597, #52878, #43623, .T. ) ;
#45286=VECTOR ( 'NONE', #59850, 1000.000000000000000 ) ;
#45296=ORIENTED_EDGE ( 'NONE', *, *, #17340, .T. ) ;
#45297=DIRECTION ( 'NONE',  ( 0.000000000000000000, 0.000000000000000000, -1.000000000000000000 ) ) ;
#45304=VERTEX_POINT ( 'NONE', #68140 ) ;
#45307=LINE ( 'NONE', #34006, #25599 ) ;
#45314=ORIENTED_EDGE ( 'NONE', *, *, #2316, .F. ) ;
#45320=PLANE ( 'NONE',  #31243 ) ;
#45322=FACE_OUTER_BOUND ( 'NONE', #5397, .T. ) ;
#45337=EDGE_CURVE ( 'NONE', #62137, #39966, #19894, .T. ) ;
#45349=CARTESIAN_POINT ( 'NONE',  ( 15.50000000000000000, 0.000000000000000000, 18.50000000000000000 ) ) ;
#45350=ORIENTED_EDGE ( 'NONE', *, *, #18112, .F. ) ;
#45351=ORIENTED_EDGE ( 'NONE', *, *, #12508, .T. ) ;
#45372=EDGE_CURVE ( 'NONE', #18037, #25620, #7464, .T. ) ;
#45377=ORIENTED_EDGE ( 'NONE', *, *, #68175, .F. ) ;
#45382=VERTEX_POINT ( 'NONE', #66285 ) ;
#45388=DIRECTION ( 'NONE',  ( -1.000000000000000000, 0.000000000000000000, 0.000000000000000000 ) ) ;
#45393=DIRECTION ( 'NONE',  ( 0.000000000000000000, 0.7278708115913771204, 0.6857142857147648929 ) ) ;
#45394=VERTEX_POINT ( 'NONE', #23494 ) ;
#45397=CIRCLE ( 'NONE', #42035, 2.000000000000001776 ) ;
#45401=VECTOR ( 'NONE', #12302, 1000.000000000000000 ) ;
#45412=DIRECTION ( 'NONE',  ( 0.000000000000000000, 1.000000000000000000, 0.000000000000000000 ) ) ;
#45423=CARTESIAN_POINT ( 'NONE',  ( 17.24945551514599984, -15.50000000000000000, -25.53140320652400064 ) ) ;
#45445=ORIENTED_EDGE ( 'NONE', *, *, #18138, .F. ) ;
#45446=VERTEX_POINT ( 'NONE', #8261 ) ;
#45454=ORIENTED_EDGE ( 'NONE', *, *, #48478, .F. ) ;
#45459=CARTESIAN_POINT ( 'NONE',  ( 30.00000000000000000, -8.959999999999999076, -12.95475478405700009 ) ) ;
#45462=ORIENTED_EDGE ( 'NONE', *, *, #29118, .F. ) ;
#45464=LINE ( 'NONE', #44415, #57609 ) ;
#45466=CARTESIAN_POINT ( 'NONE',  ( -24.00000000000000000, -16.28999999999710369, -15.00000000000794920 ) ) ;
#45468=LINE ( 'NONE', #41217, #11894 ) ;
#45477=CARTESIAN_POINT ( 'NONE',  ( 15.50000000000000000, -0.4000000000005274892, 22.50000000000000000 ) ) ;
#45481=PLANE ( 'NONE',  #52361 ) ;
#45482=EDGE_LOOP ( 'NONE', ( #4265, #16253 ) ) ;
#45489=EDGE_CURVE ( 'NONE', #54344, #69663, #3324, .T. ) ;
#45492=EDGE_CURVE ( 'NONE', #2465, #24086, #31607, .T. ) ;
#45496=FACE_OUTER_BOUND ( 'NONE', #15093, .T. ) ;
#45497=DIRECTION ( 'NONE',  ( 1.000000000000000000, -0.000000000000000000, -0.000000000000000000 ) ) ;
#45501=FACE_OUTER_BOUND ( 'NONE', #38284, .T. ) ;
#45515=CARTESIAN_POINT ( 'NONE',  ( -29.50000000000000355, -11.50000000000100009, -10.50000000000065903 ) ) ;
#45535=ORIENTED_EDGE ( 'NONE', *, *, #16758, .T. ) ;
#45537=EDGE_CURVE ( 'NONE', #11471, #20459, #26770, .T. ) ;
#45540=CARTESIAN_POINT ( 'NONE',  ( -30.00000000000000000, -17.50000000000000000, -15.70500000000000007 ) ) ;
#45556=CIRCLE ( 'NONE', #53475, 0.4000000000000600298 ) ;
#45560=ORIENTED_EDGE ( 'NONE', *, *, #30495, .T. ) ;
#45563=CIRCLE ( 'NONE', #62524, 4.500000000000191847 ) ;
#45577=LINE ( 'NONE', #23332, #33065 ) ;
#45588=EDGE_CURVE ( 'NONE', #42164, #57112, #47168, .T. ) ;
#45591=VERTEX_POINT ( 'NONE', #41845 ) ;
#45597=EDGE_CURVE ( 'NONE', #13055, #17772, #24489, .T. ) ;
#45601=VECTOR ( 'NONE', #21875, 1000.000000000000000 ) ;
#45602=AXIS2_PLACEMENT_3D ( 'NONE', #61273, #67304, #51381 ) ;
#45613=ORIENTED_EDGE ( 'NONE', *, *, #9513, .T. ) ;
#45614=ORIENTED_EDGE ( 'NONE', *, *, #32527, .F. ) ;
#45617=DIRECTION ( 'NONE',  ( 0.000000000000000000, -0.7071067811865455743, 0.7071067811865495711 ) ) ;
#45624=LINE ( 'NONE', #12742, #27627 ) ;
#45628=VERTEX_POINT ( 'NONE', #52036 ) ;
#45629=EDGE_LOOP ( 'NONE', ( #22692, #27291, #62117, #31031, #10721, #54571, #35022 ) ) ;
#45638=PLANE ( 'NONE',  #3792 ) ;
#45661=EDGE_CURVE ( 'NONE', #8473, #46156, #40718, .T. ) ;
#45666=ORIENTED_EDGE ( 'NONE', *, *, #14921, .T. ) ;
#45680=ORIENTED_EDGE ( 'NONE', *, *, #17497, .F. ) ;
#45681=CARTESIAN_POINT ( 'NONE',  ( 30.00000000000000000, -17.50000000000000000, 26.64999999999999858 ) ) ;
#45694=DIRECTION ( 'NONE',  ( 0.000000000000000000, -1.000000000000000000, 0.000000000000000000 ) ) ;
#45697=FACE_OUTER_BOUND ( 'NONE', #39036, .T. ) ;
#45698=ORIENTED_EDGE ( 'NONE', *, *, #23298, .F. ) ;
#45700=CARTESIAN_POINT ( 'NONE',  ( -11.00000000000000000, -10.85999999999999943, 9.000000000000001776 ) ) ;
#45720=SHAPE_REPRESENTATION_RELATIONSHIP ( 'NONE' , 'NONE' ,  #26379, #63000 ) ;
#45724=ORIENTED_EDGE ( 'NONE', *, *, #28455, .F. ) ;
#45725=EDGE_CURVE ( 'NONE', #49372, #64729, #35399, .T. ) ;
#45736=VERTEX_POINT ( 'NONE', #56632 ) ;
#45759=VECTOR ( 'NONE', #21485, 1000.000000000000000 ) ;
#45777=ORIENTED_EDGE ( 'NONE', *, *, #5304, .T. ) ;
#45779=LINE ( 'NONE', #6902, #27541 ) ;
#45783=DIRECTION ( 'NONE',  ( 0.000000000000000000, 0.000000000000000000, -1.000000000000000000 ) ) ;
#45785=LINE ( 'NONE', #67001, #28746 ) ;
#45788=CARTESIAN_POINT ( 'NONE',  ( 15.50000000000000000, -2.500000000000000000, -23.94337567297399971 ) ) ;
#45789=FACE_OUTER_BOUND ( 'NONE', #43238, .T. ) ;
#45800=ORIENTED_EDGE ( 'NONE', *, *, #5921, .F. ) ;
#45803=ORIENTED_EDGE ( 'NONE', *, *, #53145, .F. ) ;
#45804=ORIENTED_EDGE ( 'NONE', *, *, #30918, .F. ) ;
#45811=AXIS2_PLACEMENT_3D ( 'NONE', #8365, #24294, #41248 ) ;
#45831=LINE ( 'NONE', #56093, #12562 ) ;
#45836=LINE ( 'NONE', #61748, #29249 ) ;
#45852=CARTESIAN_POINT ( 'NONE',  ( 30.00000000000000000, -16.28999999999710369, -15.00000000000794920 ) ) ;
#45853=EDGE_CURVE ( 'NONE', #45736, #19628, #15953, .T. ) ;
#45855=CARTESIAN_POINT ( 'NONE',  ( 15.50000000000000000, -0.1999999999999999556, 22.50000000000000000 ) ) ;
#45870=DIRECTION ( 'NONE',  ( 0.000000000000000000, 1.000000000000000000, 0.000000000000000000 ) ) ;
#45874=DIRECTION ( 'NONE',  ( 0.000000000000000000, 0.000000000000000000, 1.000000000000000000 ) ) ;
#45875=ORIENTED_EDGE ( 'NONE', *, *, #63115, .T. ) ;
#45887=DIRECTION ( 'NONE',  ( -1.000000000000000000, 0.000000000000000000, 0.000000000000000000 ) ) ;
#45888=ORIENTED_EDGE ( 'NONE', *, *, #8670, .F. ) ;
#45889=VERTEX_POINT ( 'NONE', #64735 ) ;
#45890=ADVANCED_FACE ( 'NONE', ( #60457 ), #386, .F. ) ;
#45892=CARTESIAN_POINT ( 'NONE',  ( -30.00000000000000000, -11.50000000000000000, -11.00000000000000000 ) ) ;
#45893=CARTESIAN_POINT ( 'NONE',  ( 17.00000000000000000, -17.35230188589299871, 15.35019951917099945 ) ) ;
#45894=VECTOR ( 'NONE', #29077, 1000.000000000000000 ) ;
#45896=ADVANCED_FACE ( 'NONE', ( #6038 ), #27596, .F. ) ;
#45898=DIRECTION ( 'NONE',  ( -1.000000000000000000, 0.000000000000000000, 0.000000000000000000 ) ) ;
#45899=DIRECTION ( 'NONE',  ( 1.000000000000000000, 0.000000000000000000, 0.000000000000000000 ) ) ;
#45901=DIRECTION ( 'NONE',  ( -1.000000000000000000, 0.000000000000000000, 0.000000000000000000 ) ) ;
#45904=EDGE_CURVE ( 'NONE', #32467, #59441, #21943, .T. ) ;
#45910=EDGE_CURVE ( 'NONE', #48042, #24514, #8688, .T. ) ;
#45917=DIRECTION ( 'NONE',  ( 0.000000000000000000, -1.000000000000000000, 0.000000000000000000 ) ) ;
#45918=AXIS2_PLACEMENT_3D ( 'NONE', #22775, #53934, #32355 ) ;
#45920=VERTEX_POINT ( 'NONE', #65091 ) ;
#45922=CIRCLE ( 'NONE', #15456, 3.499999999999849454 ) ;
#45927=CARTESIAN_POINT ( 'NONE',  ( -29.25000000000000000, -5.200000000000001066, -11.75000000000000000 ) ) ;
#45936=DIRECTION ( 'NONE',  ( -1.000000000000000000, 0.000000000000000000, 0.000000000000000000 ) ) ;
#45940=LINE ( 'NONE', #29665, #51646 ) ;
#45941=PLANE ( 'NONE',  #20394 ) ;
#45943=ORIENTED_EDGE ( 'NONE', *, *, #16480, .F. ) ;
#45947=DIRECTION ( 'NONE',  ( 0.000000000000000000, -1.000000000000000000, 0.000000000000000000 ) ) ;
#45957=DIRECTION ( 'NONE',  ( 1.000000000000000000, -0.000000000000000000, -0.000000000000000000 ) ) ;
#45961=LINE ( 'NONE', #3187, #47035 ) ;
#45962=AXIS2_PLACEMENT_3D ( 'NONE', #28206, #12614, #17931 ) ;
#45971=PLANE ( 'NONE',  #23906 ) ;
#45973=LINE ( 'NONE', #29008, #65269 ) ;
#45974=VECTOR ( 'NONE', #62490, 1000.000000000000000 ) ;
#45982=CIRCLE ( 'NONE', #36980, 3.499999999999850342 ) ;
#45983=EDGE_CURVE ( 'NONE', #20681, #29049, #59023, .T. ) ;
#45989=DIRECTION ( 'NONE',  ( 0.000000000000000000, 0.000000000000000000, 1.000000000000000000 ) ) ;
#45990=DIRECTION ( 'NONE',  ( 0.000000000000000000, 0.000000000000000000, -1.000000000000000000 ) ) ;
#45991=DIRECTION ( 'NONE',  ( 0.000000000000000000, -0.9938079899998859545, 0.1111111111112941946 ) ) ;
#45994=ORIENTED_EDGE ( 'NONE', *, *, #46744, .T. ) ;
#45999=CARTESIAN_POINT ( 'NONE',  ( 15.50000000000000000, -2.500000000000000000, -23.94337567297399971 ) ) ;
#46003=ORIENTED_EDGE ( 'NONE', *, *, #26580, .T. ) ;
#46013=VERTEX_POINT ( 'NONE', #10993 ) ;
#46014=VECTOR ( 'NONE', #55540, 1000.000000000000000 ) ;
#46029=CARTESIAN_POINT ( 'NONE',  ( 22.14589803375000088, -17.50000000000000000, -21.50000000000000000 ) ) ;
#46030=CARTESIAN_POINT ( 'NONE',  ( 11.00000000000000000, -17.35230188589299871, -15.35019951917099945 ) ) ;
#46035=AXIS2_PLACEMENT_3D ( 'NONE', #10128, #3421, #8728 ) ;
#46039=EDGE_CURVE ( 'NONE', #54618, #62633, #45982, .T. ) ;
#46043=LINE ( 'NONE', #56649, #39242 ) ;
#46044=DIRECTION ( 'NONE',  ( -1.000000000000000000, 0.000000000000000000, 0.000000000000000000 ) ) ;
#46056=DIRECTION ( 'NONE',  ( -0.4285714285711681448, 0.000000000000000000, -0.9035079029053748600 ) ) ;
#46057=LINE ( 'NONE', #66578, #41076 ) ;
#46073=CARTESIAN_POINT ( 'NONE',  ( -11.75000000000000000, -5.000000000000000000, 26.25000000000000000 ) ) ;
#46076=ORIENTED_EDGE ( 'NONE', *, *, #10403, .T. ) ;
#46079=CARTESIAN_POINT ( 'NONE',  ( 11.00000000000000000, -17.00000000000000000, -15.70499999999969809 ) ) ;
#46080=EDGE_CURVE ( 'NONE', #2041, #62471, #24014, .T. ) ;
#46089=CARTESIAN_POINT ( 'NONE',  ( 24.00000000000000000, -16.64230188589299786, -14.64519951917100116 ) ) ;
#46111=CARTESIAN_POINT ( 'NONE',  ( 30.00000000000000000, -12.00000000000000000, 12.20000000000000107 ) ) ;
#46115=AXIS2_PLACEMENT_3D ( 'NONE', #4515, #26080, #57540 ) ;
#46117=LINE ( 'NONE', #34097, #65050 ) ;
#46118=EDGE_CURVE ( 'NONE', #14935, #15308, #40975, .T. ) ;
#46120=LINE ( 'NONE', #2995, #52823 ) ;
#46121=CYLINDRICAL_SURFACE ( 'NONE', #8006, 1.621000000000000885 ) ;
#46134=EDGE_CURVE ( 'NONE', #37432, #16302, #45940, .T. ) ;
#46138=DIRECTION ( 'NONE',  ( -0.8660254037844482555, 0.000000000000000000, 0.4999999999999831801 ) ) ;
#46140=ADVANCED_FACE ( 'NONE', ( #24725 ), #19066, .T. ) ;
#46141=DIRECTION ( 'NONE',  ( 0.000000000000000000, 0.7071067811865450192, 0.7071067811865500152 ) ) ;
#46144=VERTEX_POINT ( 'NONE', #35307 ) ;
#46150=CARTESIAN_POINT ( 'NONE',  ( -13.00000000000000178, -17.50000000000000000, -15.70500000000000007 ) ) ;
#46156=VERTEX_POINT ( 'NONE', #64309 ) ;
#46162=ORIENTED_EDGE ( 'NONE', *, *, #30479, .T. ) ;
#46164=CARTESIAN_POINT ( 'NONE',  ( 16.54686605390242349, -0.2715358723599871626, 21.66103272505201716 ) ) ;
#46166=DIRECTION ( 'NONE',  ( 1.000000000000000000, 0.000000000000000000, 0.000000000000000000 ) ) ;
#46172=EDGE_CURVE ( 'NONE', #60418, #11608, #9514, .T. ) ;
#46174=ORIENTED_EDGE ( 'NONE', *, *, #15362, .T. ) ;
#46176=AXIS2_PLACEMENT_3D ( 'NONE', #61064, #61777, #29944 ) ;
#46178=DIRECTION ( 'NONE',  ( -1.000000000000000000, 0.000000000000000000, 0.000000000000000000 ) ) ;
#46182=DIRECTION ( 'NONE',  ( -1.000000000000000000, 0.000000000000000000, 0.000000000000000000 ) ) ;
#46192=DIRECTION ( 'NONE',  ( 0.000000000000000000, 0.000000000000000000, 1.000000000000000000 ) ) ;
#46222=CARTESIAN_POINT ( 'NONE',  ( -30.00000000000000000, -11.50000000000100009, 19.50000000000103739 ) ) ;
#46223=ORIENTED_EDGE ( 'NONE', *, *, #69090, .T. ) ;
#46225=DIRECTION ( 'NONE',  ( 1.000000000000000000, 0.000000000000000000, 0.000000000000000000 ) ) ;
#46226=EDGE_CURVE ( 'NONE', #34054, #64, #21177, .T. ) ;
#46231=ORIENTED_EDGE ( 'NONE', *, *, #23330, .F. ) ;
#46233=EDGE_CURVE ( 'NONE', #12401, #36748, #20469, .T. ) ;
#46235=ORIENTED_EDGE ( 'NONE', *, *, #38870, .F. ) ;
#46241=CARTESIAN_POINT ( 'NONE',  ( -15.50000000000000000, -5.000000000000000000, 22.50000000000000000 ) ) ;
#46242=CARTESIAN_POINT ( 'NONE',  ( -11.00000000000000000, -5.200000000000001066, 60.00000000000000000 ) ) ;
#46248=LINE ( 'NONE', #35270, #46879 ) ;
#46255=EDGE_CURVE ( 'NONE', #13915, #47971, #57944, .T. ) ;
#46260=LINE ( 'NONE', #56518, #4361 ) ;
#46264=VECTOR ( 'NONE', #55518, 1000.000000000000000 ) ;
#46268=DIRECTION ( 'NONE',  ( 1.000000000000000000, -0.000000000000000000, -0.000000000000000000 ) ) ;
#46273=B_SPLINE_CURVE_WITH_KNOTS ( 'NONE', 3,
 ( #41376, #51998, #30777, #8492, #25473, #52348 ),
 .UNSPECIFIED., .F., .F.,
 ( 4, 2, 4 ),
 ( 0.0002380763768131538560, 0.7291065797294589146, 1.457975083082104550 ),
 .UNSPECIFIED. ) ;
#46278=CARTESIAN_POINT ( 'NONE',  ( 30.00000000000000000, -17.50000000000000000, -15.70500000000000007 ) ) ;
#46282=CARTESIAN_POINT ( 'NONE',  ( -24.00000000000000000, -15.50000000000000000, -19.33772233983200195 ) ) ;
#46285=FACE_OUTER_BOUND ( 'NONE', #9979, .T. ) ;
#46289=CARTESIAN_POINT ( 'NONE',  ( -15.50000000000000000, -2.500000000000000000, 23.94337567297399971 ) ) ;
#46299=CARTESIAN_POINT ( 'NONE',  ( 28.00000000000000000, -16.28999999999710369, -14.50000000000000000 ) ) ;
#46300=ADVANCED_FACE ( 'NONE', ( #60363 ), #27513, .F. ) ;
#46301=CARTESIAN_POINT ( 'NONE',  ( -23.48000000000000043, -17.50000000000000000, 26.00000000000000355 ) ) ;
#46308=LINE ( 'NONE', #39935, #44002 ) ;
#46315=VERTEX_POINT ( 'NONE', #6630 ) ;
#46316=AXIS2_PLACEMENT_3D ( 'NONE', #45852, #50469, #2030 ) ;
#46326=EDGE_LOOP ( 'NONE', ( #41557, #11099, #50824, #13991 ) ) ;
#46327=DIRECTION ( 'NONE',  ( 0.000000000000000000, -0.1249999999999996531, -0.9921567416492215186 ) ) ;
#46338=CYLINDRICAL_SURFACE ( 'NONE', #34173, 0.4000000000000617506 ) ;
#46339=ORIENTED_EDGE ( 'NONE', *, *, #24602, .F. ) ;
#46341=ORIENTED_EDGE ( 'NONE', *, *, #10395, .T. ) ;
#46348=EDGE_CURVE ( 'NONE', #35460, #35302, #1001, .T. ) ;
#46349=CARTESIAN_POINT ( 'NONE',  ( 30.00000000000000000, -5.200000000000001066, -26.59999999999999787 ) ) ;
#46351=ORIENTED_EDGE ( 'NONE', *, *, #26931, .T. ) ;
#46357=VERTEX_POINT ( 'NONE', #1333 ) ;
#46358=FACE_OUTER_BOUND ( 'NONE', #60774, .T. ) ;
#46370=CARTESIAN_POINT ( 'NONE',  ( 15.50000000000000000, 0.000000000000000000, 26.50000000000000000 ) ) ;
#46371=DIRECTION ( 'NONE',  ( 0.4999999999989361843, 0.000000000000000000, 0.8660254037850529940 ) ) ;
#46373=CARTESIAN_POINT ( 'NONE',  ( 30.00000000000000000, -17.50000000000000000, 26.64999999999999858 ) ) ;
#46376=ORIENTED_EDGE ( 'NONE', *, *, #26940, .T. ) ;
#46377=EDGE_CURVE ( 'NONE', #2319, #35777, #20000, .T. ) ;
#46378=PLANE ( 'NONE',  #22008 ) ;
#46385=DIRECTION ( 'NONE',  ( -1.000000000000000000, 0.000000000000000000, 0.000000000000000000 ) ) ;
#46392=EDGE_CURVE ( 'NONE', #34424, #57233, #1970, .T. ) ;
#46394=CIRCLE ( 'NONE', #57706, 2.000000000000001776 ) ;
#46397=VERTEX_POINT ( 'NONE', #21857 ) ;
#46400=DIRECTION ( 'NONE',  ( 0.000000000000000000, -0.1249999999999996531, -0.9921567416492215186 ) ) ;
#46404=VERTEX_POINT ( 'NONE', #22893 ) ;
#46407=ORIENTED_EDGE ( 'NONE', *, *, #5292, .T. ) ;
#46412=CARTESIAN_POINT ( 'NONE',  ( -24.00000000000000000, -15.50000000000000000, -19.33772233983200195 ) ) ;
#46416=CARTESIAN_POINT ( 'NONE',  ( 17.00000000000000000, -15.50000000000000000, 14.50000000000000000 ) ) ;
#46422=EDGE_LOOP ( 'NONE', ( #48963, #54180, #19965, #49878 ) ) ;
#46424=LINE ( 'NONE', #19551, #14063 ) ;
#46428=ORIENTED_EDGE ( 'NONE', *, *, #13001, .F. ) ;
#46429=ORIENTED_EDGE ( 'NONE', *, *, #51274, .T. ) ;
#46432=ADVANCED_FACE ( 'NONE', ( #298 ), #43417, .T. ) ;
#46435=CYLINDRICAL_SURFACE ( 'NONE', #50825, 4.000000000000000000 ) ;
#46436=ORIENTED_EDGE ( 'NONE', *, *, #6506, .F. ) ;
#46437=VERTEX_POINT ( 'NONE', #33157 ) ;
#46445=ORIENTED_EDGE ( 'NONE', *, *, #14012, .T. ) ;
#46446=DIRECTION ( 'NONE',  ( 0.000000000000000000, 0.000000000000000000, 1.000000000000000000 ) ) ;
#46448=AXIS2_PLACEMENT_3D ( 'NONE', #68462, #20015, #15761 ) ;
#46450=DIRECTION ( 'NONE',  ( 1.000000000000000000, -0.000000000000000000, -0.000000000000000000 ) ) ;
#46457=CIRCLE ( 'NONE', #29494, 4.000000000000000888 ) ;
#46466=CARTESIAN_POINT ( 'NONE',  ( -17.00000000000000000, -17.50000000000000000, 19.33772233983200195 ) ) ;
#46479=LINE ( 'NONE', #35880, #65814 ) ;
#46483=DIRECTION ( 'NONE',  ( 0.000000000000000000, 0.000000000000000000, 1.000000000000000000 ) ) ;
#46489=DIRECTION ( 'NONE',  ( 0.000000000000000000, 0.000000000000000000, -1.000000000000000000 ) ) ;
#46500=ORIENTED_EDGE ( 'NONE', *, *, #16797, .F. ) ;
#46503=CIRCLE ( 'NONE', #30720, 4.000000000000000888 ) ;
#46530=CARTESIAN_POINT ( 'NONE',  ( 30.00000000000000000, -12.00000000000000000, 10.52786404500095863 ) ) ;
#46539=CARTESIAN_POINT ( 'NONE',  ( -11.75000000000000000, -5.000000000000000000, -26.25000000000000000 ) ) ;
#46541=LINE ( 'NONE', #52571, #51701 ) ;
#46550=DIRECTION ( 'NONE',  ( 0.000000000000000000, 1.000000000000000000, 0.000000000000000000 ) ) ;
#46555=EDGE_LOOP ( 'NONE', ( #11241, #36986, #37864, #64424 ) ) ;
#46556=CARTESIAN_POINT ( 'NONE',  ( 24.00000000000000000, -17.00000000000000000, -15.70499999999969809 ) ) ;
#46567=ADVANCED_FACE ( 'NONE', ( #29223 ), #50798, .T. ) ;
#46571=DIRECTION ( 'NONE',  ( 0.000000000000000000, 0.000000000000000000, 1.000000000000000000 ) ) ;
#46574=CARTESIAN_POINT ( 'NONE',  ( -11.00000000000000000, -5.200000000000001066, 60.00000000000000000 ) ) ;
#46575=CIRCLE ( 'NONE', #42096, 4.000000000000000888 ) ;
#46581=ORIENTED_EDGE ( 'NONE', *, *, #29756, .T. ) ;
#46596=VECTOR ( 'NONE', #6906, 1000.000000000000000 ) ;
#46600=CARTESIAN_POINT ( 'NONE',  ( -11.50000000000000000, -12.00000000000000000, 11.03137303340310282 ) ) ;
#46608=EDGE_CURVE ( 'NONE', #23311, #45889, #58214, .T. ) ;
#46615=CARTESIAN_POINT ( 'NONE',  ( -14.25000000000000000, -2.500000000000000000, 23.22168783648699986 ) ) ;
#46632=EDGE_CURVE ( 'NONE', #5665, #36973, #9424, .T. ) ;
#46633=EDGE_CURVE ( 'NONE', #1993, #11369, #14732, .T. ) ;
#46636=DIRECTION ( 'NONE',  ( 0.000000000000000000, 0.7096009616570518874, 0.7046037717862339012 ) ) ;
#46639=CARTESIAN_POINT ( 'NONE',  ( -11.00000000000000000, -16.64230188589299786, 14.64519951917100116 ) ) ;
#46640=EDGE_CURVE ( 'NONE', #51018, #1191, #6533, .T. ) ;
#46642=CARTESIAN_POINT ( 'NONE',  ( -23.48000000000000043, -15.50000000000000000, -26.00000000000000355 ) ) ;
#46645=CIRCLE ( 'NONE', #375, 3.499999999999849454 ) ;
#46646=EDGE_CURVE ( 'NONE', #42454, #32370, #46541, .T. ) ;
#46652=VERTEX_POINT ( 'NONE', #63529 ) ;
#46653=CARTESIAN_POINT ( 'NONE',  ( 30.00000000000000000, -14.33999999999999986, 14.50000000000000000 ) ) ;
#46659=DIRECTION ( 'NONE',  ( 0.000000000000000000, -0.9938079899998859545, 0.1111111111112941946 ) ) ;
#46679=CARTESIAN_POINT ( 'NONE',  ( 30.00000000000000000, -12.00000000000000000, -10.20500000000000007 ) ) ;
#46680=ORIENTED_EDGE ( 'NONE', *, *, #13674, .T. ) ;
#46691=EDGE_LOOP ( 'NONE', ( #25689, #68014, #6855, #34941 ) ) ;
#46702=EDGE_LOOP ( 'NONE', ( #56220, #43484, #68453, #16364 ) ) ;
#46717=ADVANCED_FACE ( 'NONE', ( #64917 ), #5523, .F. ) ;
#46720=DIRECTION ( 'NONE',  ( 1.000000000000000000, -0.000000000000000000, -0.000000000000000000 ) ) ;
#46736=VECTOR ( 'NONE', #61975, 1000.000000000000000 ) ;
#46739=ADVANCED_FACE ( 'NONE', ( #27080 ), #48653, .T. ) ;
#46741=ORIENTED_EDGE ( 'NONE', *, *, #28073, .F. ) ;
#46744=EDGE_CURVE ( 'NONE', #58038, #50249, #68612, .T. ) ;
#46749=CARTESIAN_POINT ( 'NONE',  ( 30.00000000000000000, -9.487228132326899654, -12.50000000000000000 ) ) ;
#46752=ORIENTED_EDGE ( 'NONE', *, *, #3874, .F. ) ;
#46755=EDGE_LOOP ( 'NONE', ( #5680, #46786, #52489, #10191, #60165, #48020, #58072 ) ) ;
#46758=DIRECTION ( 'NONE',  ( -1.000000000000000000, 0.000000000000000000, 0.000000000000000000 ) ) ;
#46765=VERTEX_POINT ( 'NONE', #32398 ) ;
#46772=AXIS2_PLACEMENT_3D ( 'NONE', #16711, #10695, #16350 ) ;
#46775=ORIENTED_EDGE ( 'NONE', *, *, #47117, .T. ) ;
#46780=VECTOR ( 'NONE', #61227, 1000.000000000000000 ) ;
#46784=EDGE_CURVE ( 'NONE', #62351, #4816, #26740, .T. ) ;
#46786=ORIENTED_EDGE ( 'NONE', *, *, #57345, .T. ) ;
#46790=CARTESIAN_POINT ( 'NONE',  ( -29.25000000000000000, -5.200000000000001066, 60.00000000000000000 ) ) ;
#46796=CARTESIAN_POINT ( 'NONE',  ( 30.00000000000000000, -11.50000000000000000, 15.00000000000000000 ) ) ;
#46799=VECTOR ( 'NONE', #31141, 1000.000000000000000 ) ;
#46800=VERTEX_POINT ( 'NONE', #38390 ) ;
#46801=CARTESIAN_POINT ( 'NONE',  ( 14.66434062215688883, -0.3156604612129069731, 21.53909249377453250 ) ) ;
#46805=EDGE_LOOP ( 'NONE', ( #53695, #33811, #10272, #20066 ) ) ;
#46806=PLANE ( 'NONE',  #67624 ) ;
#46810=VECTOR ( 'NONE', #35003, 1000.000000000000000 ) ;
#46814=CIRCLE ( 'NONE', #50192, 0.5000000000001392220 ) ;
#46815=ORIENTED_EDGE ( 'NONE', *, *, #49645, .T. ) ;
#46817=CARTESIAN_POINT ( 'NONE',  ( 30.00000000000000000, -5.599999999999999645, 27.00000000000000000 ) ) ;
#46824=LINE ( 'NONE', #68406, #41106 ) ;
#46832=FACE_OUTER_BOUND ( 'NONE', #57463, .T. ) ;
#46842=CARTESIAN_POINT ( 'NONE',  ( -22.14589803375000088, -15.50000000000000000, 21.50000000000000000 ) ) ;
#46860=DIRECTION ( 'NONE',  ( 0.000000000000000000, 0.7046037717862339012, 0.7096009616570518874 ) ) ;
#46865=ORIENTED_EDGE ( 'NONE', *, *, #55265, .F. ) ;
#46866=LINE ( 'NONE', #62075, #59836 ) ;
#46873=VECTOR ( 'NONE', #51753, 1000.000000000000000 ) ;
#46878=VERTEX_POINT ( 'NONE', #12536 ) ;
#46879=VECTOR ( 'NONE', #2419, 1000.000000000000000 ) ;
#46886=CIRCLE ( 'NONE', #2874, 3.299999999999473577 ) ;
#46892=DIRECTION ( 'NONE',  ( 0.000000000000000000, 0.6857142857142869419, -0.7278708115918273158 ) ) ;
#46904=CARTESIAN_POINT ( 'NONE',  ( -25.50000000000000355, 0.000000000000000000, -22.50000000000000000 ) ) ;
#46907=CARTESIAN_POINT ( 'NONE',  ( -11.00000000000000000, -14.04000000000000092, 17.04524521594300523 ) ) ;
#46912=CARTESIAN_POINT ( 'NONE',  ( 11.50000000000000000, -11.50000000000000000, -19.00000000000000000 ) ) ;
#46913=EDGE_CURVE ( 'NONE', #58012, #41307, #1944, .T. ) ;
#46924=CYLINDRICAL_SURFACE ( 'NONE', #11919, 4.500000000000189182 ) ;
#46927=VECTOR ( 'NONE', #37769, 1000.000000000000000 ) ;
#46955=CARTESIAN_POINT ( 'NONE',  ( 28.00000000000000000, -15.50000000000000000, 14.50000000000000000 ) ) ;
#46957=VERTEX_POINT ( 'NONE', #24207 ) ;
#46959=CARTESIAN_POINT ( 'NONE',  ( -29.50000000000000355, -11.70000000000000284, 11.00000000000000000 ) ) ;
#46968=EDGE_LOOP ( 'NONE', ( #45462, #13080, #3131, #13290, #44017, #22532, #65255 ) ) ;
#46970=CARTESIAN_POINT ( 'NONE',  ( -15.08565937784311295, -0.3156604612129216836, -23.70415600323552852 ) ) ;
#46981=FACE_OUTER_BOUND ( 'NONE', #38602, .T. ) ;
#46986=CARTESIAN_POINT ( 'NONE',  ( 30.00000000000000000, -5.200000000000001066, -9.400000000000000355 ) ) ;
#46991=CARTESIAN_POINT ( 'NONE',  ( 15.50000000000000000, -1.037157890325000054, -22.50000000000000000 ) ) ;
#46993=CARTESIAN_POINT ( 'NONE',  ( -13.00000000000000178, -17.50000000000000000, -20.05051025721700242 ) ) ;
#47003=DIRECTION ( 'NONE',  ( 0.8660254037844485886, 0.000000000000000000, -0.4999999999999827360 ) ) ;
#47004=CARTESIAN_POINT ( 'NONE',  ( 11.50000000000000000, -12.00000000000000000, -10.69999999999999929 ) ) ;
#47012=CARTESIAN_POINT ( 'NONE',  ( -25.50000000000000355, -17.50000000000000000, -22.50000000000000000 ) ) ;
#47022=DIRECTION ( 'NONE',  ( 0.3479852726768751237, 0.000000000000000000, 0.9375000000000004441 ) ) ;
#47024=DIRECTION ( 'NONE',  ( 0.000000000000000000, 0.000000000000000000, -1.000000000000000000 ) ) ;
#47031=CARTESIAN_POINT ( 'NONE',  ( -25.50000000000000355, -15.50000000000000000, -24.50000000000000000 ) ) ;
#47032=VERTEX_POINT ( 'NONE', #46466 ) ;
#47035=VECTOR ( 'NONE', #19774, 1000.000000000000000 ) ;
#47043=FACE_OUTER_BOUND ( 'NONE', #24095, .T. ) ;
#47049=ORIENTED_EDGE ( 'NONE', *, *, #66413, .T. ) ;
#47061=ORIENTED_EDGE ( 'NONE', *, *, #2287, .F. ) ;
#47066=CARTESIAN_POINT ( 'NONE',  ( 25.50000000000000355, -5.200000000000001066, -20.49999999999999645 ) ) ;
#47068=FACE_OUTER_BOUND ( 'NONE', #42190, .T. ) ;
#47069=ORIENTED_EDGE ( 'NONE', *, *, #5649, .F. ) ;
#47071=DIRECTION ( 'NONE',  ( 0.000000000000000000, 0.000000000000000000, 1.000000000000000000 ) ) ;
#47073=AXIS2_PLACEMENT_3D ( 'NONE', #2121, #45237, #44543 ) ;
#47078=VECTOR ( 'NONE', #35213, 1000.000000000000000 ) ;
#47080=ADVANCED_FACE ( 'NONE', ( #63795 ), #47525, .T. ) ;
#47084=CIRCLE ( 'NONE', #10996, 2.250000000000001776 ) ;
#47092=CARTESIAN_POINT ( 'NONE',  ( -14.25000000000000000, -2.500000000000000000, -23.22168783648699986 ) ) ;
#47095=CARTESIAN_POINT ( 'NONE',  ( 30.00000000000000000, -17.35230188589299871, -15.35019951917099945 ) ) ;
#47097=VECTOR ( 'NONE', #55810, 1000.000000000000114 ) ;
#47099=LINE ( 'NONE', #25179, #37664 ) ;
#47101=VERTEX_POINT ( 'NONE', #58131 ) ;
#47106=B_SPLINE_CURVE_WITH_KNOTS ( 'NONE', 3,
 ( #14696, #46164, #51475, #19294, #41569, #36609 ),
 .UNSPECIFIED., .F., .F.,
 ( 4, 2, 4 ),
 ( 0.0002380763768132232450, 0.7291065797294586925, 1.457975083082104106 ),
 .UNSPECIFIED. ) ;
#47107=VECTOR ( 'NONE', #62907, 999.9999999999998863 ) ;
#47113=ORIENTED_EDGE ( 'NONE', *, *, #30391, .F. ) ;
#47114=DIRECTION ( 'NONE',  ( -1.000000000000000000, 0.000000000000000000, 0.000000000000000000 ) ) ;
#47117=EDGE_CURVE ( 'NONE', #13055, #6004, #5796, .T. ) ;
#47121=VERTEX_POINT ( 'NONE', #58841 ) ;
#47122=ORIENTED_EDGE ( 'NONE', *, *, #19091, .T. ) ;
#47123=LINE ( 'NONE', #57014, #5818 ) ;
#47125=ORIENTED_EDGE ( 'NONE', *, *, #38577, .F. ) ;
#47126=CARTESIAN_POINT ( 'NONE',  ( 25.50000000000000355, -17.50000000000000000, -22.50000000000000000 ) ) ;
#47134=ORIENTED_EDGE ( 'NONE', *, *, #66736, .F. ) ;
#47138=EDGE_CURVE ( 'NONE', #17638, #43882, #4747, .T. ) ;
#47140=ORIENTED_EDGE ( 'NONE', *, *, #21431, .T. ) ;
#47141=CYLINDRICAL_SURFACE ( 'NONE', #620, 3.499999999999850342 ) ;
#47152=VECTOR ( 'NONE', #7226, 1000.000000000000000 ) ;
#47153=AXIS2_PLACEMENT_3D ( 'NONE', #46242, #8770, #67819 ) ;
#47155=VERTEX_POINT ( 'NONE', #11426 ) ;
#47168=LINE ( 'NONE', #68734, #792 ) ;
#47170=VERTEX_POINT ( 'NONE', #10397 ) ;
#47173=LINE ( 'NONE', #20287, #4148 ) ;
#47178=FACE_OUTER_BOUND ( 'NONE', #54101, .T. ) ;
#47181=CARTESIAN_POINT ( 'NONE',  ( -28.00000000000000000, -17.50000000000000000, -20.05051025721700242 ) ) ;
#47188=CIRCLE ( 'NONE', #18912, 4.000000000000000888 ) ;
#47189=ADVANCED_FACE ( 'NONE', ( #16051 ), #59184, .T. ) ;
#47206=CARTESIAN_POINT ( 'NONE',  ( 29.50000000000000355, -11.50000000000000000, -15.00000000000000000 ) ) ;
#47213=ORIENTED_EDGE ( 'NONE', *, *, #22093, .F. ) ;
#47219=ORIENTED_EDGE ( 'NONE', *, *, #54401, .T. ) ;
#47223=VERTEX_POINT ( 'NONE', #42915 ) ;
#47232=DIRECTION ( 'NONE',  ( 0.4999999999999827360, 0.000000000000000000, 0.8660254037844485886 ) ) ;
#47241=CIRCLE ( 'NONE', #23502, 4.000000000000000000 ) ;
#47243=EDGE_CURVE ( 'NONE', #16302, #7103, #42759, .T. ) ;
#47247=ADVANCED_FACE ( 'NONE', ( #33685 ), #39363, .T. ) ;
#47257=CARTESIAN_POINT ( 'NONE',  ( 29.50000000000000355, -11.70000000000000284, 11.00000000000000000 ) ) ;
#47263=CARTESIAN_POINT ( 'NONE',  ( 11.00000000000000000, -13.79999999999979998, 17.30000000000000071 ) ) ;
#47268=EDGE_CURVE ( 'NONE', #65337, #47349, #49943, .T. ) ;
#47274=CARTESIAN_POINT ( 'NONE',  ( 15.08565937784311117, -0.3156604612129225162, 23.70415600323552852 ) ) ;
#47279=DIRECTION ( 'NONE',  ( 1.000000000000000000, 0.000000000000000000, 0.000000000000000000 ) ) ;
#47284=VECTOR ( 'NONE', #31024, 1000.000000000000000 ) ;
#47285=VERTEX_POINT ( 'NONE', #65863 ) ;
#47291=VECTOR ( 'NONE', #68561, 1000.000000000000000 ) ;
#47311=ORIENTED_EDGE ( 'NONE', *, *, #27594, .T. ) ;
#47312=LINE ( 'NONE', #48366, #64963 ) ;
#47313=DIRECTION ( 'NONE',  ( 1.000000000000000000, -0.000000000000000000, -0.000000000000000000 ) ) ;
#47314=ORIENTED_EDGE ( 'NONE', *, *, #26728, .F. ) ;
#47316=LINE ( 'NONE', #26455, #22683 ) ;
#47323=ORIENTED_EDGE ( 'NONE', *, *, #32352, .T. ) ;
#47328=CARTESIAN_POINT ( 'NONE',  ( -17.24945551514599984, -17.50000000000000000, -25.53140320652400064 ) ) ;
#47330=AXIS2_PLACEMENT_3D ( 'NONE', #44573, #1450, #23021 ) ;
#47338=CARTESIAN_POINT ( 'NONE',  ( 30.00000000000000000, -12.00000000000000000, 11.03137303340310282 ) ) ;
#47347=VECTOR ( 'NONE', #64850, 1000.000000000000000 ) ;
#47349=VERTEX_POINT ( 'NONE', #23774 ) ;
#47355=CARTESIAN_POINT ( 'NONE',  ( 15.50000000000000000, -0.4000000000005274892, -19.20000000000052864 ) ) ;
#47359=CARTESIAN_POINT ( 'NONE',  ( -30.00000000000000000, -5.599999999999999645, -9.000000000000001776 ) ) ;
#47361=LINE ( 'NONE', #42757, #24878 ) ;
#47367=FACE_OUTER_BOUND ( 'NONE', #33664, .T. ) ;
#47369=ADVANCED_FACE ( 'NONE', ( #34022 ), #61582, .T. ) ;
#47375=ORIENTED_EDGE ( 'NONE', *, *, #8840, .F. ) ;
#47377=ORIENTED_EDGE ( 'NONE', *, *, #60866, .T. ) ;
#47378=DIRECTION ( 'NONE',  ( 1.000000000000000000, 0.000000000000000000, 0.000000000000000000 ) ) ;
#47382=CIRCLE ( 'NONE', #23637, 4.000000000000000888 ) ;
#47385=LINE ( 'NONE', #31489, #48265 ) ;
#47389=DIRECTION ( 'NONE',  ( -1.000000000000000000, 0.000000000000000000, 0.000000000000000000 ) ) ;
#47392=ORIENTED_EDGE ( 'NONE', *, *, #36771, .T. ) ;
#47400=ORIENTED_EDGE ( 'NONE', *, *, #19402, .F. ) ;
#47401=ORIENTED_EDGE ( 'NONE', *, *, #35671, .F. ) ;
#47408=DIRECTION ( 'NONE',  ( -1.000000000000000000, 0.000000000000000000, 0.000000000000000000 ) ) ;
#47411=CIRCLE ( 'NONE', #11269, 4.000000000000000888 ) ;
#47415=VERTEX_POINT ( 'NONE', #56647 ) ;
#47416=LINE ( 'NONE', #32570, #7646 ) ;
#47423=CARTESIAN_POINT ( 'NONE',  ( -11.00000000000000000, -9.200000000000120082, 17.30000000000000071 ) ) ;
#47431=VECTOR ( 'NONE', #16141, 1000.000000000000000 ) ;
#47434=EDGE_CURVE ( 'NONE', #42236, #30238, #37108, .T. ) ;
#47435=CARTESIAN_POINT ( 'NONE',  ( 14.25000000000000000, -0.2038245569916330158, -21.77831216351300014 ) ) ;
#47439=FACE_OUTER_BOUND ( 'NONE', #10963, .T. ) ;
#47448=ADVANCED_FACE ( 'NONE', ( #3255 ), #64323, .T. ) ;
#47462=DIRECTION ( 'NONE',  ( 0.000000000000000000, -1.000000000000000000, 0.000000000000000000 ) ) ;
#47476=EDGE_LOOP ( 'NONE', ( #35416, #6098, #38541, #14645 ) ) ;
#47480=VECTOR ( 'NONE', #65756, 1000.000000000000000 ) ;
#47488=FACE_OUTER_BOUND ( 'NONE', #30435, .T. ) ;
#47496=DIRECTION ( 'NONE',  ( 0.000000000000000000, 0.000000000000000000, 1.000000000000000000 ) ) ;
#47504=ADVANCED_FACE ( 'NONE', ( #10567 ), #5281, .F. ) ;
#47509=DIRECTION ( 'NONE',  ( 0.000000000000000000, 0.000000000000000000, 1.000000000000000000 ) ) ;
#47510=VECTOR ( 'NONE', #2259, 1000.000000000000000 ) ;
#47520=AXIS2_PLACEMENT_3D ( 'NONE', #60343, #1315, #65669 ) ;
#47525=PLANE ( 'NONE',  #3190 ) ;
#47527=EDGE_CURVE ( 'NONE', #34438, #44371, #2118, .T. ) ;
#47529=EDGE_LOOP ( 'NONE', ( #43090, #60147, #63838, #65108, #15489, #40954, #13280, #14311, #46351, #56495, #13367, #63362, #61913, #40843, #59758 ) ) ;
#47533=EDGE_CURVE ( 'NONE', #16044, #69842, #38234, .T. ) ;
#47536=ORIENTED_EDGE ( 'NONE', *, *, #32860, .F. ) ;
#47537=CARTESIAN_POINT ( 'NONE',  ( 17.00000000000000000, -15.50000000000000000, 14.50000000000000000 ) ) ;
#47543=ORIENTED_EDGE ( 'NONE', *, *, #10968, .F. ) ;
#47563=ORIENTED_EDGE ( 'NONE', *, *, #23293, .F. ) ;
#47574=ORIENTED_EDGE ( 'NONE', *, *, #18884, .F. ) ;
#47580=ORIENTED_EDGE ( 'NONE', *, *, #55502, .F. ) ;
#47584=DIRECTION ( 'NONE',  ( 0.000000000000000000, 1.000000000000000000, 0.000000000000000000 ) ) ;
#47585=CARTESIAN_POINT ( 'NONE',  ( 30.00000000000000000, -11.50000000000000000, -15.00000000000000000 ) ) ;
#47588=EDGE_LOOP ( 'NONE', ( #30436, #35959, #27567, #19118 ) ) ;
#47591=AXIS2_PLACEMENT_3D ( 'NONE', #65643, #65311, #23542 ) ;
#47598=CARTESIAN_POINT ( 'NONE',  ( -25.49999999999869971, -15.50000000000000000, 22.50000000000000000 ) ) ;
#47613=VECTOR ( 'NONE', #61292, 1000.000000000000000 ) ;
#47633=DIRECTION ( 'NONE',  ( -1.000000000000000000, 0.000000000000000000, 0.000000000000000000 ) ) ;
#47655=ORIENTED_EDGE ( 'NONE', *, *, #12831, .T. ) ;
#47660=DIRECTION ( 'NONE',  ( 0.000000000000000000, 0.000000000000000000, -1.000000000000000000 ) ) ;
#47666=VERTEX_POINT ( 'NONE', #21870 ) ;
#47695=CYLINDRICAL_SURFACE ( 'NONE', #42587, 4.500000000000188294 ) ;
#47696=DIRECTION ( 'NONE',  ( 0.000000000000000000, 0.000000000000000000, 1.000000000000000000 ) ) ;
#47705=CARTESIAN_POINT ( 'NONE',  ( -11.00000000000000000, -11.50000000000100009, -19.50000000000103739 ) ) ;
#47707=LINE ( 'NONE', #69276, #58041 ) ;
#47709=EDGE_LOOP ( 'NONE', ( #35117, #13305, #47536, #61089 ) ) ;
#47712=DIRECTION ( 'NONE',  ( 0.000000000000000000, -0.1111111111108836896, -0.9938079899999319178 ) ) ;
#47716=ORIENTED_EDGE ( 'NONE', *, *, #11189, .T. ) ;
#47717=CARTESIAN_POINT ( 'NONE',  ( -11.00000000000000000, -17.50000000000000000, -15.70500000000000007 ) ) ;
#47720=EDGE_CURVE ( 'NONE', #22255, #67830, #8368, .T. ) ;
#47721=DIRECTION ( 'NONE',  ( 0.000000000000000000, 1.000000000000000000, 0.000000000000000000 ) ) ;
#47722=ADVANCED_FACE ( 'NONE', ( #66724, #23248, #17936, #67444, #45501 ), #50808, .F. ) ;
#47726=DIRECTION ( 'NONE',  ( 0.000000000000000000, 1.000000000000000000, 0.000000000000000000 ) ) ;
#47730=ORIENTED_EDGE ( 'NONE', *, *, #67999, .T. ) ;
#47732=LINE ( 'NONE', #20861, #69939 ) ;
#47733=CARTESIAN_POINT ( 'NONE',  ( -30.00000000000000000, -11.10796162543699950, -9.102987789146602893 ) ) ;
#47748=AXIS2_PLACEMENT_3D ( 'NONE', #60297, #17517, #5880 ) ;
#47752=VERTEX_POINT ( 'NONE', #2379 ) ;
#47757=EDGE_CURVE ( 'NONE', #66251, #58795, #7674, .T. ) ;
#47761=EDGE_CURVE ( 'NONE', #64729, #30577, #51874, .T. ) ;
#47763=CARTESIAN_POINT ( 'NONE',  ( 17.00000000000000000, -16.28999999999710369, 15.00000000000794920 ) ) ;
#47781=CARTESIAN_POINT ( 'NONE',  ( -24.00000000000000000, -17.50000000000000000, -15.70500000000000007 ) ) ;
#47786=CARTESIAN_POINT ( 'NONE',  ( 30.00000000000000000, -11.70000000000012008, -10.70000000000011831 ) ) ;
#47826=DIRECTION ( 'NONE',  ( -0.4999999999999832356, 0.000000000000000000, 0.8660254037844483666 ) ) ;
#47830=VECTOR ( 'NONE', #68761, 1000.000000000000000 ) ;
#47831=CARTESIAN_POINT ( 'NONE',  ( 11.00000000000000000, -16.64230188589299786, 14.64519951917100116 ) ) ;
#47834=ORIENTED_EDGE ( 'NONE', *, *, #44484, .T. ) ;
#47849=VERTEX_POINT ( 'NONE', #53289 ) ;
#47853=AXIS2_PLACEMENT_3D ( 'NONE', #2791, #45936, #52291 ) ;
#47865=ORIENTED_EDGE ( 'NONE', *, *, #1793, .T. ) ;
#47867=DIRECTION ( 'NONE',  ( 0.000000000000000000, -0.9938079899998859545, 0.1111111111112941946 ) ) ;
#47871=CARTESIAN_POINT ( 'NONE',  ( 30.00000000000000000, -14.04000000000000092, 17.04524521594300523 ) ) ;
#47874=ORIENTED_EDGE ( 'NONE', *, *, #6556, .T. ) ;
#47878=CARTESIAN_POINT ( 'NONE',  ( -15.50000000000000000, -0.4000000000000000222, -22.50000000000000000 ) ) ;
#47881=DIRECTION ( 'NONE',  ( -1.000000000000000000, 0.000000000000000000, 0.000000000000000000 ) ) ;
#47882=ORIENTED_EDGE ( 'NONE', *, *, #38044, .F. ) ;
#47886=DIRECTION ( 'NONE',  ( 0.000000000000000000, 0.000000000000000000, 1.000000000000000000 ) ) ;
#47893=EDGE_CURVE ( 'NONE', #65641, #49539, #68130, .T. ) ;
#47924=EDGE_CURVE ( 'NONE', #45591, #18488, #10138, .T. ) ;
#47927=LINE ( 'NONE', #11136, #37283 ) ;
#47932=CARTESIAN_POINT ( 'NONE',  ( -30.00000000000000000, -5.599999999999379696, 26.60000000000059828 ) ) ;
#47936=EDGE_LOOP ( 'NONE', ( #66581, #28692, #25321, #38904, #692, #7359, #21034, #58667, #33975, #24298, #38101, #65387, #19560, #69056, #23849 ) ) ;
#47941=EDGE_CURVE ( 'NONE', #11904, #46878, #16134, .T. ) ;
#47942=CARTESIAN_POINT ( 'NONE',  ( 30.00000000000000000, -8.959999999999999076, 17.04524521594300523 ) ) ;
#47962=LINE ( 'NONE', #21090, #9614 ) ;
#47969=CARTESIAN_POINT ( 'NONE',  ( -25.50000000000000355, 0.000000000000000000, -20.24999999999999645 ) ) ;
#47971=VERTEX_POINT ( 'NONE', #6578 ) ;
#47973=CARTESIAN_POINT ( 'NONE',  ( 15.50000000000000000, -1.037157890325000054, -18.50000000000000000 ) ) ;
#47974=CARTESIAN_POINT ( 'NONE',  ( 30.00000000000000000, -11.50000000000100009, 15.00000000000084910 ) ) ;
#47984=ORIENTED_EDGE ( 'NONE', *, *, #289, .F. ) ;
#47985=ADVANCED_FACE ( 'NONE', ( #59957 ), #17516, .F. ) ;
#47987=DIRECTION ( 'NONE',  ( 0.000000000000000000, 0.000000000000000000, 1.000000000000000000 ) ) ;
#47990=ORIENTED_EDGE ( 'NONE', *, *, #47243, .T. ) ;
#48000=AXIS2_PLACEMENT_3D ( 'NONE', #27571, #56179, #33566 ) ;
#48001=DIRECTION ( 'NONE',  ( 0.000000000000000000, 0.000000000000000000, -1.000000000000000000 ) ) ;
#48006=CARTESIAN_POINT ( 'NONE',  ( 29.25000000000000000, -5.200000000000001066, -26.25000000000000000 ) ) ;
#48011=EDGE_CURVE ( 'NONE', #33817, #50086, #33089, .T. ) ;
#48020=ORIENTED_EDGE ( 'NONE', *, *, #17572, .F. ) ;
#48022=CIRCLE ( 'NONE', #17518, 2.000000000000001776 ) ;
#48024=VERTEX_POINT ( 'NONE', #571 ) ;
#48025=CARTESIAN_POINT ( 'NONE',  ( 11.75000000000000000, -5.000000000000000000, 21.10805890929250239 ) ) ;
#48031=CARTESIAN_POINT ( 'NONE',  ( 30.00000000000000000, -16.28999999999710369, 15.00000000000794920 ) ) ;
#48039=FACE_OUTER_BOUND ( 'NONE', #40771, .T. ) ;
#48042=VERTEX_POINT ( 'NONE', #17168 ) ;
#48050=AXIS2_PLACEMENT_3D ( 'NONE', #11551, #33130, #29824 ) ;
#48054=VECTOR ( 'NONE', #31029, 1000.000000000000000 ) ;
#48055=VECTOR ( 'NONE', #52886, 1000.000000000000000 ) ;
#48061=LINE ( 'NONE', #64330, #52618 ) ;
#48067=CARTESIAN_POINT ( 'NONE',  ( -25.50000000000000355, -5.200000000000001066, -22.50000000000000000 ) ) ;
#48070=VERTEX_POINT ( 'NONE', #53630 ) ;
#48076=DIRECTION ( 'NONE',  ( 0.000000000000000000, 1.000000000000000000, 0.000000000000000000 ) ) ;
#48088=CARTESIAN_POINT ( 'NONE',  ( 14.66434062215688883, -0.3156604612129108589, -23.46090750622545684 ) ) ;
#48089=DIRECTION ( 'NONE',  ( 0.000000000000000000, -0.7057491738665943037, -0.7084617869628675457 ) ) ;
#48096=CARTESIAN_POINT ( 'NONE',  ( -15.50000000000000000, -15.50000000000000000, -25.99999999999985079 ) ) ;
#48100=AXIS2_PLACEMENT_3D ( 'NONE', #24238, #55712, #18571 ) ;
#48105=VECTOR ( 'NONE', #27437, 1000.000000000000000 ) ;
#48106=DIRECTION ( 'NONE',  ( -1.000000000000000000, 0.000000000000000000, 0.000000000000000000 ) ) ;
#48110=AXIS2_PLACEMENT_3D ( 'NONE', #8143, #24425, #45989 ) ;
#48115=LINE ( 'NONE', #58387, #10461 ) ;
#48117=VECTOR ( 'NONE', #39809, 1000.000000000000000 ) ;
#48130=EDGE_CURVE ( 'NONE', #33635, #55576, #25917, .T. ) ;
#48131=FACE_OUTER_BOUND ( 'NONE', #19365, .T. ) ;
#48135=ADVANCED_FACE ( 'NONE', ( #29516 ), #12545, .T. ) ;
#48154=CIRCLE ( 'NONE', #34596, 0.4999999999991842636 ) ;
#48156=AXIS2_PLACEMENT_3D ( 'NONE', #9941, #31510, #42796 ) ;
#48159=VERTEX_POINT ( 'NONE', #50728 ) ;
#48164=VECTOR ( 'NONE', #36886, 1000.000000000000000 ) ;
#48172=FACE_OUTER_BOUND ( 'NONE', #16221, .T. ) ;
#48191=DIRECTION ( 'NONE',  ( 0.000000000000000000, 0.7071067811865496822, 0.7071067811865454633 ) ) ;
#48192=ORIENTED_EDGE ( 'NONE', *, *, #34732, .T. ) ;
#48194=VECTOR ( 'NONE', #58, 1000.000000000000000 ) ;
#48204=CIRCLE ( 'NONE', #17700, 3.499999999999849454 ) ;
#48206=CARTESIAN_POINT ( 'NONE',  ( -16.75000000000000000, -0.2038245569916330158, -23.22168783648699986 ) ) ;
#48207=ORIENTED_EDGE ( 'NONE', *, *, #38404, .T. ) ;
#48212=CARTESIAN_POINT ( 'NONE',  ( 11.00000000000000000, -15.46862696659690073, -14.50000000000000000 ) ) ;
#48223=LINE ( 'NONE', #69433, #56469 ) ;
#48229=DIRECTION ( 'NONE',  ( 0.000000000000000000, -0.7278708115916149302, -0.6857142857145122061 ) ) ;
#48239=DIRECTION ( 'NONE',  ( 0.000000000000000000, -1.000000000000000000, 0.000000000000000000 ) ) ;
#48245=CARTESIAN_POINT ( 'NONE',  ( -30.00000000000000000, -16.64230188589299786, -14.64519951917100116 ) ) ;
#48249=B_SPLINE_CURVE_WITH_KNOTS ( 'NONE', 3,
 ( #54610, #16775, #38681, #21025, #15733, #37999 ),
 .UNSPECIFIED., .F., .F.,
 ( 4, 2, 4 ),
 ( 0.0002380763768132926339, 0.7291065797294586925, 1.457975083082104106 ),
 .UNSPECIFIED. ) ;
#48251=ORIENTED_EDGE ( 'NONE', *, *, #23747, .T. ) ;
#48257=DIRECTION ( 'NONE',  ( -1.000000000000000000, 0.000000000000000000, 0.000000000000000000 ) ) ;
#48259=EDGE_CURVE ( 'NONE', #38194, #52237, #66564, .T. ) ;
#48260=PLANE ( 'NONE',  #35702 ) ;
#48263=EDGE_CURVE ( 'NONE', #39654, #50592, #51792, .T. ) ;
#48265=VECTOR ( 'NONE', #16617, 1000.000000000000000 ) ;
#48268=ADVANCED_FACE ( 'NONE', ( #25630 ), #57787, .F. ) ;
#48277=CARTESIAN_POINT ( 'NONE',  ( -11.00000000000000000, -17.14999999999999858, -27.00000000000000000 ) ) ;
#48279=EDGE_LOOP ( 'NONE', ( #62395, #38261 ) ) ;
#48284=ORIENTED_EDGE ( 'NONE', *, *, #58933, .F. ) ;
#48286=CARTESIAN_POINT ( 'NONE',  ( 30.00000000000000000, -11.85423089348099879, 9.852125413066602277 ) ) ;
#48290=LINE ( 'NONE', #53257, #64541 ) ;
#48295=AXIS2_PLACEMENT_3D ( 'NONE', #9861, #14807, #52998 ) ;
#48298=VERTEX_POINT ( 'NONE', #4062 ) ;
#48309=CARTESIAN_POINT ( 'NONE',  ( 29.50000000000000355, -11.50000000000100009, 19.50000000000103739 ) ) ;
#48311=EDGE_CURVE ( 'NONE', #27939, #56472, #25980, .T. ) ;
#48323=CARTESIAN_POINT ( 'NONE',  ( -25.50000000000000355, 0.000000000000000000, -20.87899999999999778 ) ) ;
#48329=DIRECTION ( 'NONE',  ( 0.000000000000000000, 0.6857142857146703019, -0.7278708115914659382 ) ) ;
#48332=VERTEX_POINT ( 'NONE', #68052 ) ;
#48340=DIRECTION ( 'NONE',  ( -1.000000000000000000, 0.000000000000000000, 0.000000000000000000 ) ) ;
#48341=ORIENTED_EDGE ( 'NONE', *, *, #2710, .T. ) ;
#48349=EDGE_CURVE ( 'NONE', #49918, #17310, #19125, .T. ) ;
#48361=ORIENTED_EDGE ( 'NONE', *, *, #27491, .T. ) ;
#48362=EDGE_CURVE ( 'NONE', #8384, #19992, #5803, .T. ) ;
#48366=CARTESIAN_POINT ( 'NONE',  ( -28.00000000000000000, -17.35230188589299871, -15.35019951917099945 ) ) ;
#48370=DIRECTION ( 'NONE',  ( 0.000000000000000000, 0.000000000000000000, -1.000000000000000000 ) ) ;
#48371=CARTESIAN_POINT ( 'NONE',  ( 11.75000000000000000, -5.000000000000000000, -23.89194109070750471 ) ) ;
#48377=CARTESIAN_POINT ( 'NONE',  ( -14.45313394609757118, -0.2715358723599894386, -23.33896727494798284 ) ) ;
#48379=ORIENTED_EDGE ( 'NONE', *, *, #2853, .T. ) ;
#48382=CARTESIAN_POINT ( 'NONE',  ( -13.00000000000000178, -15.50000000000000000, 14.50000000000000000 ) ) ;
#48386=EDGE_CURVE ( 'NONE', #14923, #49745, #32324, .T. ) ;
#48391=CARTESIAN_POINT ( 'NONE',  ( 13.00000000000000178, -15.50000000000000000, 20.05051025721700242 ) ) ;
#48392=ADVANCED_FACE ( 'NONE', ( #37284 ), #49289, .F. ) ;
#48393=CARTESIAN_POINT ( 'NONE',  ( -11.00000000000000000, -11.85423089348099879, 9.852125413066602277 ) ) ;
#48395=DIRECTION ( 'NONE',  ( 0.000000000000000000, 0.000000000000000000, 1.000000000000000000 ) ) ;
#48399=FACE_OUTER_BOUND ( 'NONE', #67168, .T. ) ;
#48404=DIRECTION ( 'NONE',  ( -1.000000000000000000, 0.000000000000000000, 0.000000000000000000 ) ) ;
#48418=ADVANCED_FACE ( 'NONE', ( #10745 ), #21712, .T. ) ;
#48424=EDGE_LOOP ( 'NONE', ( #12083, #6396, #17218, #13794, #45454, #51610, #61187, #54545, #61945, #12486, #58810 ) ) ;
#48430=ORIENTED_EDGE ( 'NONE', *, *, #38115, .F. ) ;
#48438=DIRECTION ( 'NONE',  ( 0.000000000000000000, -1.000000000000000000, 0.000000000000000000 ) ) ;
#48447=ORIENTED_EDGE ( 'NONE', *, *, #1530, .F. ) ;
#48450=AXIS2_PLACEMENT_3D ( 'NONE', #61894, #13098, #67195 ) ;
#48452=ORIENTED_EDGE ( 'NONE', *, *, #46744, .F. ) ;
#48459=CARTESIAN_POINT ( 'NONE',  ( 28.00000000000000000, -15.50000000000000000, 20.05051025721700242 ) ) ;
#48478=EDGE_CURVE ( 'NONE', #4626, #11704, #34953, .T. ) ;
#48482=EDGE_CURVE ( 'NONE', #67437, #3267, #3383, .T. ) ;
#48492=EDGE_LOOP ( 'NONE', ( #8243, #62685, #37810, #5496 ) ) ;
#48493=CARTESIAN_POINT ( 'NONE',  ( 30.00000000000000000, -8.959999999999999076, -12.95475478405700009 ) ) ;
#48494=CARTESIAN_POINT ( 'NONE',  ( -25.49999999999869971, -15.50000000000000000, 22.50000000000000000 ) ) ;
#48505=VERTEX_POINT ( 'NONE', #34367 ) ;
#48507=FACE_BOUND ( 'NONE', #59909, .T. ) ;
#48508=CARTESIAN_POINT ( 'NONE',  ( 15.50000000000000000, -0.4000000000005274892, 19.20000000000052864 ) ) ;
#48510=CARTESIAN_POINT ( 'NONE',  ( 30.00000000000000000, -11.70000000000012008, 10.70000000000011831 ) ) ;
#48511=CARTESIAN_POINT ( 'NONE',  ( 24.00000000000000000, -16.64230188589299786, 14.64519951917100116 ) ) ;
#48515=ORIENTED_EDGE ( 'NONE', *, *, #5633, .F. ) ;
#48519=DIRECTION ( 'NONE',  ( -1.000000000000000000, 0.000000000000000000, 0.000000000000000000 ) ) ;
#48521=EDGE_CURVE ( 'NONE', #67310, #32707, #12464, .T. ) ;
#48523=AXIS2_PLACEMENT_3D ( 'NONE', #28112, #34429, #66628 ) ;
#48530=ORIENTED_EDGE ( 'NONE', *, *, #36911, .T. ) ;
#48541=LINE ( 'NONE', #21675, #30012 ) ;
#48547=ORIENTED_EDGE ( 'NONE', *, *, #23866, .T. ) ;
#48557=CARTESIAN_POINT ( 'NONE',  ( 15.50000000000000000, -2.500000000000000000, 23.94337567297399971 ) ) ;
#48563=VECTOR ( 'NONE', #35503, 1000.000000000000000 ) ;
#48570=AXIS2_PLACEMENT_3D ( 'NONE', #39002, #44639, #33693 ) ;
#48574=ADVANCED_FACE ( 'NONE', ( #55960, #40023 ), #40395, .T. ) ;
#48578=AXIS2_PLACEMENT_3D ( 'NONE', #61732, #46166, #7975 ) ;
#48581=DIRECTION ( 'NONE',  ( 1.000000000000000000, 0.000000000000000000, 0.000000000000000000 ) ) ;
#48585=CARTESIAN_POINT ( 'NONE',  ( 11.50000000000000000, -11.50000000000100009, 15.00000000000084910 ) ) ;
#48592=CARTESIAN_POINT ( 'NONE',  ( 25.50000000000000355, -5.578999999999999737, 24.12099999999999511 ) ) ;
#48593=CARTESIAN_POINT ( 'NONE',  ( -23.48000000000000043, -15.50000000000000000, 26.00000000000000355 ) ) ;
#48607=EDGE_CURVE ( 'NONE', #49327, #40754, #16913, .T. ) ;
#48614=ORIENTED_EDGE ( 'NONE', *, *, #49144, .F. ) ;
#48622=VECTOR ( 'NONE', #61280, 1000.000000000000000 ) ;
#48623=ORIENTED_EDGE ( 'NONE', *, *, #28891, .T. ) ;
#48624=VERTEX_POINT ( 'NONE', #20576 ) ;
#48634=CARTESIAN_POINT ( 'NONE',  ( -22.14589803375000088, -15.50000000000000000, 21.50000000000000000 ) ) ;
#48637=VECTOR ( 'NONE', #15614, 1000.000000000000000 ) ;
#48641=CARTESIAN_POINT ( 'NONE',  ( -11.75000000000000000, -5.200000000000001066, -11.75000000000000000 ) ) ;
#48647=EDGE_CURVE ( 'NONE', #52778, #27455, #19874, .T. ) ;
#48653=CYLINDRICAL_SURFACE ( 'NONE', #2013, 4.000000000000000000 ) ;
#48656=AXIS2_PLACEMENT_3D ( 'NONE', #1708, #17278, #38842 ) ;
#48658=EDGE_CURVE ( 'NONE', #12490, #69842, #24836, .T. ) ;
#48668=AXIS2_PLACEMENT_3D ( 'NONE', #43779, #1663, #23236 ) ;
#48679=CARTESIAN_POINT ( 'NONE',  ( 11.00000000000000000, -11.50000000000100009, -15.00000000000084910 ) ) ;
#48682=VERTEX_POINT ( 'NONE', #56997 ) ;
#48686=EDGE_CURVE ( 'NONE', #5255, #12276, #41087, .T. ) ;
#48687=CYLINDRICAL_SURFACE ( 'NONE', #36811, 3.499999999999038547 ) ;
#48688=EDGE_LOOP ( 'NONE', ( #63426, #46003, #23028, #42188 ) ) ;
#48694=CYLINDRICAL_SURFACE ( 'NONE', #50788, 3.499999999999038547 ) ;
#48698=ORIENTED_EDGE ( 'NONE', *, *, #69046, .F. ) ;
#48700=CARTESIAN_POINT ( 'NONE',  ( 11.00000000000000000, -14.04000000000000092, -14.80000000000000071 ) ) ;
#48702=DIRECTION ( 'NONE',  ( 0.000000000000000000, 1.000000000000000000, 0.000000000000000000 ) ) ;
#48704=ORIENTED_EDGE ( 'NONE', *, *, #22139, .T. ) ;
#48705=EDGE_LOOP ( 'NONE', ( #24712, #68681, #15286, #15297, #59000, #9009 ) ) ;
#48711=CARTESIAN_POINT ( 'NONE',  ( 30.00000000000000000, -17.50000000000000000, -15.70500000000000007 ) ) ;
#48713=AXIS2_PLACEMENT_3D ( 'NONE', #4353, #47462, #25913 ) ;
#48714=CARTESIAN_POINT ( 'NONE',  ( 24.00000000000000000, -17.50000000000000000, 15.70500000000000007 ) ) ;
#48717=ORIENTED_EDGE ( 'NONE', *, *, #10042, .T. ) ;
#48731=ORIENTED_EDGE ( 'NONE', *, *, #20427, .F. ) ;
#48735=CARTESIAN_POINT ( 'NONE',  ( -11.50000000000000000, -11.50000000000000000, 15.00000000000000000 ) ) ;
#48738=ADVANCED_FACE ( 'NONE', ( #53127 ), #24492, .T. ) ;
#48742=VECTOR ( 'NONE', #15951, 1000.000000000000000 ) ;
#48745=DIRECTION ( 'NONE',  ( 0.000000000000000000, 0.000000000000000000, 1.000000000000000000 ) ) ;
#48749=FACE_OUTER_BOUND ( 'NONE', #65235, .T. ) ;
#48754=DIRECTION ( 'NONE',  ( -1.000000000000000000, 0.000000000000000000, 0.000000000000000000 ) ) ;
#48767=ORIENTED_EDGE ( 'NONE', *, *, #3528, .F. ) ;
#48770=ORIENTED_EDGE ( 'NONE', *, *, #25397, .F. ) ;
#48771=CARTESIAN_POINT ( 'NONE',  ( -15.50000000000000000, 0.000000000000000000, -22.50000000000000000 ) ) ;
#48776=VERTEX_POINT ( 'NONE', #10668 ) ;
#48781=EDGE_LOOP ( 'NONE', ( #61877, #40038, #24125, #2244 ) ) ;
#48782=PRODUCT_DEFINITION_CONTEXT ( 'detailed design', #54903, 'design' ) ;
#48785=LINE ( 'NONE', #6338, #8359 ) ;
#48794=ADVANCED_FACE ( 'NONE', ( #11022 ), #32235, .F. ) ;
#48799=EDGE_CURVE ( 'NONE', #22437, #10280, #15857, .T. ) ;
#48803=ADVANCED_FACE ( 'NONE', ( #4675 ), #58769, .T. ) ;
#48811=EDGE_CURVE ( 'NONE', #18896, #2326, #4559, .T. ) ;
#48813=CARTESIAN_POINT ( 'NONE',  ( -25.50000000000000355, -15.50000000000000000, -22.50000000000000000 ) ) ;
#48819=AXIS2_PLACEMENT_3D ( 'NONE', #10239, #36772, #58342 ) ;
#48823=CARTESIAN_POINT ( 'NONE',  ( 29.25000000000000000, -5.000000000000000000, -11.75000000000000000 ) ) ;
#48828=AXIS2_PLACEMENT_3D ( 'NONE', #31804, #37109, #10568 ) ;
#48832=CARTESIAN_POINT ( 'NONE',  ( 29.50000000000000355, -12.00000000000000000, -11.03137303340310282 ) ) ;
#48833=CARTESIAN_POINT ( 'NONE',  ( 30.00000000000000000, -12.00000000000000000, 10.52786404500095863 ) ) ;
#48839=ADVANCED_FACE ( 'NONE', ( #38590 ), #50914, .T. ) ;
#48843=DIRECTION ( 'NONE',  ( 0.000000000000000000, -0.1249999999999996531, -0.9921567416492215186 ) ) ;
#48847=CARTESIAN_POINT ( 'NONE',  ( 15.50000000000000000, -1.037157890325000054, -22.50000000000000000 ) ) ;
#48848=VECTOR ( 'NONE', #58588, 1000.000000000000000 ) ;
#48854=EDGE_LOOP ( 'NONE', ( #3746, #44756, #23735, #13523, #9583, #64612, #5623, #13274, #24257, #69597, #14829, #65199, #31065, #33322 ) ) ;
#48857=ORIENTED_EDGE ( 'NONE', *, *, #19864, .F. ) ;
#48860=CARTESIAN_POINT ( 'NONE',  ( -24.00000000000000000, -15.50000000000000000, 14.50000000000000000 ) ) ;
#48873=ADVANCED_FACE ( 'NONE', ( #17707 ), #54849, .F. ) ;
#48878=VECTOR ( 'NONE', #36132, 1000.000000000000000 ) ;
#48881=DIRECTION ( 'NONE',  ( -0.000000000000000000, 1.000000000000000000, -0.000000000000000000 ) ) ;
#48883=ORIENTED_EDGE ( 'NONE', *, *, #19868, .F. ) ;
#48887=ADVANCED_FACE ( 'NONE', ( #67178 ), #39269, .F. ) ;
#48894=FACE_OUTER_BOUND ( 'NONE', #41474, .T. ) ;
#48903=CARTESIAN_POINT ( 'NONE',  ( 15.50000000000000000, -0.4000000000000000222, -19.00000000000000355 ) ) ;
#48906=CIRCLE ( 'NONE', #3762, 4.000000000000000000 ) ;
#48922=CARTESIAN_POINT ( 'NONE',  ( -11.00000000000000000, -17.50000000000000000, -15.70500000000000007 ) ) ;
#48923=EDGE_CURVE ( 'NONE', #8038, #20570, #60825, .T. ) ;
#48924=LINE ( 'NONE', #16750, #26869 ) ;
#48929=VERTEX_POINT ( 'NONE', #65798 ) ;
#48938=CARTESIAN_POINT ( 'NONE',  ( 29.50000000000000355, -11.50000000000000000, 15.00000000000000000 ) ) ;
#48944=DIRECTION ( 'NONE',  ( 1.000000000000000000, 0.000000000000000000, 0.000000000000000000 ) ) ;
#48946=AXIS2_PLACEMENT_3D ( 'NONE', #48711, #16183, #27835 ) ;
#48963=ORIENTED_EDGE ( 'NONE', *, *, #20696, .F. ) ;
#48965=EDGE_CURVE ( 'NONE', #29553, #30907, #6798, .T. ) ;
#48967=DIRECTION ( 'NONE',  ( 0.000000000000000000, 0.000000000000000000, -1.000000000000000000 ) ) ;
#48970=EDGE_CURVE ( 'NONE', #36267, #39887, #51837, .T. ) ;
#48977=AXIS2_PLACEMENT_3D ( 'NONE', #62752, #14330, #9004 ) ;
#48983=AXIS2_PLACEMENT_3D ( 'NONE', #11374, #32611, #21991 ) ;
#48999=EDGE_CURVE ( 'NONE', #17134, #24869, #30407, .T. ) ;
#49000=CARTESIAN_POINT ( 'NONE',  ( 30.00000000000000000, -10.85999999999999943, -9.000000000000001776 ) ) ;
#49006=CARTESIAN_POINT ( 'NONE',  ( 29.50000000000000355, -11.50000000000100009, 15.00000000000084910 ) ) ;
#49016=LINE ( 'NONE', #38739, #54976 ) ;
#49017=LINE ( 'NONE', #17172, #46596 ) ;
#49020=VECTOR ( 'NONE', #1248, 1000.000000000000000 ) ;
#49022=CARTESIAN_POINT ( 'NONE',  ( -30.00000000000000000, -12.00000000000000000, 12.20000000000000107 ) ) ;
#49026=CARTESIAN_POINT ( 'NONE',  ( 30.00000000000000000, -12.00000000000000000, 11.03137303340310282 ) ) ;
#49029=ORIENTED_EDGE ( 'NONE', *, *, #9894, .F. ) ;
#49032=ORIENTED_EDGE ( 'NONE', *, *, #8896, .F. ) ;
#49041=ORIENTED_EDGE ( 'NONE', *, *, #32518, .F. ) ;
#49043=CARTESIAN_POINT ( 'NONE',  ( -11.00000000000000000, -12.00000000000000000, 10.52786404500095863 ) ) ;
#49048=ORIENTED_EDGE ( 'NONE', *, *, #16984, .T. ) ;
#49064=ORIENTED_EDGE ( 'NONE', *, *, #21427, .T. ) ;
#49081=VERTEX_POINT ( 'NONE', #3543 ) ;
#49087=DIRECTION ( 'NONE',  ( -0.9583148474998867128, 0.000000000000000000, 0.2857142857143631365 ) ) ;
#49094=DIRECTION ( 'NONE',  ( -1.000000000000000000, 0.000000000000000000, 0.000000000000000000 ) ) ;
#49106=B_SPLINE_CURVE_WITH_KNOTS ( 'NONE', 3,
 ( #9299, #12913, #67387, #67021, #1616, #2324 ),
 .UNSPECIFIED., .F., .F.,
 ( 4, 2, 4 ),
 ( 1.820537833122031213, 2.555393473688635453, 3.290249114255239693 ),
 .UNSPECIFIED. ) ;
#49112=AXIS2_PLACEMENT_3D ( 'NONE', #37817, #17273, #5983 ) ;
#49113=LINE ( 'NONE', #33537, #55864 ) ;
#49120=ORIENTED_EDGE ( 'NONE', *, *, #1072, .F. ) ;
#49131=CARTESIAN_POINT ( 'NONE',  ( -29.25000000000000000, -5.200000000000001066, -11.75000000000000000 ) ) ;
#49136=CARTESIAN_POINT ( 'NONE',  ( 15.50000000000000000, 0.000000000000000000, -22.50000000000000000 ) ) ;
#49137=ADVANCED_FACE ( 'NONE', ( #24399 ), #67545, .F. ) ;
#49140=EDGE_CURVE ( 'NONE', #28197, #68445, #17569, .T. ) ;
#49141=EDGE_CURVE ( 'NONE', #8140, #47285, #60710, .T. ) ;
#49144=EDGE_CURVE ( 'NONE', #31847, #47032, #2695, .T. ) ;
#49149=CARTESIAN_POINT ( 'NONE',  ( 29.50000000000000355, -12.00000000000000000, 11.03137303340310282 ) ) ;
#49152=DIRECTION ( 'NONE',  ( 0.000000000000000000, 1.000000000000000000, 0.000000000000000000 ) ) ;
#49156=ORIENTED_EDGE ( 'NONE', *, *, #44484, .F. ) ;
#49159=DIRECTION ( 'NONE',  ( -0.4998444328988824181, 0.000000000000000000, 0.8661152018640445593 ) ) ;
#49166=CARTESIAN_POINT ( 'NONE',  ( 30.00000000000000000, -12.00000000000000000, -12.20000000000000107 ) ) ;
#49168=AXIS2_PLACEMENT_3D ( 'NONE', #64528, #4085, #63475 ) ;
#49169=DIRECTION ( 'NONE',  ( 1.000000000000000000, -0.000000000000000000, -0.000000000000000000 ) ) ;
#49170=DIRECTION ( 'NONE',  ( 0.000000000000000000, 0.000000000000000000, 1.000000000000000000 ) ) ;
#49185=ORIENTED_EDGE ( 'NONE', *, *, #38202, .T. ) ;
#49187=DIRECTION ( 'NONE',  ( 0.000000000000000000, 0.000000000000000000, -1.000000000000000000 ) ) ;
#49196=CARTESIAN_POINT ( 'NONE',  ( 30.00000000000000000, -11.50000000000100009, 15.00000000000084910 ) ) ;
#49208=DIRECTION ( 'NONE',  ( 0.000000000000000000, 0.000000000000000000, 1.000000000000000000 ) ) ;
#49210=ORIENTED_EDGE ( 'NONE', *, *, #5404, .T. ) ;
#49213=ADVANCED_FACE ( 'NONE', ( #13312 ), #44429, .T. ) ;
#49224=CIRCLE ( 'NONE', #58250, 0.3499999999999611200 ) ;
#49237=CARTESIAN_POINT ( 'NONE',  ( 30.00000000000000000, -4.000000000000000000, 26.25000000000000000 ) ) ;
#49238=ADVANCED_FACE ( 'NONE', ( #29211 ), #24785, .T. ) ;
#49241=DIRECTION ( 'NONE',  ( 0.000000000000000000, 0.000000000000000000, 1.000000000000000000 ) ) ;
#49243=ORIENTED_EDGE ( 'NONE', *, *, #16860, .T. ) ;
#49254=ORIENTED_EDGE ( 'NONE', *, *, #23866, .F. ) ;
#49263=AXIS2_PLACEMENT_3D ( 'NONE', #47206, #21720, #28067 ) ;
#49284=FACE_OUTER_BOUND ( 'NONE', #32758, .T. ) ;
#49289=CYLINDRICAL_SURFACE ( 'NONE', #24833, 4.500000000000188294 ) ;
#49304=EDGE_LOOP ( 'NONE', ( #20026, #41315 ) ) ;
#49305=EDGE_CURVE ( 'NONE', #17555, #46800, #69162, .T. ) ;
#49308=CARTESIAN_POINT ( 'NONE',  ( -11.00000000000000000, -11.50000000000100009, -15.00000000000084910 ) ) ;
#49310=VECTOR ( 'NONE', #2894, 1000.000000000000000 ) ;
#49327=VERTEX_POINT ( 'NONE', #35939 ) ;
#49347=DIRECTION ( 'NONE',  ( 1.000000000000000000, 0.000000000000000000, 0.000000000000000000 ) ) ;
#49349=LINE ( 'NONE', #44020, #24173 ) ;
#49372=VERTEX_POINT ( 'NONE', #28710 ) ;
#49378=DIRECTION ( 'NONE',  ( 0.000000000000000000, 1.000000000000000000, 0.000000000000000000 ) ) ;
#49379=ORIENTED_EDGE ( 'NONE', *, *, #36245, .T. ) ;
#49400=FACE_OUTER_BOUND ( 'NONE', #27380, .T. ) ;
#49403=ORIENTED_EDGE ( 'NONE', *, *, #26635, .T. ) ;
#49411=AXIS2_PLACEMENT_3D ( 'NONE', #57349, #60649, #8548 ) ;
#49422=EDGE_LOOP ( 'NONE', ( #3416, #55392 ) ) ;
#49430=ADVANCED_FACE ( 'NONE', ( #5166 ), #62014, .F. ) ;
#49436=CARTESIAN_POINT ( 'NONE',  ( 30.00000000000000000, -12.00000000000000000, -11.00000000000000000 ) ) ;
#49438=CARTESIAN_POINT ( 'NONE',  ( -16.33565937784310762, -0.3156604612129118026, 21.53909249377453250 ) ) ;
#49447=ADVANCED_FACE ( 'NONE', ( #33672 ), #64217, .T. ) ;
#49452=ORIENTED_EDGE ( 'NONE', *, *, #66413, .F. ) ;
#49453=DIRECTION ( 'NONE',  ( -1.000000000000000000, 0.000000000000000000, 0.000000000000000000 ) ) ;
#49460=DIRECTION ( 'NONE',  ( 1.000000000000000000, -0.000000000000000000, -0.000000000000000000 ) ) ;
#49466=FACE_OUTER_BOUND ( 'NONE', #21358, .T. ) ;
#49467=AXIS2_PLACEMENT_3D ( 'NONE', #52273, #35279, #35640 ) ;
#49477=LINE ( 'NONE', #38847, #47097 ) ;
#49481=ADVANCED_FACE ( 'NONE', ( #1491 ), #16115, .F. ) ;
#49493=VECTOR ( 'NONE', #60134, 1000.000000000000000 ) ;
#49496=DIRECTION ( 'NONE',  ( 0.000000000000000000, 1.000000000000000000, 0.000000000000000000 ) ) ;
#49499=LINE ( 'NONE', #44174, #13887 ) ;
#49501=LINE ( 'NONE', #44515, #36166 ) ;
#49530=DIRECTION ( 'NONE',  ( -1.000000000000000000, 0.000000000000000000, 0.000000000000000000 ) ) ;
#49533=DIRECTION ( 'NONE',  ( 0.000000000000000000, 0.000000000000000000, -1.000000000000000000 ) ) ;
#49536=CARTESIAN_POINT ( 'NONE',  ( 11.00000000000000000, -9.454754784057099570, 17.53999999999999915 ) ) ;
#49539=VERTEX_POINT ( 'NONE', #14655 ) ;
#49545=CIRCLE ( 'NONE', #38306, 3.499999999999999556 ) ;
#49548=ORIENTED_EDGE ( 'NONE', *, *, #29051, .T. ) ;
#49549=VERTEX_POINT ( 'NONE', #8991 ) ;
#49555=PLANE ( 'NONE',  #58005 ) ;
#49568=CYLINDRICAL_SURFACE ( 'NONE', #54714, 0.3499999999999302558 ) ;
#49574=CIRCLE ( 'NONE', #56378, 0.3499999999999308664 ) ;
#49583=ORIENTED_EDGE ( 'NONE', *, *, #2151, .F. ) ;
#49589=FACE_OUTER_BOUND ( 'NONE', #3943, .T. ) ;
#49591=LINE ( 'NONE', #59522, #2391 ) ;
#49596=ORIENTED_EDGE ( 'NONE', *, *, #60366, .T. ) ;
#49601=DIRECTION ( 'NONE',  ( 1.000000000000000000, 0.000000000000000000, 0.000000000000000000 ) ) ;
#49622=DIRECTION ( 'NONE',  ( 0.000000000000000000, 1.000000000000000000, 0.000000000000000000 ) ) ;
#49624=CARTESIAN_POINT ( 'NONE',  ( -11.00000000000000000, -15.46862696659690073, 14.50000000000000000 ) ) ;
#49630=DIRECTION ( 'NONE',  ( 0.000000000000000000, 0.5000000000000199840, 0.8660254037844271613 ) ) ;
#49631=ORIENTED_EDGE ( 'NONE', *, *, #17855, .T. ) ;
#49635=ORIENTED_EDGE ( 'NONE', *, *, #69876, .T. ) ;
#49645=EDGE_CURVE ( 'NONE', #64214, #58583, #36566, .T. ) ;
#49647=ORIENTED_EDGE ( 'NONE', *, *, #44147, .T. ) ;
#49654=EDGE_CURVE ( 'NONE', #17772, #62784, #20650, .T. ) ;
#49655=ORIENTED_EDGE ( 'NONE', *, *, #64102, .F. ) ;
#49659=CARTESIAN_POINT ( 'NONE',  ( -30.00000000000000000, -11.50000000000000000, -15.00000000000000000 ) ) ;
#49661=CARTESIAN_POINT ( 'NONE',  ( -11.00000000000000000, -15.97213595500069871, -14.50000000000000000 ) ) ;
#49682=VECTOR ( 'NONE', #14363, 1000.000000000000000 ) ;
#49694=CARTESIAN_POINT ( 'NONE',  ( -30.00000000000000000, -14.33999999999999986, 14.50000000000000000 ) ) ;
#49697=EDGE_LOOP ( 'NONE', ( #32286, #54449, #6377, #58117 ) ) ;
#49704=CARTESIAN_POINT ( 'NONE',  ( 17.00000000000000000, -17.35230188589299871, 15.35019951917099945 ) ) ;
#49712=AXIS2_PLACEMENT_3D ( 'NONE', #6411, #7776, #13077 ) ;
#49722=VERTEX_POINT ( 'NONE', #39264 ) ;
#49725=LINE ( 'NONE', #22519, #37665 ) ;
#49729=VECTOR ( 'NONE', #45917, 1000.000000000000000 ) ;
#49732=EDGE_CURVE ( 'NONE', #20510, #2132, #65794, .T. ) ;
#49733=LINE ( 'NONE', #42694, #13158 ) ;
#49736=EDGE_CURVE ( 'NONE', #18504, #58887, #30481, .T. ) ;
#49745=VERTEX_POINT ( 'NONE', #49536 ) ;
#49747=VECTOR ( 'NONE', #40709, 1000.000000000000000 ) ;
#49748=CARTESIAN_POINT ( 'NONE',  ( -25.50000000000000355, -15.50000000000000000, -22.50000000000000000 ) ) ;
#49750=ORIENTED_EDGE ( 'NONE', *, *, #41238, .T. ) ;
#49760=DIRECTION ( 'NONE',  ( -1.000000000000000000, 0.000000000000000000, 0.000000000000000000 ) ) ;
#49761=LINE ( 'NONE', #7303, #44396 ) ;
#49767=DIRECTION ( 'NONE',  ( 0.000000000000000000, 0.000000000000000000, -1.000000000000000000 ) ) ;
#49769=DIRECTION ( 'NONE',  ( 0.000000000000000000, 1.000000000000000000, 0.000000000000000000 ) ) ;
#49774=LINE ( 'NONE', #50805, #26521 ) ;
#49778=AXIS2_PLACEMENT_3D ( 'NONE', #9852, #64982, #60704 ) ;
#49780=EDGE_CURVE ( 'NONE', #9391, #37986, #7427, .T. ) ;
#49783=ORIENTED_EDGE ( 'NONE', *, *, #56287, .T. ) ;
#49791=CARTESIAN_POINT ( 'NONE',  ( 11.50000000000000000, -15.97213595500069871, -14.50000000000000000 ) ) ;
#49795=ORIENTED_EDGE ( 'NONE', *, *, #43277, .F. ) ;
#49803=CARTESIAN_POINT ( 'NONE',  ( -28.00000000000000000, -15.50000000000000000, -14.50000000000000000 ) ) ;
#49825=ADVANCED_FACE ( 'NONE', ( #40305 ), #19437, .F. ) ;
#49830=LINE ( 'NONE', #33902, #22415 ) ;
#49833=ORIENTED_EDGE ( 'NONE', *, *, #28311, .T. ) ;
#49836=CARTESIAN_POINT ( 'NONE',  ( 11.00000000000000000, -11.10796162543699950, 9.102987789146602893 ) ) ;
#49838=LINE ( 'NONE', #38212, #39858 ) ;
#49839=CARTESIAN_POINT ( 'NONE',  ( 30.00000000000000000, -11.50000000000082068, 10.20500000000000007 ) ) ;
#49843=CARTESIAN_POINT ( 'NONE',  ( 30.00000000000000000, -14.33999999999999986, -14.50000000000000000 ) ) ;
#49844=DIRECTION ( 'NONE',  ( 1.000000000000000000, 0.000000000000000000, 0.000000000000000000 ) ) ;
#49851=DIRECTION ( 'NONE',  ( 0.000000000000000000, -1.000000000000000000, 0.000000000000000000 ) ) ;
#49857=ORIENTED_EDGE ( 'NONE', *, *, #18125, .T. ) ;
#49866=EDGE_CURVE ( 'NONE', #62137, #62471, #46308, .T. ) ;
#49878=ORIENTED_EDGE ( 'NONE', *, *, #24602, .T. ) ;
#49888=ORIENTED_EDGE ( 'NONE', *, *, #61714, .F. ) ;
#49893=CYLINDRICAL_SURFACE ( 'NONE', #47330, 0.3500000000002719824 ) ;
#49910=DIRECTION ( 'NONE',  ( 0.000000000000000000, 0.000000000000000000, 1.000000000000000000 ) ) ;
#49916=DIRECTION ( 'NONE',  ( -1.000000000000000000, 0.000000000000000000, 0.000000000000000000 ) ) ;
#49918=VERTEX_POINT ( 'NONE', #62220 ) ;
#49929=CARTESIAN_POINT ( 'NONE',  ( 30.00000000000000000, -16.64230188589299786, -14.64519951917100116 ) ) ;
#49935=ORIENTED_EDGE ( 'NONE', *, *, #67714, .F. ) ;
#49938=VERTEX_POINT ( 'NONE', #30758 ) ;
#49943=LINE ( 'NONE', #23074, #51789 ) ;
#49944=ORIENTED_EDGE ( 'NONE', *, *, #1840, .T. ) ;
#49945=ADVANCED_FACE ( 'NONE', ( #2473 ), #67723, .F. ) ;
#49949=CONICAL_SURFACE ( 'NONE', #25136, 2.000000000000001776, 0.7853981633974503884 ) ;
#49958=CARTESIAN_POINT ( 'NONE',  ( 13.00000000000000178, -16.28999999999710369, 14.50000000000000000 ) ) ;
#49960=DIRECTION ( 'NONE',  ( -1.000000000000000000, 0.000000000000000000, 0.000000000000000000 ) ) ;
#49974=CARTESIAN_POINT ( 'NONE',  ( 25.50000000000000355, -15.50000000000000000, 24.50000000000000000 ) ) ;
#49975=CARTESIAN_POINT ( 'NONE',  ( -14.25000000000000000, -2.500000000000000000, 23.22168783648699986 ) ) ;
#49984=EDGE_CURVE ( 'NONE', #3700, #44054, #21449, .T. ) ;
#49991=VECTOR ( 'NONE', #42437, 1000.000000000000000 ) ;
#49992=LINE ( 'NONE', #24530, #48622 ) ;
#49994=EDGE_CURVE ( 'NONE', #46156, #68853, #39493, .T. ) ;
#49999=CARTESIAN_POINT ( 'NONE',  ( 24.00000000000000000, -16.28999999999710369, -15.00000000000794920 ) ) ;
#50000=ADVANCED_FACE ( 'NONE', ( #36401 ), #26159, .F. ) ;
#50004=DIRECTION ( 'NONE',  ( 1.000000000000000000, -0.000000000000000000, -0.000000000000000000 ) ) ;
#50005=AXIS2_PLACEMENT_3D ( 'NONE', #36882, #26259, #21651 ) ;
#50009=ORIENTED_EDGE ( 'NONE', *, *, #30479, .F. ) ;
#50014=AXIS2_PLACEMENT_3D ( 'NONE', #7666, #49769, #6633 ) ;
#50018=AXIS2_PLACEMENT_3D ( 'NONE', #8077, #19052, #34948 ) ;
#50022=DIRECTION ( 'NONE',  ( 0.000000000000000000, -1.000000000000000000, 0.000000000000000000 ) ) ;
#50025=AXIS2_PLACEMENT_3D ( 'NONE', #25984, #26323, #30237 ) ;
#50026=EDGE_CURVE ( 'NONE', #67811, #5431, #47361, .T. ) ;
#50028=DIRECTION ( 'NONE',  ( 0.000000000000000000, 0.000000000000000000, 1.000000000000000000 ) ) ;
#50033=LINE ( 'NONE', #1589, #2911 ) ;
#50036=DIRECTION ( 'NONE',  ( 0.000000000000000000, 1.000000000000000000, 0.000000000000000000 ) ) ;
#50042=CARTESIAN_POINT ( 'NONE',  ( 30.00000000000000000, -14.04000000000000092, -17.04524521594300523 ) ) ;
#50044=CARTESIAN_POINT ( 'NONE',  ( 23.75054448485400016, -15.50000000000000000, -25.53140320652400064 ) ) ;
#50053=ADVANCED_FACE ( 'NONE', ( #36770 ), #4934, .T. ) ;
#50056=VECTOR ( 'NONE', #68229, 1000.000000000000000 ) ;
#50060=ORIENTED_EDGE ( 'NONE', *, *, #64966, .T. ) ;
#50061=EDGE_CURVE ( 'NONE', #62351, #44232, #58681, .T. ) ;
#50067=VERTEX_POINT ( 'NONE', #26859 ) ;
#50072=CYLINDRICAL_SURFACE ( 'NONE', #23463, 3.499999999999850342 ) ;
#50075=VERTEX_POINT ( 'NONE', #65713 ) ;
#50078=LINE ( 'NONE', #5573, #33855 ) ;
#50079=ORIENTED_EDGE ( 'NONE', *, *, #63821, .F. ) ;
#50081=ORIENTED_EDGE ( 'NONE', *, *, #69354, .T. ) ;
#50085=DIRECTION ( 'NONE',  ( 1.000000000000000000, -0.000000000000000000, -0.000000000000000000 ) ) ;
#50086=VERTEX_POINT ( 'NONE', #49791 ) ;
#50088=PLANE ( 'NONE',  #32267 ) ;
#50095=DIRECTION ( 'NONE',  ( 0.000000000000000000, -1.000000000000000000, 0.000000000000000000 ) ) ;
#50116=CYLINDRICAL_SURFACE ( 'NONE', #14085, 2.250000000000001776 ) ;
#50117=EDGE_CURVE ( 'NONE', #14877, #67332, #1356, .T. ) ;
#50127=ORIENTED_EDGE ( 'NONE', *, *, #31127, .F. ) ;
#50134=ORIENTED_EDGE ( 'NONE', *, *, #2989, .F. ) ;
#50137=LINE ( 'NONE', #34906, #65000 ) ;
#50145=ORIENTED_EDGE ( 'NONE', *, *, #10332, .T. ) ;
#50147=CARTESIAN_POINT ( 'NONE',  ( 30.00000000000000000, -5.599999999999999645, -27.00000000000000000 ) ) ;
#50148=VERTEX_POINT ( 'NONE', #1025 ) ;
#50152=AXIS2_PLACEMENT_3D ( 'NONE', #69973, #5964, #55103 ) ;
#50161=ORIENTED_EDGE ( 'NONE', *, *, #8079, .F. ) ;
#50172=CARTESIAN_POINT ( 'NONE',  ( -15.50000000000000000, 998.9628421096749662, 22.50000000000000000 ) ) ;
#50177=CARTESIAN_POINT ( 'NONE',  ( 30.00000000000000000, -17.00000000000000000, 15.70499999999969809 ) ) ;
#50178=ORIENTED_EDGE ( 'NONE', *, *, #69090, .F. ) ;
#50180=CARTESIAN_POINT ( 'NONE',  ( -23.48000000000000043, -15.50000000000000000, 26.00000000000000355 ) ) ;
#50184=DIRECTION ( 'NONE',  ( 0.000000000000000000, -0.7046037717859411353, -0.7096009616573427659 ) ) ;
#50186=LINE ( 'NONE', #23321, #57774 ) ;
#50192=AXIS2_PLACEMENT_3D ( 'NONE', #57186, #68142, #58236 ) ;
#50200=EDGE_CURVE ( 'NONE', #67430, #43499, #54270, .T. ) ;
#50213=FACE_OUTER_BOUND ( 'NONE', #52900, .T. ) ;
#50217=CARTESIAN_POINT ( 'NONE',  ( 11.00000000000000000, -12.00000000000000000, 11.03137303340310282 ) ) ;
#50231=LINE ( 'NONE', #18384, #62981 ) ;
#50233=DIRECTION ( 'NONE',  ( 0.000000000000000000, 0.000000000000000000, 1.000000000000000000 ) ) ;
#50235=VERTEX_POINT ( 'NONE', #56144 ) ;
#50241=CARTESIAN_POINT ( 'NONE',  ( 30.00000000000000000, -11.10796162543699950, -9.102987789146602893 ) ) ;
#50246=FACE_OUTER_BOUND ( 'NONE', #20435, .T. ) ;
#50247=VERTEX_POINT ( 'NONE', #62126 ) ;
#50249=VERTEX_POINT ( 'NONE', #45515 ) ;
#50264=EDGE_CURVE ( 'NONE', #11691, #23447, #37312, .T. ) ;
#50269=DIRECTION ( 'NONE',  ( 0.000000000000000000, -0.7084617869615144059, 0.7057491738679528837 ) ) ;
#50272=CARTESIAN_POINT ( 'NONE',  ( 22.14589803375000088, -17.50000000000000000, 21.50000000000000000 ) ) ;
#50274=AXIS2_PLACEMENT_3D ( 'NONE', #19661, #9069, #30985 ) ;
#50284=CARTESIAN_POINT ( 'NONE',  ( -15.50000000000000000, -0.2038245569916614930, -21.05662432702600029 ) ) ;
#50285=CARTESIAN_POINT ( 'NONE',  ( 30.00000000000000000, -14.04000000000000092, -17.04524521594300523 ) ) ;
#50288=DIRECTION ( 'NONE',  ( 0.000000000000000000, 0.000000000000000000, -1.000000000000000000 ) ) ;
#50304=DIRECTION ( 'NONE',  ( -0.8660254037850496633, 0.000000000000000000, -0.4999999999989417909 ) ) ;
#50308=VERTEX_POINT ( 'NONE', #39854 ) ;
#50311=FACE_OUTER_BOUND ( 'NONE', #52357, .T. ) ;
#50316=VECTOR ( 'NONE', #1314, 1000.000000000000000 ) ;
#50323=DIRECTION ( 'NONE',  ( -1.000000000000000000, 0.000000000000000000, 0.000000000000000000 ) ) ;
#50330=ORIENTED_EDGE ( 'NONE', *, *, #18671, .F. ) ;
#50331=EDGE_LOOP ( 'NONE', ( #11447, #11255, #52993, #32344 ) ) ;
#50334=CARTESIAN_POINT ( 'NONE',  ( -13.00000000000000178, -15.50000000000000000, 14.50000000000000000 ) ) ;
#50339=ADVANCED_FACE ( 'NONE', ( #67455 ), #8380, .T. ) ;
#50340=ADVANCED_FACE ( 'NONE', ( #24308 ), #3101, .F. ) ;
#50348=ORIENTED_EDGE ( 'NONE', *, *, #60245, .F. ) ;
#50349=CIRCLE ( 'NONE', #15394, 0.5000000000001357803 ) ;
#50359=DIRECTION ( 'NONE',  ( 0.9583148474998870459, 0.000000000000000000, -0.2857142857143623593 ) ) ;
#50360=EDGE_LOOP ( 'NONE', ( #4949, #23618, #41747, #47401 ) ) ;
#50366=CARTESIAN_POINT ( 'NONE',  ( -15.50000000000000000, -2.500000000000000000, 23.94337567297399971 ) ) ;
#50375=FACE_OUTER_BOUND ( 'NONE', #43652, .T. ) ;
#50384=ADVANCED_FACE ( 'NONE', ( #25364 ), #63551, .T. ) ;
#50385=ORIENTED_EDGE ( 'NONE', *, *, #15445, .T. ) ;
#50398=DIRECTION ( 'NONE',  ( 0.000000000000000000, 0.000000000000000000, -1.000000000000000000 ) ) ;
#50399=ADVANCED_FACE ( 'NONE', ( #58937 ), #3794, .F. ) ;
#50414=ORIENTED_EDGE ( 'NONE', *, *, #5649, .T. ) ;
#50423=ORIENTED_EDGE ( 'NONE', *, *, #61405, .F. ) ;
#50432=ORIENTED_EDGE ( 'NONE', *, *, #6477, .F. ) ;
#50438=VERTEX_POINT ( 'NONE', #21452 ) ;
#50441=AXIS2_PLACEMENT_3D ( 'NONE', #69003, #24821, #41074 ) ;
#50451=DIRECTION ( 'NONE',  ( 0.000000000000000000, 0.000000000000000000, -1.000000000000000000 ) ) ;
#50454=CARTESIAN_POINT ( 'NONE',  ( -25.50000000000000355, 0.000000000000000000, -22.50000000000000000 ) ) ;
#50456=EDGE_CURVE ( 'NONE', #39125, #60969, #20752, .T. ) ;
#50464=EDGE_CURVE ( 'NONE', #11065, #47223, #115, .T. ) ;
#50465=VECTOR ( 'NONE', #5590, 1000.000000000000000 ) ;
#50466=CARTESIAN_POINT ( 'NONE',  ( -29.50000000000000355, -11.50000000000000000, -15.00000000000000000 ) ) ;
#50469=DIRECTION ( 'NONE',  ( -1.000000000000000000, 0.000000000000000000, 0.000000000000000000 ) ) ;
#50475=DIRECTION ( 'NONE',  ( 0.4998444328988824181, 0.000000000000000000, -0.8661152018640445593 ) ) ;
#50482=CARTESIAN_POINT ( 'NONE',  ( -30.00000000000000000, -12.00000000000000000, 10.20500000000000007 ) ) ;
#50486=VERTEX_POINT ( 'NONE', #58597 ) ;
#50487=EDGE_CURVE ( 'NONE', #33635, #39125, #5544, .T. ) ;
#50491=AXIS2_PLACEMENT_3D ( 'NONE', #53368, #4922, #69631 ) ;
#50493=LINE ( 'NONE', #7342, #69848 ) ;
#50500=ORIENTED_EDGE ( 'NONE', *, *, #22, .F. ) ;
#50509=CYLINDRICAL_SURFACE ( 'NONE', #10711, 4.500000000000188294 ) ;
#50511=ORIENTED_EDGE ( 'NONE', *, *, #32391, .F. ) ;
#50518=EDGE_LOOP ( 'NONE', ( #29438, #36135, #4343, #64973 ) ) ;
#50545=CARTESIAN_POINT ( 'NONE',  ( -25.50000000000000355, -15.12100000000000044, -22.50000000000000000 ) ) ;
#50550=CARTESIAN_POINT ( 'NONE',  ( 15.50000000000000000, -15.50000000000000000, 22.50000000000000000 ) ) ;
#50551=EDGE_CURVE ( 'NONE', #23827, #62386, #17180, .T. ) ;
#50555=VERTEX_POINT ( 'NONE', #28142 ) ;
#50557=CARTESIAN_POINT ( 'NONE',  ( 30.00000000000000000, -9.200000000000120082, 17.30000000000000071 ) ) ;
#50560=VECTOR ( 'NONE', #69737, 1000.000000000000000 ) ;
#50564=LINE ( 'NONE', #18360, #59495 ) ;
#50573=CARTESIAN_POINT ( 'NONE',  ( 11.00000000000000000, -11.50000000000000000, -15.00000000000000000 ) ) ;
#50582=DIRECTION ( 'NONE',  ( 0.000000000000000000, 1.000000000000000000, 0.000000000000000000 ) ) ;
#50583=ORIENTED_EDGE ( 'NONE', *, *, #65791, .F. ) ;
#50585=CARTESIAN_POINT ( 'NONE',  ( 30.00000000000000000, -11.70000000000000284, 12.50000000000000000 ) ) ;
#50590=VERTEX_POINT ( 'NONE', #33451 ) ;
#50592=VERTEX_POINT ( 'NONE', #55039 ) ;
#50596=AXIS2_PLACEMENT_3D ( 'NONE', #406, #21967, #43876 ) ;
#50600=ORIENTED_EDGE ( 'NONE', *, *, #12040, .T. ) ;
#50602=ORIENTED_EDGE ( 'NONE', *, *, #17065, .F. ) ;
#50603=EDGE_LOOP ( 'NONE', ( #68873, #37364, #16031, #19367, #19340, #53744 ) ) ;
#50606=VECTOR ( 'NONE', #14502, 1000.000000000000000 ) ;
#50612=CIRCLE ( 'NONE', #29154, 0.5000000000079367624 ) ;
#50627=ORIENTED_EDGE ( 'NONE', *, *, #66432, .F. ) ;
#50637=CARTESIAN_POINT ( 'NONE',  ( -16.75000000000000000, -2.500000000000000000, 23.22168783648699986 ) ) ;
#50639=DIRECTION ( 'NONE',  ( 0.000000000000000000, 1.000000000000000000, 0.000000000000000000 ) ) ;
#50642=CARTESIAN_POINT ( 'NONE',  ( -30.00000000000000000, -10.85999999999999943, -9.350000000000269651 ) ) ;
#50643=DIRECTION ( 'NONE',  ( 0.000000000000000000, 1.000000000000000000, 0.000000000000000000 ) ) ;
#50647=AXIS2_PLACEMENT_3D ( 'NONE', #46574, #42326, #19696 ) ;
#50656=CARTESIAN_POINT ( 'NONE',  ( 25.50000000000000355, -5.578999999999999737, -20.87899999999999778 ) ) ;
#50660=DIRECTION ( 'NONE',  ( 0.000000000000000000, 1.000000000000000000, 0.000000000000000000 ) ) ;
#50666=ORIENTED_EDGE ( 'NONE', *, *, #38430, .T. ) ;
#50695=EDGE_CURVE ( 'NONE', #26381, #28340, #39437, .T. ) ;
#50707=CARTESIAN_POINT ( 'NONE',  ( 25.50000000000000355, -5.578999999999999737, 20.87900000000000134 ) ) ;
#50710=FACE_OUTER_BOUND ( 'NONE', #22690, .T. ) ;
#50711=ORIENTED_EDGE ( 'NONE', *, *, #23519, .F. ) ;
#50716=DIRECTION ( 'NONE',  ( 0.000000000000000000, -0.7084617869615144059, 0.7057491738679528837 ) ) ;
#50719=VECTOR ( 'NONE', #65770, 1000.000000000000000 ) ;
#50723=( NAMED_UNIT ( * ) PLANE_ANGLE_UNIT ( ) SI_UNIT ( $, .RADIAN. ) );
#50728=CARTESIAN_POINT ( 'NONE',  ( 15.50000000000000000, -0.1999999999999999556, -21.05000000000000426 ) ) ;
#50735=ORIENTED_EDGE ( 'NONE', *, *, #67381, .F. ) ;
#50739=ADVANCED_FACE ( 'NONE', ( #30243 ), #51802, .F. ) ;
#50753=AXIS2_PLACEMENT_3D ( 'NONE', #31117, #21537, #68592 ) ;
#50756=ORIENTED_EDGE ( 'NONE', *, *, #53998, .F. ) ;
#50759=AXIS2_PLACEMENT_3D ( 'NONE', #42576, #58143, #25268 ) ;
#50760=FACE_OUTER_BOUND ( 'NONE', #20769, .T. ) ;
#50764=FACE_OUTER_BOUND ( 'NONE', #43542, .T. ) ;
#50768=VERTEX_POINT ( 'NONE', #56398 ) ;
#50777=EDGE_CURVE ( 'NONE', #14914, #35164, #3020, .T. ) ;
#50778=CIRCLE ( 'NONE', #29325, 0.3499999999999295341 ) ;
#50783=CARTESIAN_POINT ( 'NONE',  ( -11.00000000000000000, -11.50000000000100009, 15.00000000000084910 ) ) ;
#50788=AXIS2_PLACEMENT_3D ( 'NONE', #10511, #16169, #258 ) ;
#50791=DIRECTION ( 'NONE',  ( 0.000000000000000000, 1.000000000000000000, 0.000000000000000000 ) ) ;
#50792=DIRECTION ( 'NONE',  ( 0.000000000000000000, 0.000000000000000000, 1.000000000000000000 ) ) ;
#50796=AXIS2_PLACEMENT_3D ( 'NONE', #39497, #65690, #61059 ) ;
#50797=CARTESIAN_POINT ( 'NONE',  ( 28.00000000000000000, -17.35230188589299871, -15.35019951917099945 ) ) ;
#50798=CYLINDRICAL_SURFACE ( 'NONE', #67497, 4.000000000000000000 ) ;
#50803=PLANE ( 'NONE',  #22603 ) ;
#50805=CARTESIAN_POINT ( 'NONE',  ( 29.25000000000000000, -5.000000000000000000, -11.75000000000000000 ) ) ;
#50806=VECTOR ( 'NONE', #44297, 1000.000000000000000 ) ;
#50808=PLANE ( 'NONE',  #46176 ) ;
#50814=CARTESIAN_POINT ( 'NONE',  ( 17.00000000000000000, -16.28999999999710369, -15.00000000000794920 ) ) ;
#50815=ORIENTED_EDGE ( 'NONE', *, *, #42089, .T. ) ;
#50820=CARTESIAN_POINT ( 'NONE',  ( -11.00000000000000000, -11.85423089348099879, -9.852125413066602277 ) ) ;
#50824=ORIENTED_EDGE ( 'NONE', *, *, #1829, .F. ) ;
#50825=AXIS2_PLACEMENT_3D ( 'NONE', #8949, #62694, #69055 ) ;
#50829=EDGE_CURVE ( 'NONE', #64273, #31007, #41545, .T. ) ;
#50836=AXIS2_PLACEMENT_3D ( 'NONE', #69694, #53086, #16642 ) ;
#50838=VERTEX_POINT ( 'NONE', #5116 ) ;
#50841=AXIS2_PLACEMENT_3D ( 'NONE', #13958, #13262, #24924 ) ;
#50846=LINE ( 'NONE', #45540, #25971 ) ;
#50851=VERTEX_POINT ( 'NONE', #68063 ) ;
#50858=CARTESIAN_POINT ( 'NONE',  ( 17.51999999999999957, -15.50000000000000000, 26.00000000000000355 ) ) ;
#50864=AXIS2_PLACEMENT_3D ( 'NONE', #64890, #54279, #5838 ) ;
#50870=CARTESIAN_POINT ( 'NONE',  ( 17.00000000000000000, -15.50000000000000000, -19.33772233983200195 ) ) ;
#50882=DIRECTION ( 'NONE',  ( 0.000000000000000000, 0.000000000000000000, 1.000000000000000000 ) ) ;
#50890=DIRECTION ( 'NONE',  ( 0.8660254037850496633, 0.000000000000000000, -0.4999999999989417909 ) ) ;
#50906=FACE_OUTER_BOUND ( 'NONE', #65319, .T. ) ;
#50914=CYLINDRICAL_SURFACE ( 'NONE', #49712, 0.4000000000000600298 ) ;
#50919=CIRCLE ( 'NONE', #55427, 0.4999999999991850963 ) ;
#50922=DIRECTION ( 'NONE',  ( -1.000000000000000000, 0.000000000000000000, 0.000000000000000000 ) ) ;
#50925=EDGE_LOOP ( 'NONE', ( #21989, #57731, #59832, #60679 ) ) ;
#50946=EDGE_CURVE ( 'NONE', #68170, #24393, #16074, .T. ) ;
#50948=CIRCLE ( 'NONE', #20475, 0.4999999999991850963 ) ;
#50950=CARTESIAN_POINT ( 'NONE',  ( 11.00000000000000000, -14.04000000000000092, 17.04524521594300523 ) ) ;
#50972=ORIENTED_EDGE ( 'NONE', *, *, #33146, .T. ) ;
#50977=EDGE_CURVE ( 'NONE', #12080, #61212, #28346, .T. ) ;
#50979=LINE ( 'NONE', #2532, #33505 ) ;
#50984=CARTESIAN_POINT ( 'NONE',  ( 17.00000000000000000, -15.50000000000000000, -19.33772233983200195 ) ) ;
#50988=CARTESIAN_POINT ( 'NONE',  ( -30.00000000000000000, -5.000000000000000000, -27.00000000000000000 ) ) ;
#50994=CARTESIAN_POINT ( 'NONE',  ( 30.00000000000000000, -5.599999999999999645, -9.000000000000001776 ) ) ;
#51002=ORIENTED_EDGE ( 'NONE', *, *, #33638, .T. ) ;
#51003=EDGE_CURVE ( 'NONE', #6765, #40705, #54254, .T. ) ;
#51012=LINE ( 'NONE', #61607, #62515 ) ;
#51018=VERTEX_POINT ( 'NONE', #33023 ) ;
#51025=AXIS2_PLACEMENT_3D ( 'NONE', #33266, #60472, #12019 ) ;
#51030=EDGE_LOOP ( 'NONE', ( #12892, #56498, #41841, #7882, #42157 ) ) ;
#51032=EDGE_LOOP ( 'NONE', ( #19614, #46752, #53795, #59305 ) ) ;
#51051=ORIENTED_EDGE ( 'NONE', *, *, #28069, .F. ) ;
#51058=CARTESIAN_POINT ( 'NONE',  ( -11.00000000000000000, -13.79999999999979998, 17.30000000000000071 ) ) ;
#51062=VECTOR ( 'NONE', #61007, 1000.000000000000000 ) ;
#51063=DIRECTION ( 'NONE',  ( 0.000000000000000000, -1.000000000000000000, 0.000000000000000000 ) ) ;
#51076=FILL_AREA_STYLE_COLOUR ( '', #61796 ) ;
#51078=DIRECTION ( 'NONE',  ( -1.000000000000000000, 0.000000000000000000, 0.000000000000000000 ) ) ;
#51082=DIRECTION ( 'NONE',  ( 0.000000000000000000, 0.000000000000000000, 1.000000000000000000 ) ) ;
#51088=CARTESIAN_POINT ( 'NONE',  ( -15.08757311576351334, -0.3152598339557977081, -21.29473909966096556 ) ) ;
#51091=AXIS2_PLACEMENT_3D ( 'NONE', #24221, #13609, #45783 ) ;
#51098=CIRCLE ( 'NONE', #7076, 4.000000000000000000 ) ;
#51110=VERTEX_POINT ( 'NONE', #19186 ) ;
#51111=VERTEX_POINT ( 'NONE', #45349 ) ;
#51118=ORIENTED_EDGE ( 'NONE', *, *, #37830, .T. ) ;
#51119=CARTESIAN_POINT ( 'NONE',  ( -11.00000000000000000, -9.487228132326899654, 12.50000000000000000 ) ) ;
#51130=ADVANCED_FACE ( 'NONE', ( #45697 ), #23092, .F. ) ;
#51145=DIRECTION ( 'NONE',  ( 0.000000000000000000, 1.000000000000000000, 0.000000000000000000 ) ) ;
#51149=DIRECTION ( 'NONE',  ( 0.000000000000000000, 0.000000000000000000, 1.000000000000000000 ) ) ;
#51155=CARTESIAN_POINT ( 'NONE',  ( -11.75000000000000000, -5.000000000000000000, 26.25000000000000000 ) ) ;
#51156=DIRECTION ( 'NONE',  ( 0.000000000000000000, 0.000000000000000000, 1.000000000000000000 ) ) ;
#51175=CIRCLE ( 'NONE', #370, 0.3499999999998875677 ) ;
#51177=EDGE_CURVE ( 'NONE', #66376, #17317, #24143, .T. ) ;
#51182=DIRECTION ( 'NONE',  ( 1.000000000000000000, 0.000000000000000000, 0.000000000000000000 ) ) ;
#51186=ORIENTED_EDGE ( 'NONE', *, *, #32565, .F. ) ;
#51199=ORIENTED_EDGE ( 'NONE', *, *, #26218, .F. ) ;
#51205=VERTEX_POINT ( 'NONE', #9992 ) ;
#51206=VERTEX_POINT ( 'NONE', #15645 ) ;
#51209=CARTESIAN_POINT ( 'NONE',  ( 11.50000000000000000, -11.50000000000100009, -15.00000000000084910 ) ) ;
#51216=CIRCLE ( 'NONE', #6068, 4.000000000000000888 ) ;
#51222=ADVANCED_FACE ( 'NONE', ( #3982 ), #41095, .F. ) ;
#51226=AXIS2_PLACEMENT_3D ( 'NONE', #41103, #62672, #14250 ) ;
#51228=CARTESIAN_POINT ( 'NONE',  ( 11.00000000000000000, -9.199999999999999289, -12.34999999999989839 ) ) ;
#51236=CARTESIAN_POINT ( 'NONE',  ( 11.00000000000000000, -11.50000000000000000, 15.00000000000000000 ) ) ;
#51242=LINE ( 'NONE', #23670, #60598 ) ;
#51249=DIRECTION ( 'NONE',  ( 0.4999999999999827360, 0.000000000000000000, 0.8660254037844485886 ) ) ;
#51268=ORIENTED_EDGE ( 'NONE', *, *, #1545, .F. ) ;
#51274=EDGE_CURVE ( 'NONE', #17772, #10, #62663, .T. ) ;
#51281=EDGE_CURVE ( 'NONE', #57835, #43126, #14241, .T. ) ;
#51283=ORIENTED_EDGE ( 'NONE', *, *, #45910, .F. ) ;
#51285=CARTESIAN_POINT ( 'NONE',  ( 29.50000000000000355, -12.00000000000000000, -10.52786404500095863 ) ) ;
#51292=CARTESIAN_POINT ( 'NONE',  ( -30.00000000000000000, -11.50000000000100009, -15.00000000000084910 ) ) ;
#51295=EDGE_LOOP ( 'NONE', ( #62718, #28758, #40300, #52279 ) ) ;
#51309=FACE_OUTER_BOUND ( 'NONE', #13016, .T. ) ;
#51311=ORIENTED_EDGE ( 'NONE', *, *, #55349, .T. ) ;
#51315=CARTESIAN_POINT ( 'NONE',  ( 30.00000000000000000, -14.33999999999999986, -14.50000000000000000 ) ) ;
#51319=DIRECTION ( 'NONE',  ( 0.000000000000000000, 0.000000000000000000, 1.000000000000000000 ) ) ;
#51322=CYLINDRICAL_SURFACE ( 'NONE', #65644, 4.000000000000000000 ) ;
#51328=DIRECTION ( 'NONE',  ( 1.000000000000000000, -0.000000000000000000, -0.000000000000000000 ) ) ;
#51332=VERTEX_POINT ( 'NONE', #14941 ) ;
#51342=EDGE_CURVE ( 'NONE', #50768, #46357, #39697, .T. ) ;
#51343=ORIENTED_EDGE ( 'NONE', *, *, #33259, .F. ) ;
#51348=DIRECTION ( 'NONE',  ( 0.000000000000000000, 1.000000000000000000, 0.000000000000000000 ) ) ;
#51350=AXIS2_PLACEMENT_3D ( 'NONE', #17621, #5984, #65723 ) ;
#51354=LINE ( 'NONE', #46749, #51409 ) ;
#51359=ADVANCED_FACE ( 'NONE', ( #16329, #21639 ), #425, .F. ) ;
#51362=ORIENTED_EDGE ( 'NONE', *, *, #65856, .F. ) ;
#51373=DIRECTION ( 'NONE',  ( 1.000000000000000000, -0.000000000000000000, -0.000000000000000000 ) ) ;
#51375=ADVANCED_FACE ( 'NONE', ( #5394 ), #81, .F. ) ;
#51381=DIRECTION ( 'NONE',  ( 0.000000000000000000, 0.000000000000000000, 1.000000000000000000 ) ) ;
#51386=EDGE_LOOP ( 'NONE', ( #30928, #351, #66987, #35277, #41081, #44051, #22634, #23047, #43267, #19579, #49064 ) ) ;
#51391=VERTEX_POINT ( 'NONE', #11028 ) ;
#51393=VERTEX_POINT ( 'NONE', #48511 ) ;
#51406=ORIENTED_EDGE ( 'NONE', *, *, #14716, .F. ) ;
#51407=ORIENTED_EDGE ( 'NONE', *, *, #49732, .F. ) ;
#51409=VECTOR ( 'NONE', #52063, 1000.000000000000000 ) ;
#51413=EDGE_CURVE ( 'NONE', #63027, #1158, #59119, .T. ) ;
#51417=VECTOR ( 'NONE', #2805, 1000.000000000000000 ) ;
#51420=CARTESIAN_POINT ( 'NONE',  ( 30.00000000000000000, -11.10796162543699950, -9.102987789146602893 ) ) ;
#51429=DIRECTION ( 'NONE',  ( 0.8660254037850496633, 0.000000000000000000, 0.4999999999989417909 ) ) ;
#51431=EDGE_CURVE ( 'NONE', #974, #42297, #64430, .T. ) ;
#51443=CARTESIAN_POINT ( 'NONE',  ( -15.50000000000000000, -0.4000000000005236034, -25.79999999999947136 ) ) ;
#51445=EDGE_LOOP ( 'NONE', ( #49655, #23126, #22823, #1824 ) ) ;
#51467=CARTESIAN_POINT ( 'NONE',  ( -13.00000000000000178, -16.64230188589299786, 14.64519951917100116 ) ) ;
#51472=CIRCLE ( 'NONE', #53767, 0.2999999999998732569 ) ;
#51475=CARTESIAN_POINT ( 'NONE',  ( 16.33757311576526305, -0.3152598339554795182, 21.54019739087904384 ) ) ;
#51489=CARTESIAN_POINT ( 'NONE',  ( -11.50000000000000000, -12.00000000000000000, -11.00000000000000000 ) ) ;
#51491=CARTESIAN_POINT ( 'NONE',  ( 15.50000000000000000, -2.500000000000000000, -21.05662432702600029 ) ) ;
#51497=EDGE_CURVE ( 'NONE', #701, #51774, #35979, .T. ) ;
#51508=VERTEX_POINT ( 'NONE', #14419 ) ;
#51512=VECTOR ( 'NONE', #59286, 1000.000000000000000 ) ;
#51518=CARTESIAN_POINT ( 'NONE',  ( -31.00000000000000000, -2.500000000000000000, 0.000000000000000000 ) ) ;
#51530=DIRECTION ( 'NONE',  ( 0.000000000000000000, 0.000000000000000000, 1.000000000000000000 ) ) ;
#51544=CARTESIAN_POINT ( 'NONE',  ( -23.48000000000000043, -15.50000000000000000, 26.00000000000000355 ) ) ;
#51545=CARTESIAN_POINT ( 'NONE',  ( 30.00000000000000000, 0.000000000000000000, -27.00000000000000000 ) ) ;
#51549=ORIENTED_EDGE ( 'NONE', *, *, #17237, .T. ) ;
#51551=VERTEX_POINT ( 'NONE', #7087 ) ;
#51552=EDGE_LOOP ( 'NONE', ( #16707, #63951, #48447, #52761 ) ) ;
#51553=LINE ( 'NONE', #34916, #12633 ) ;
#51554=ORIENTED_EDGE ( 'NONE', *, *, #4612, .T. ) ;
#51556=CARTESIAN_POINT ( 'NONE',  ( -17.24945551514599984, -15.50000000000000000, -25.53140320652400064 ) ) ;
#51560=ORIENTED_EDGE ( 'NONE', *, *, #46784, .F. ) ;
#51564=ORIENTED_EDGE ( 'NONE', *, *, #20225, .F. ) ;
#51567=AXIS2_PLACEMENT_3D ( 'NONE', #19897, #41467, #41104 ) ;
#51575=AXIS2_PLACEMENT_3D ( 'NONE', #46904, #68494, #41612 ) ;
#51578=CARTESIAN_POINT ( 'NONE',  ( -13.00000000000000178, -16.28999999999710369, 15.00000000000794920 ) ) ;
#51592=VECTOR ( 'NONE', #32213, 1000.000000000000000 ) ;
#51596=LINE ( 'NONE', #9505, #369 ) ;
#51600=LINE ( 'NONE', #23662, #61098 ) ;
#51606=CARTESIAN_POINT ( 'NONE',  ( -11.00000000000000000, -16.64230188589299786, -14.64519951917100116 ) ) ;
#51610=ORIENTED_EDGE ( 'NONE', *, *, #28229, .F. ) ;
#51622=B_SPLINE_CURVE_WITH_KNOTS ( 'NONE', 3,
 ( #52240, #52955, #36678, #62850, #41978, #4513 ),
 .UNSPECIFIED., .F., .F.,
 ( 4, 2, 4 ),
 ( 0.0002380763768129734448, 0.7291065797294585815, 1.457975083082104328 ),
 .UNSPECIFIED. ) ;
#51626=DIRECTION ( 'NONE',  ( 1.000000000000000000, 0.000000000000000000, 0.000000000000000000 ) ) ;
#51632=ORIENTED_EDGE ( 'NONE', *, *, #31562, .F. ) ;
#51646=VECTOR ( 'NONE', #67521, 1000.000000000000000 ) ;
#51647=FACE_OUTER_BOUND ( 'NONE', #33574, .T. ) ;
#51652=DIRECTION ( 'NONE',  ( 0.000000000000000000, 1.000000000000000000, 0.000000000000000000 ) ) ;
#51661=DIRECTION ( 'NONE',  ( 0.000000000000000000, -0.1111111111108840643, -0.9938079899999319178 ) ) ;
#51671=VECTOR ( 'NONE', #9418, 1000.000000000000000 ) ;
#51683=ORIENTED_EDGE ( 'NONE', *, *, #15531, .F. ) ;
#51686=CIRCLE ( 'NONE', #927, 1.449999999999999956 ) ;
#51687=CYLINDRICAL_SURFACE ( 'NONE', #64994, 0.5000000000079367624 ) ;
#51689=EDGE_CURVE ( 'NONE', #9560, #50838, #11484, .T. ) ;
#51691=DIRECTION ( 'NONE',  ( 0.000000000000000000, -1.000000000000000000, 0.000000000000000000 ) ) ;
#51694=ADVANCED_FACE ( 'NONE', ( #58606 ), #10851, .T. ) ;
#51695=CARTESIAN_POINT ( 'NONE',  ( 15.50000000000000000, -5.000000000000000000, 26.50000000000000000 ) ) ;
#51701=VECTOR ( 'NONE', #40890, 1000.000000000000000 ) ;
#51704=CARTESIAN_POINT ( 'NONE',  ( 28.00000000000000000, -15.50000000000000000, 20.05051025721700242 ) ) ;
#51709=CYLINDRICAL_SURFACE ( 'NONE', #7942, 0.5000000000001357803 ) ;
#51713=ORIENTED_EDGE ( 'NONE', *, *, #25297, .F. ) ;
#51714=CARTESIAN_POINT ( 'NONE',  ( 28.00000000000000000, -17.00000000000000000, 15.70499999999969809 ) ) ;
#51719=FACE_OUTER_BOUND ( 'NONE', #58142, .T. ) ;
#51736=EDGE_CURVE ( 'NONE', #50249, #24514, #15120, .T. ) ;
#51753=DIRECTION ( 'NONE',  ( -1.000000000000000000, 0.000000000000000000, 0.000000000000000000 ) ) ;
#51758=B_SPLINE_CURVE_WITH_KNOTS ( 'NONE', 3,
 ( #315, #53721, #1348, #43793, #38492, #64662 ),
 .UNSPECIFIED., .F., .F.,
 ( 4, 2, 4 ),
 ( 0.0002380763768132926339, 0.7291065797294586925, 1.457975083082104106 ),
 .UNSPECIFIED. ) ;
#51759=CARTESIAN_POINT ( 'NONE',  ( 24.00000000000000000, -17.50000000000000000, 19.33772233983200195 ) ) ;
#51770=LINE ( 'NONE', #8627, #13696 ) ;
#51773=EDGE_CURVE ( 'NONE', #13228, #51111, #37731, .T. ) ;
#51774=VERTEX_POINT ( 'NONE', #42680 ) ;
#51779=CARTESIAN_POINT ( 'NONE',  ( -15.50000000000000000, -5.000000000000000000, 22.50000000000000000 ) ) ;
#51782=DIRECTION ( 'NONE',  ( 0.000000000000000000, 0.000000000000000000, 1.000000000000000000 ) ) ;
#51784=DIRECTION ( 'NONE',  ( 0.4999999999989417354, 0.000000000000000000, -0.8660254037850495523 ) ) ;
#51789=VECTOR ( 'NONE', #1506, 1000.000000000000000 ) ;
#51791=ORIENTED_EDGE ( 'NONE', *, *, #44925, .T. ) ;
#51792=LINE ( 'NONE', #30570, #13468 ) ;
#51796=CARTESIAN_POINT ( 'NONE',  ( -30.00000000000000000, -11.50000000000100009, 15.00000000000084910 ) ) ;
#51802=PLANE ( 'NONE',  #9133 ) ;
#51822=DIRECTION ( 'NONE',  ( 0.000000000000000000, -0.7046037717806115097, -0.7096009616626348659 ) ) ;
#51825=EDGE_CURVE ( 'NONE', #8763, #37085, #45397, .T. ) ;
#51827=FACE_OUTER_BOUND ( 'NONE', #10535, .T. ) ;
#51829=CIRCLE ( 'NONE', #22510, 4.500000000000190958 ) ;
#51834=EDGE_CURVE ( 'NONE', #45446, #54520, #44061, .T. ) ;
#51837=CIRCLE ( 'NONE', #58608, 4.000000000000000888 ) ;
#51846=DIRECTION ( 'NONE',  ( -1.000000000000000000, 0.000000000000000000, 0.000000000000000000 ) ) ;
#51854=DIRECTION ( 'NONE',  ( -1.000000000000000000, 0.000000000000000000, 0.000000000000000000 ) ) ;
#51860=ORIENTED_EDGE ( 'NONE', *, *, #44870, .T. ) ;
#51866=DIRECTION ( 'NONE',  ( -1.000000000000000000, 0.000000000000000000, 0.000000000000000000 ) ) ;
#51870=VECTOR ( 'NONE', #8386, 1000.000000000000000 ) ;
#51874=LINE ( 'NONE', #18279, #34856 ) ;
#51876=VECTOR ( 'NONE', #15960, 1000.000000000000000 ) ;
#51877=CARTESIAN_POINT ( 'NONE',  ( 15.50000000000000000, -17.50000000000000000, -22.50000000000000000 ) ) ;
#51889=AXIS2_PLACEMENT_3D ( 'NONE', #38070, #59624, #65945 ) ;
#51892=VERTEX_POINT ( 'NONE', #1614 ) ;
#51902=ORIENTED_EDGE ( 'NONE', *, *, #9912, .T. ) ;
#51907=ORIENTED_EDGE ( 'NONE', *, *, #24037, .F. ) ;
#51915=FACE_OUTER_BOUND ( 'NONE', #8742, .T. ) ;
#51925=CARTESIAN_POINT ( 'NONE',  ( 11.00000000000000000, -10.85999999999999943, 9.000000000000001776 ) ) ;
#51926=VERTEX_POINT ( 'NONE', #2663 ) ;
#51927=DIRECTION ( 'NONE',  ( 0.000000000000000000, -1.000000000000000000, 0.000000000000000000 ) ) ;
#51933=VERTEX_POINT ( 'NONE', #62056 ) ;
#51937=VECTOR ( 'NONE', #39387, 1000.000000000000000 ) ;
#51948=DIRECTION ( 'NONE',  ( 0.4999999999989361843, 0.000000000000000000, 0.8660254037850529940 ) ) ;
#51960=ORIENTED_EDGE ( 'NONE', *, *, #31562, .T. ) ;
#51977=ORIENTED_EDGE ( 'NONE', *, *, #17616, .F. ) ;
#51985=AXIS2_PLACEMENT_3D ( 'NONE', #58340, #53037, #9900 ) ;
#51990=ORIENTED_EDGE ( 'NONE', *, *, #30224, .F. ) ;
#51992=AXIS2_PLACEMENT_3D ( 'NONE', #23403, #59844, #28020 ) ;
#51998=CARTESIAN_POINT ( 'NONE',  ( -16.54686605390241994, -0.2715358723599897717, -21.66103272505201360 ) ) ;
#52005=DIRECTION ( 'NONE',  ( -0.000000000000000000, 1.000000000000000000, -0.000000000000000000 ) ) ;
#52014=CONICAL_SURFACE ( 'NONE', #39565, 1732.050807568789651, 1.047197551196575871 ) ;
#52020=EDGE_LOOP ( 'NONE', ( #11787, #28911, #39827, #56208 ) ) ;
#52022=DIRECTION ( 'NONE',  ( 0.000000000000000000, 0.000000000000000000, 1.000000000000000000 ) ) ;
#52036=CARTESIAN_POINT ( 'NONE',  ( -29.50000000000000355, -11.70000000000000284, -11.00000000000000000 ) ) ;
#52038=EDGE_CURVE ( 'NONE', #2156, #47666, #60048, .T. ) ;
#52040=DIRECTION ( 'NONE',  ( 0.000000000000000000, 0.7278708115913771204, 0.6857142857147648929 ) ) ;
#52042=VERTEX_POINT ( 'NONE', #46150 ) ;
#52044=VECTOR ( 'NONE', #11448, 1000.000000000000000 ) ;
#52056=LINE ( 'NONE', #30484, #48878 ) ;
#52057=ORIENTED_EDGE ( 'NONE', *, *, #21265, .T. ) ;
#52061=DIRECTION ( 'NONE',  ( -1.000000000000000000, 0.000000000000000000, 0.000000000000000000 ) ) ;
#52063=DIRECTION ( 'NONE',  ( -1.000000000000000000, 0.000000000000000000, 0.000000000000000000 ) ) ;
#52073=AXIS2_PLACEMENT_3D ( 'NONE', #39566, #49844, #1404 ) ;
#52077=DIRECTION ( 'NONE',  ( -0.000000000000000000, 1.000000000000000000, -0.000000000000000000 ) ) ;
#52083=ORIENTED_EDGE ( 'NONE', *, *, #27491, .F. ) ;
#52085=VECTOR ( 'NONE', #40404, 1000.000000000000000 ) ;
#52093=AXIS2_PLACEMENT_3D ( 'NONE', #7746, #67856, #50882 ) ;
#52096=ORIENTED_EDGE ( 'NONE', *, *, #46392, .T. ) ;
#52097=CONICAL_SURFACE ( 'NONE', #21625, 1732.050807568789651, 1.047197551196575871 ) ;
#52109=PLANE ( 'NONE',  #60016 ) ;
#52116=DIRECTION ( 'NONE',  ( 1.000000000000000000, 0.000000000000000000, 0.000000000000000000 ) ) ;
#52118=EDGE_CURVE ( 'NONE', #16302, #37166, #3725, .T. ) ;
#52133=EDGE_CURVE ( 'NONE', #38076, #67332, #26005, .T. ) ;
#52134=LINE ( 'NONE', #4754, #56194 ) ;
#52135=LINE ( 'NONE', #19598, #625 ) ;
#52139=DIRECTION ( 'NONE',  ( 8.659560562354951347E-17, -0.7071067811865460184, 0.7071067811865489050 ) ) ;
#52148=CARTESIAN_POINT ( 'NONE',  ( 30.00000000000000000, -17.00000000000000000, -15.70499999999969809 ) ) ;
#52151=ORIENTED_EDGE ( 'NONE', *, *, #9777, .T. ) ;
#52152=CARTESIAN_POINT ( 'NONE',  ( 29.50000000000000355, -15.46862696659690073, 14.50000000000000000 ) ) ;
#52167=EDGE_LOOP ( 'NONE', ( #12661, #9680, #60817, #31170 ) ) ;
#52177=PLANE ( 'NONE',  #30126 ) ;
#52178=CARTESIAN_POINT ( 'NONE',  ( -25.50000000000000355, -5.200000000000001066, -24.75000000000000000 ) ) ;
#52180=VERTEX_POINT ( 'NONE', #9019 ) ;
#52182=ORIENTED_EDGE ( 'NONE', *, *, #61714, .T. ) ;
#52191=ORIENTED_EDGE ( 'NONE', *, *, #47434, .T. ) ;
#52192=AXIS2_PLACEMENT_3D ( 'NONE', #15879, #48404, #69633 ) ;
#52199=DIRECTION ( 'NONE',  ( 1.000000000000000000, 0.000000000000000000, 0.000000000000000000 ) ) ;
#52207=LINE ( 'NONE', #63532, #8271 ) ;
#52224=ORIENTED_EDGE ( 'NONE', *, *, #15383, .T. ) ;
#52236=CIRCLE ( 'NONE', #26303, 1.620999999999997332 ) ;
#52237=VERTEX_POINT ( 'NONE', #54965 ) ;
#52238=PLANE ( 'NONE',  #31601 ) ;
#52240=CARTESIAN_POINT ( 'NONE',  ( -15.50000000000000000, -0.2038245569916614930, 23.94337567297399971 ) ) ;
#52242=CARTESIAN_POINT ( 'NONE',  ( -17.51999999999999957, -15.50000000000000000, 26.00000000000000355 ) ) ;
#52244=CIRCLE ( 'NONE', #61246, 0.3499999999998875677 ) ;
#52249=VERTEX_POINT ( 'NONE', #38347 ) ;
#52251=ORIENTED_EDGE ( 'NONE', *, *, #4596, .F. ) ;
#52252=LINE ( 'NONE', #63205, #14792 ) ;
#52256=EDGE_CURVE ( 'NONE', #29308, #36191, #32347, .T. ) ;
#52262=PLANE ( 'NONE',  #55282 ) ;
#52270=LINE ( 'NONE', #46955, #36751 ) ;
#52271=CARTESIAN_POINT ( 'NONE',  ( 16.75000000000000000, -0.3156864504677172611, -22.25638000318208398 ) ) ;
#52273=CARTESIAN_POINT ( 'NONE',  ( -15.50000000000000000, -15.50000000000000000, -22.50000000000000000 ) ) ;
#52275=ORIENTED_EDGE ( 'NONE', *, *, #28786, .T. ) ;
#52276=ORIENTED_EDGE ( 'NONE', *, *, #8153, .T. ) ;
#52279=ORIENTED_EDGE ( 'NONE', *, *, #11910, .F. ) ;
#52281=LINE ( 'NONE', #48025, #35813 ) ;
#52290=ORIENTED_EDGE ( 'NONE', *, *, #39740, .F. ) ;
#52291=DIRECTION ( 'NONE',  ( 0.000000000000000000, 0.6857142857146703019, 0.7278708115914659382 ) ) ;
#52297=DIRECTION ( 'NONE',  ( 0.000000000000000000, 0.000000000000000000, 1.000000000000000000 ) ) ;
#52306=DIRECTION ( 'NONE',  ( 0.000000000000000000, 1.000000000000000000, 0.000000000000000000 ) ) ;
#52308=DIRECTION ( 'NONE',  ( 0.000000000000000000, 1.000000000000000000, 0.000000000000000000 ) ) ;
#52323=DIRECTION ( 'NONE',  ( 0.000000000000000000, -0.7057491738665943037, -0.7084617869628675457 ) ) ;
#52325=CARTESIAN_POINT ( 'NONE',  ( 30.00000000000000000, -17.35230188589299871, 15.35019951917099945 ) ) ;
#52331=CARTESIAN_POINT ( 'NONE',  ( 30.00000000000000000, -11.85423089348099879, 9.852125413066602277 ) ) ;
#52333=ORIENTED_EDGE ( 'NONE', *, *, #21558, .T. ) ;
#52336=FACE_OUTER_BOUND ( 'NONE', #54192, .T. ) ;
#52339=DIRECTION ( 'NONE',  ( 1.000000000000000000, 0.000000000000000000, 0.000000000000000000 ) ) ;
#52343=ADVANCED_FACE ( 'NONE', ( #12827 ), #34392, .F. ) ;
#52348=CARTESIAN_POINT ( 'NONE',  ( -15.50000000000000000, -0.2038245569916614930, -21.05662432702600029 ) ) ;
#52350=VERTEX_POINT ( 'NONE', #39370 ) ;
#52353=CARTESIAN_POINT ( 'NONE',  ( 25.50000000000000355, -15.50000000000000000, 24.50000000000000000 ) ) ;
#52354=DIRECTION ( 'NONE',  ( 1.000000000000000000, -0.000000000000000000, -0.000000000000000000 ) ) ;
#52357=EDGE_LOOP ( 'NONE', ( #66923, #16422, #8123, #12295 ) ) ;
#52359=ORIENTED_EDGE ( 'NONE', *, *, #2569, .T. ) ;
#52361=AXIS2_PLACEMENT_3D ( 'NONE', #28530, #29217, #50792 ) ;
#52362=AXIS2_PLACEMENT_3D ( 'NONE', #32630, #59146, #6100 ) ;
#52368=DIRECTION ( 'NONE',  ( 0.000000000000000000, 0.6857142857142869419, -0.7278708115918273158 ) ) ;
#52369=VERTEX_POINT ( 'NONE', #23806 ) ;
#52372=DIRECTION ( 'NONE',  ( 0.000000000000000000, 1.000000000000000000, 0.000000000000000000 ) ) ;
#52375=CARTESIAN_POINT ( 'NONE',  ( 25.50000000000000355, 0.000000000000000000, -22.50000000000000000 ) ) ;
#52382=FACE_OUTER_BOUND ( 'NONE', #66727, .T. ) ;
#52386=PLANE ( 'NONE',  #3032 ) ;
#52396=VECTOR ( 'NONE', #3439, 1000.000000000000000 ) ;
#52404=CARTESIAN_POINT ( 'NONE',  ( -16.75000000000000000, -0.2038245569916330158, 23.22168783648699986 ) ) ;
#52405=DIRECTION ( 'NONE',  ( -1.000000000000000000, 0.000000000000000000, 0.000000000000000000 ) ) ;
#52413=ORIENTED_EDGE ( 'NONE', *, *, #9447, .F. ) ;
#52418=LINE ( 'NONE', #25549, #39248 ) ;
#52427=ORIENTED_EDGE ( 'NONE', *, *, #56139, .T. ) ;
#52430=CARTESIAN_POINT ( 'NONE',  ( 11.00000000000000000, -16.64230188589299786, -14.64519951917100116 ) ) ;
#52431=DIRECTION ( 'NONE',  ( 0.000000000000000000, 1.000000000000000000, 0.000000000000000000 ) ) ;
#52437=CARTESIAN_POINT ( 'NONE',  ( 30.00000000000000000, -11.50000000000000000, 15.00000000000000000 ) ) ;
#52440=CIRCLE ( 'NONE', #43387, 4.500000000000190958 ) ;
#52454=CIRCLE ( 'NONE', #16308, 0.4000000000000609179 ) ;
#52459=VERTEX_POINT ( 'NONE', #46073 ) ;
#52461=CIRCLE ( 'NONE', #65959, 4.500000000000190958 ) ;
#52463=ORIENTED_EDGE ( 'NONE', *, *, #46255, .T. ) ;
#52465=EDGE_CURVE ( 'NONE', #60150, #16696, #34758, .T. ) ;
#52466=CARTESIAN_POINT ( 'NONE',  ( -11.00000000000000000, -11.50000000000100009, 15.00000000000084910 ) ) ;
#52469=ORIENTED_EDGE ( 'NONE', *, *, #1793, .F. ) ;
#52470=AXIS2_PLACEMENT_3D ( 'NONE', #26885, #44160, #5662 ) ;
#52476=ADVANCED_FACE ( 'NONE', ( #13893 ), #40422, .F. ) ;
#52477=EDGE_CURVE ( 'NONE', #62314, #45394, #17422, .T. ) ;
#52482=EDGE_CURVE ( 'NONE', #27939, #10, #24512, .T. ) ;
#52484=CIRCLE ( 'NONE', #14099, 4.500000000000191847 ) ;
#52488=AXIS2_PLACEMENT_3D ( 'NONE', #42668, #65296, #63894 ) ;
#52489=ORIENTED_EDGE ( 'NONE', *, *, #34185, .T. ) ;
#52496=DIRECTION ( 'NONE',  ( -0.8660254037844482555, 0.000000000000000000, 0.4999999999999831801 ) ) ;
#52510=ORIENTED_EDGE ( 'NONE', *, *, #286, .T. ) ;
#52514=VECTOR ( 'NONE', #33669, 1000.000000000000000 ) ;
#52528=CIRCLE ( 'NONE', #61524, 4.000000000000001776 ) ;
#52539=ORIENTED_EDGE ( 'NONE', *, *, #22090, .T. ) ;
#52548=DIRECTION ( 'NONE',  ( 1.000000000000000000, -0.000000000000000000, -0.000000000000000000 ) ) ;
#52554=VECTOR ( 'NONE', #9297, 1000.000000000000000 ) ;
#52556=AXIS2_PLACEMENT_3D ( 'NONE', #35455, #58458, #9663 ) ;
#52560=VECTOR ( 'NONE', #57784, 1000.000000000000000 ) ;
#52564=EDGE_CURVE ( 'NONE', #2326, #43590, #32124, .T. ) ;
#52567=DIRECTION ( 'NONE',  ( 0.3479852726768751237, 0.000000000000000000, -0.9375000000000004441 ) ) ;
#52569=DIRECTION ( 'NONE',  ( -1.000000000000000000, 0.000000000000000000, 0.000000000000000000 ) ) ;
#52571=CARTESIAN_POINT ( 'NONE',  ( -11.75000000000000000, -5.200000000000001066, 11.75000000000000000 ) ) ;
#52582=VECTOR ( 'NONE', #39150, 1000.000000000000000 ) ;
#52585=CARTESIAN_POINT ( 'NONE',  ( -29.50000000000000355, -12.00000000000000000, -10.52786404500095863 ) ) ;
#52590=CARTESIAN_POINT ( 'NONE',  ( -29.50000000000000355, -11.50000000000100009, -15.00000000000084910 ) ) ;
#52591=CARTESIAN_POINT ( 'NONE',  ( -17.51999999999999957, -17.50000000000000000, -26.00000000000000355 ) ) ;
#52594=LINE ( 'NONE', #25726, #11640 ) ;
#52595=CARTESIAN_POINT ( 'NONE',  ( 29.50000000000000355, -15.46862696659690073, -14.50000000000000000 ) ) ;
#52596=ORIENTED_EDGE ( 'NONE', *, *, #3804, .T. ) ;
#52597=AXIS2_PLACEMENT_3D ( 'NONE', #13570, #23128, #40072 ) ;
#52602=DIRECTION ( 'NONE',  ( 0.000000000000000000, 0.000000000000000000, -1.000000000000000000 ) ) ;
#52603=ORIENTED_EDGE ( 'NONE', *, *, #30757, .T. ) ;
#52609=VECTOR ( 'NONE', #64659, 1000.000000000000000 ) ;
#52618=VECTOR ( 'NONE', #37458, 1000.000000000000000 ) ;
#52620=ORIENTED_EDGE ( 'NONE', *, *, #52887, .F. ) ;
#52624=DIRECTION ( 'NONE',  ( -1.000000000000000000, 0.000000000000000000, 0.000000000000000000 ) ) ;
#52637=EDGE_LOOP ( 'NONE', ( #60028, #38380, #68112, #28507 ) ) ;
#52641=FACE_BOUND ( 'NONE', #38069, .T. ) ;
#52651=VECTOR ( 'NONE', #51078, 1000.000000000000000 ) ;
#52657=VERTEX_POINT ( 'NONE', #65145 ) ;
#52660=LINE ( 'NONE', #46986, #476 ) ;
#52663=CIRCLE ( 'NONE', #27814, 0.5000000000079367624 ) ;
#52687=PLANE ( 'NONE',  #53556 ) ;
#52689=LINE ( 'NONE', #8118, #55668 ) ;
#52690=ORIENTED_EDGE ( 'NONE', *, *, #1152, .T. ) ;
#52694=ORIENTED_EDGE ( 'NONE', *, *, #61016, .T. ) ;
#52707=ORIENTED_EDGE ( 'NONE', *, *, #59966, .T. ) ;
#52717=AXIS2_PLACEMENT_3D ( 'NONE', #27349, #6119, #53884 ) ;
#52725=VERTEX_POINT ( 'NONE', #16341 ) ;
#52734=EDGE_CURVE ( 'NONE', #60914, #7905, #12860, .T. ) ;
#52745=DIRECTION ( 'NONE',  ( -1.000000000000000000, 0.000000000000000000, 0.000000000000000000 ) ) ;
#52750=ORIENTED_EDGE ( 'NONE', *, *, #64189, .F. ) ;
#52758=VECTOR ( 'NONE', #3849, 1000.000000000000000 ) ;
#52761=ORIENTED_EDGE ( 'NONE', *, *, #37584, .F. ) ;
#52762=LINE ( 'NONE', #4321, #51876 ) ;
#52763=CARTESIAN_POINT ( 'NONE',  ( -17.00000000000000000, -16.64230188589299786, -14.64519951917100116 ) ) ;
#52773=AXIS2_PLACEMENT_3D ( 'NONE', #32905, #37524, #6039 ) ;
#52777=DIRECTION ( 'NONE',  ( 0.000000000000000000, 0.000000000000000000, 1.000000000000000000 ) ) ;
#52778=VERTEX_POINT ( 'NONE', #61183 ) ;
#52782=LINE ( 'NONE', #68316, #59011 ) ;
#52800=FACE_OUTER_BOUND ( 'NONE', #61921, .T. ) ;
#52803=CARTESIAN_POINT ( 'NONE',  ( 11.00000000000000000, -12.00000000000000000, -10.52786404500095863 ) ) ;
#52821=ORIENTED_EDGE ( 'NONE', *, *, #39740, .T. ) ;
#52822=LINE ( 'NONE', #42534, #59879 ) ;
#52823=VECTOR ( 'NONE', #13594, 1000.000000000000000 ) ;
#52838=CARTESIAN_POINT ( 'NONE',  ( 13.00000000000000178, -16.28999999999710369, 15.00000000000794920 ) ) ;
#52840=EDGE_LOOP ( 'NONE', ( #16111, #24741, #45206, #44747 ) ) ;
#52846=ORIENTED_EDGE ( 'NONE', *, *, #1840, .F. ) ;
#52852=ADVANCED_FACE ( 'NONE', ( #44578 ), #12399, .F. ) ;
#52853=DIRECTION ( 'NONE',  ( 0.000000000000000000, 1.000000000000000000, 0.000000000000000000 ) ) ;
#52854=DIRECTION ( 'NONE',  ( 0.000000000000000000, 0.000000000000000000, 1.000000000000000000 ) ) ;
#52869=FACE_OUTER_BOUND ( 'NONE', #47709, .T. ) ;
#52878=VERTEX_POINT ( 'NONE', #8496 ) ;
#52882=LINE ( 'NONE', #63820, #21434 ) ;
#52886=DIRECTION ( 'NONE',  ( 8.659560562354963673E-17, 0.7071067811865450192, -0.7071067811865500152 ) ) ;
#52887=EDGE_CURVE ( 'NONE', #14877, #32707, #45624, .T. ) ;
#52889=ADVANCED_FACE ( 'NONE', ( #7454 ), #56251, .F. ) ;
#52896=LINE ( 'NONE', #57817, #30942 ) ;
#52900=EDGE_LOOP ( 'NONE', ( #38532, #3677, #13548, #40295 ) ) ;
#52912=AXIS2_PLACEMENT_3D ( 'NONE', #4943, #48076, #36411 ) ;
#52926=DIRECTION ( 'NONE',  ( -1.000000000000000000, 0.000000000000000000, 0.000000000000000000 ) ) ;
#52934=EDGE_CURVE ( 'NONE', #41126, #67437, #42434, .T. ) ;
#52935=DIRECTION ( 'NONE',  ( 0.000000000000000000, -0.6857142857147903170, -0.7278708115913530285 ) ) ;
#52938=CARTESIAN_POINT ( 'NONE',  ( -11.00000000000000000, -9.454754784057099570, 17.53999999999999915 ) ) ;
#52951=DIRECTION ( 'NONE',  ( -1.000000000000000000, 0.000000000000000000, 0.000000000000000000 ) ) ;
#52955=CARTESIAN_POINT ( 'NONE',  ( -15.29686605391142606, -0.2715358723588648937, 23.82609623451821079 ) ) ;
#52957=CYLINDRICAL_SURFACE ( 'NONE', #46115, 3.499999999999999556 ) ;
#52959=CARTESIAN_POINT ( 'NONE',  ( 15.50000000000000000, -1.037157890325000054, 18.50000000000000000 ) ) ;
#52962=FACE_OUTER_BOUND ( 'NONE', #21335, .T. ) ;
#52985=EDGE_LOOP ( 'NONE', ( #12189, #58366, #67530, #45614 ) ) ;
#52993=ORIENTED_EDGE ( 'NONE', *, *, #50777, .T. ) ;
#52998=DIRECTION ( 'NONE',  ( 0.000000000000000000, 0.000000000000000000, 1.000000000000000000 ) ) ;
#53001=ORIENTED_EDGE ( 'NONE', *, *, #63111, .F. ) ;
#53003=CARTESIAN_POINT ( 'NONE',  ( -15.50000000000000000, -0.4000000000005236034, 22.50000000000000000 ) ) ;
#53027=EDGE_CURVE ( 'NONE', #35617, #40989, #36658, .T. ) ;
#53030=DIRECTION ( 'NONE',  ( 0.000000000000000000, 0.7071067811865455743, 0.7071067811865495711 ) ) ;
#53031=CARTESIAN_POINT ( 'NONE',  ( -11.00000000000000000, -9.487228132326899654, 12.50000000000000000 ) ) ;
#53034=DIRECTION ( 'NONE',  ( 1.000000000000000000, -0.000000000000000000, -0.000000000000000000 ) ) ;
#53036=EDGE_CURVE ( 'NONE', #42264, #55585, #37144, .T. ) ;
#53037=DIRECTION ( 'NONE',  ( -1.000000000000000000, 0.000000000000000000, 0.000000000000000000 ) ) ;
#53038=CARTESIAN_POINT ( 'NONE',  ( 11.50000000000000000, -12.00000000000000000, 10.52786404500095863 ) ) ;
#53040=ORIENTED_EDGE ( 'NONE', *, *, #32523, .T. ) ;
#53043=EDGE_LOOP ( 'NONE', ( #46235, #19458, #6611, #24084, #54699, #63658, #12648, #28182, #30094, #31324, #48452 ) ) ;
#53044=ORIENTED_EDGE ( 'NONE', *, *, #65392, .F. ) ;
#53048=CYLINDRICAL_SURFACE ( 'NONE', #40025, 4.000000000000000000 ) ;
#53059=LINE ( 'NONE', #36427, #67068 ) ;
#53063=AXIS2_PLACEMENT_3D ( 'NONE', #31881, #54141, #53446 ) ;
#53064=CYLINDRICAL_SURFACE ( 'NONE', #58310, 0.3999999999993835154 ) ;
#53068=LINE ( 'NONE', #68966, #49991 ) ;
#53077=DIRECTION ( 'NONE',  ( 0.000000000000000000, 0.000000000000000000, 1.000000000000000000 ) ) ;
#53078=ORIENTED_EDGE ( 'NONE', *, *, #66398, .F. ) ;
#53086=DIRECTION ( 'NONE',  ( 1.000000000000000000, -0.000000000000000000, -0.000000000000000000 ) ) ;
#53088=CARTESIAN_POINT ( 'NONE',  ( 11.50000000000000000, -11.50000000000100009, -15.00000000000084910 ) ) ;
#53090=EDGE_CURVE ( 'NONE', #18754, #67430, #63780, .T. ) ;
#53093=ORIENTED_EDGE ( 'NONE', *, *, #56457, .T. ) ;
#53094=CARTESIAN_POINT ( 'NONE',  ( 15.50000000000000000, -0.4000000000000000222, -22.50000000000000000 ) ) ;
#53095=ORIENTED_EDGE ( 'NONE', *, *, #45853, .F. ) ;
#53097=LINE ( 'NONE', #14544, #64590 ) ;
#53116=ORIENTED_EDGE ( 'NONE', *, *, #5618, .T. ) ;
#53117=CYLINDRICAL_SURFACE ( 'NONE', #61344, 0.2999999999998732569 ) ;
#53127=FACE_OUTER_BOUND ( 'NONE', #5679, .T. ) ;
#53137=EDGE_CURVE ( 'NONE', #14914, #28218, #3913, .T. ) ;
#53141=ORIENTED_EDGE ( 'NONE', *, *, #18502, .T. ) ;
#53145=EDGE_CURVE ( 'NONE', #57228, #38183, #6678, .T. ) ;
#53151=FACE_OUTER_BOUND ( 'NONE', #24829, .T. ) ;
#53152=ADVANCED_FACE ( 'NONE', ( #61104 ), #67115, .F. ) ;
#53169=VECTOR ( 'NONE', #14737, 1000.000000000000000 ) ;
#53175=ORIENTED_EDGE ( 'NONE', *, *, #47138, .T. ) ;
#53177=LINE ( 'NONE', #53870, #18700 ) ;
#53185=AXIS2_PLACEMENT_3D ( 'NONE', #12347, #54826, #6384 ) ;
#53188=DIRECTION ( 'NONE',  ( 0.000000000000000000, 0.000000000000000000, 1.000000000000000000 ) ) ;
#53194=ADVANCED_FACE ( 'NONE', ( #56507 ), #1719, .F. ) ;
#53196=DIRECTION ( 'NONE',  ( -1.000000000000000000, 0.000000000000000000, 0.000000000000000000 ) ) ;
#53197=CARTESIAN_POINT ( 'NONE',  ( 16.75000000000000355, -0.2715193793361441177, 22.98718409945082897 ) ) ;
#53198=CIRCLE ( 'NONE', #1237, 2.250000000000001776 ) ;
#53199=LINE ( 'NONE', #41864, #57330 ) ;
#53201=PLANE ( 'NONE',  #31826 ) ;
#53202=DIRECTION ( 'NONE',  ( 0.8660254037844482555, 0.000000000000000000, 0.4999999999999831801 ) ) ;
#53210=EDGE_LOOP ( 'NONE', ( #53629, #33036, #49254, #12713 ) ) ;
#53212=FACE_OUTER_BOUND ( 'NONE', #34768, .T. ) ;
#53220=CARTESIAN_POINT ( 'NONE',  ( 30.00000000000000000, -13.79999999999979998, 17.30000000000000071 ) ) ;
#53223=CARTESIAN_POINT ( 'NONE',  ( -30.00000000000000000, -11.50000000000000000, -19.00000000000000000 ) ) ;
#53231=CARTESIAN_POINT ( 'NONE',  ( 28.00000000000000000, -16.64230188589299786, 14.64519951917100116 ) ) ;
#53232=ORIENTED_EDGE ( 'NONE', *, *, #61727, .T. ) ;
#53243=EDGE_CURVE ( 'NONE', #39690, #1158, #50846, .T. ) ;
#53245=ORIENTED_EDGE ( 'NONE', *, *, #42802, .F. ) ;
#53255=ORIENTED_EDGE ( 'NONE', *, *, #69046, .T. ) ;
#53257=CARTESIAN_POINT ( 'NONE',  ( -11.00000000000000000, -11.10796162543699950, 9.102987789146602893 ) ) ;
#53258=LINE ( 'NONE', #15420, #67425 ) ;
#53261=AXIS2_PLACEMENT_3D ( 'NONE', #4681, #26249, #64096 ) ;
#53267=ADVANCED_FACE ( 'NONE', ( #61824 ), #13376, .T. ) ;
#53271=ORIENTED_EDGE ( 'NONE', *, *, #18356, .T. ) ;
#53274=ADVANCED_FACE ( 'NONE', ( #13722 ), #52262, .F. ) ;
#53275=CIRCLE ( 'NONE', #20502, 3.499999999999999556 ) ;
#53288=ORIENTED_EDGE ( 'NONE', *, *, #34277, .T. ) ;
#53289=CARTESIAN_POINT ( 'NONE',  ( 30.00000000000000000, -11.50000000000100009, -10.50000000000065903 ) ) ;
#53320=DIRECTION ( 'NONE',  ( 0.000000000000000000, 0.000000000000000000, 1.000000000000000000 ) ) ;
#53328=CARTESIAN_POINT ( 'NONE',  ( -17.00000000000000000, -17.50000000000000000, 15.70499999999969809 ) ) ;
#53329=ORIENTED_EDGE ( 'NONE', *, *, #69231, .T. ) ;
#53334=FACE_OUTER_BOUND ( 'NONE', #2229, .T. ) ;
#53339=ORIENTED_EDGE ( 'NONE', *, *, #854, .T. ) ;
#53356=CARTESIAN_POINT ( 'NONE',  ( -17.00000000000000000, -17.50000000000000000, -15.70500000000000007 ) ) ;
#53368=CARTESIAN_POINT ( 'NONE',  ( 30.00000000000000000, -16.28999999999710369, 15.00000000000794920 ) ) ;
#53371=DIRECTION ( 'NONE',  ( -1.000000000000000000, 0.000000000000000000, 0.000000000000000000 ) ) ;
#53374=DIRECTION ( 'NONE',  ( 0.000000000000000000, -0.9938079899998859545, 0.1111111111112941946 ) ) ;
#53386=ORIENTED_EDGE ( 'NONE', *, *, #2032, .F. ) ;
#53389=ORIENTED_EDGE ( 'NONE', *, *, #34813, .T. ) ;
#53391=CARTESIAN_POINT ( 'NONE',  ( -11.00000000000000000, -11.50000000000100009, -10.50000000000065903 ) ) ;
#53393=FACE_OUTER_BOUND ( 'NONE', #40802, .T. ) ;
#53399=EDGE_LOOP ( 'NONE', ( #53943, #43774, #34070, #5815, #4851, #62188, #8033 ) ) ;
#53409=ORIENTED_EDGE ( 'NONE', *, *, #58729, .F. ) ;
#53414=FACE_OUTER_BOUND ( 'NONE', #27466, .T. ) ;
#53419=VECTOR ( 'NONE', #68144, 1000.000000000000114 ) ;
#53422=ORIENTED_EDGE ( 'NONE', *, *, #55739, .F. ) ;
#53425=LINE ( 'NONE', #42457, #14298 ) ;
#53436=ORIENTED_EDGE ( 'NONE', *, *, #54295, .F. ) ;
#53439=CIRCLE ( 'NONE', #29683, 4.500000000000190958 ) ;
#53441=CARTESIAN_POINT ( 'NONE',  ( 15.50000000000000000, -1.037157890325000054, 26.00000000000000000 ) ) ;
#53446=DIRECTION ( 'NONE',  ( 0.000000000000000000, 0.000000000000000000, -1.000000000000000000 ) ) ;
#53450=PLANE ( 'NONE',  #17493 ) ;
#53470=VERTEX_POINT ( 'NONE', #53667 ) ;
#53475=AXIS2_PLACEMENT_3D ( 'NONE', #55369, #43719, #7250 ) ;
#53482=DIRECTION ( 'NONE',  ( 0.000000000000000000, 0.000000000000000000, 1.000000000000000000 ) ) ;
#53496=CARTESIAN_POINT ( 'NONE',  ( 30.00000000000000000, -15.97213595500069871, -14.50000000000000000 ) ) ;
#53497=B_SPLINE_CURVE_WITH_KNOTS ( 'NONE', 3,
 ( #38305, #32989, #43248, #60196, #44275, #836 ),
 .UNSPECIFIED., .F., .F.,
 ( 4, 2, 4 ),
 ( 0.0002380763768129734448, 0.7291065797294589146, 1.457975083082104995 ),
 .UNSPECIFIED. ) ;
#53500=CARTESIAN_POINT ( 'NONE',  ( -11.50000000000000000, -15.97213595500069871, -14.50000000000000000 ) ) ;
#53522=ORIENTED_EDGE ( 'NONE', *, *, #37584, .T. ) ;
#53534=ORIENTED_EDGE ( 'NONE', *, *, #25314, .T. ) ;
#53537=ADVANCED_FACE ( 'NONE', ( #50710 ), #2622, .F. ) ;
#53538=CYLINDRICAL_SURFACE ( 'NONE', #32520, 4.000000000000000000 ) ;
#53540=DIRECTION ( 'NONE',  ( -1.000000000000000000, 0.000000000000000000, 0.000000000000000000 ) ) ;
#53543=EDGE_CURVE ( 'NONE', #43882, #29308, #22804, .T. ) ;
#53544=CARTESIAN_POINT ( 'NONE',  ( 11.50000000000000000, -11.50000000000100009, 15.00000000000084910 ) ) ;
#53549=DIRECTION ( 'NONE',  ( 0.000000000000000000, 0.7096009616570518874, -0.7046037717862339012 ) ) ;
#53556=AXIS2_PLACEMENT_3D ( 'NONE', #25810, #67884, #68227 ) ;
#53561=LINE ( 'NONE', #5118, #52044 ) ;
#53563=CIRCLE ( 'NONE', #17395, 4.000000000000000888 ) ;
#53565=LINE ( 'NONE', #46842, #44031 ) ;
#53581=LINE ( 'NONE', #48277, #42696 ) ;
#53584=ADVANCED_FACE ( 'NONE', ( #55338 ), #34963, .F. ) ;
#53591=ORIENTED_EDGE ( 'NONE', *, *, #37753, .T. ) ;
#53595=DIRECTION ( 'NONE',  ( 0.000000000000000000, -0.7278708115916125987, 0.6857142857145147596 ) ) ;
#53596=VERTEX_POINT ( 'NONE', #23139 ) ;
#53602=EDGE_CURVE ( 'NONE', #45591, #53754, #44698, .T. ) ;
#53614=ORIENTED_EDGE ( 'NONE', *, *, #33230, .F. ) ;
#53623=DIRECTION ( 'NONE',  ( 0.000000000000000000, 0.000000000000000000, 1.000000000000000000 ) ) ;
#53629=ORIENTED_EDGE ( 'NONE', *, *, #67643, .F. ) ;
#53630=CARTESIAN_POINT ( 'NONE',  ( 30.00000000000000000, -11.70000000000000284, -12.50000000000000000 ) ) ;
#53634=LINE ( 'NONE', #4497, #48848 ) ;
#53639=CARTESIAN_POINT ( 'NONE',  ( 13.00000000000000178, -15.50000000000000000, -20.05051025721700242 ) ) ;
#53641=DIRECTION ( 'NONE',  ( 0.000000000000000000, 1.000000000000000000, 0.000000000000000000 ) ) ;
#53644=CARTESIAN_POINT ( 'NONE',  ( -27.50000000000000000, -5.200000000000001066, 22.50000000000000000 ) ) ;
#53645=CARTESIAN_POINT ( 'NONE',  ( 14.25000000000000000, -2.500000000000000000, -23.22168783648699986 ) ) ;
#53651=ORIENTED_EDGE ( 'NONE', *, *, #56682, .T. ) ;
#53667=CARTESIAN_POINT ( 'NONE',  ( -30.00000000000000000, -12.00000000000000000, 10.52786404500095863 ) ) ;
#53673=ORIENTED_EDGE ( 'NONE', *, *, #58388, .F. ) ;
#53677=DIRECTION ( 'NONE',  ( -1.000000000000000000, 0.000000000000000000, 0.000000000000000000 ) ) ;
#53688=DIRECTION ( 'NONE',  ( -1.000000000000000000, 0.000000000000000000, 0.000000000000000000 ) ) ;
#53695=ORIENTED_EDGE ( 'NONE', *, *, #16984, .F. ) ;
#53696=DIRECTION ( 'NONE',  ( 0.000000000000000000, -1.000000000000000000, 0.000000000000000000 ) ) ;
#53700=DIRECTION ( 'NONE',  ( 0.000000000000000000, 0.000000000000000000, 1.000000000000000000 ) ) ;
#53705=CARTESIAN_POINT ( 'NONE',  ( 29.50000000000000355, -12.00000000000000000, 11.00000000000000000 ) ) ;
#53710=CIRCLE ( 'NONE', #25436, 0.3999999999993835154 ) ;
#53717=CIRCLE ( 'NONE', #7397, 4.000000000000000000 ) ;
#53721=CARTESIAN_POINT ( 'NONE',  ( -14.45313394609757651, -0.2715358723599896051, 21.66103272505202781 ) ) ;
#53724=DIRECTION ( 'NONE',  ( 0.000000000000000000, 0.7096009616570518874, 0.7046037717862339012 ) ) ;
#53732=ORIENTED_EDGE ( 'NONE', *, *, #23162, .T. ) ;
#53737=LINE ( 'NONE', #59031, #63034 ) ;
#53744=ORIENTED_EDGE ( 'NONE', *, *, #6477, .T. ) ;
#53751=DIRECTION ( 'NONE',  ( 0.000000000000000000, -5.800915303574361727E-12, -1.000000000000000000 ) ) ;
#53754=VERTEX_POINT ( 'NONE', #57063 ) ;
#53760=ORIENTED_EDGE ( 'NONE', *, *, #54782, .F. ) ;
#53767=AXIS2_PLACEMENT_3D ( 'NONE', #42099, #26195, #3227 ) ;
#53773=LINE ( 'NONE', #59757, #15400 ) ;
#53775=ORIENTED_EDGE ( 'NONE', *, *, #56636, .F. ) ;
#53776=FACE_OUTER_BOUND ( 'NONE', #61441, .T. ) ;
#53783=DIRECTION ( 'NONE',  ( -1.000000000000000000, 0.000000000000000000, 0.000000000000000000 ) ) ;
#53785=ORIENTED_EDGE ( 'NONE', *, *, #54401, .F. ) ;
#53788=EDGE_LOOP ( 'NONE', ( #20281, #18159, #57413, #55384, #12512, #34618, #36820, #59864, #22279 ) ) ;
#53795=ORIENTED_EDGE ( 'NONE', *, *, #45725, .F. ) ;
#53799=ORIENTED_EDGE ( 'NONE', *, *, #42089, .F. ) ;
#53801=AXIS2_PLACEMENT_3D ( 'NONE', #34798, #39750, #50716 ) ;
#53808=FACE_OUTER_BOUND ( 'NONE', #25287, .T. ) ;
#53811=EDGE_LOOP ( 'NONE', ( #57841, #61653, #68759, #36406 ) ) ;
#53812=DIRECTION ( 'NONE',  ( 0.000000000000000000, 0.000000000000000000, -1.000000000000000000 ) ) ;
#53818=VECTOR ( 'NONE', #4245, 1000.000000000000000 ) ;
#53841=DIRECTION ( 'NONE',  ( 1.000000000000000000, -0.000000000000000000, -0.000000000000000000 ) ) ;
#53845=ORIENTED_EDGE ( 'NONE', *, *, #68744, .T. ) ;
#53847=ORIENTED_EDGE ( 'NONE', *, *, #18490, .F. ) ;
#53848=DIRECTION ( 'NONE',  ( 0.000000000000000000, 0.000000000000000000, -1.000000000000000000 ) ) ;
#53850=EDGE_CURVE ( 'NONE', #46878, #37678, #48223, .T. ) ;
#53857=AXIS2_PLACEMENT_3D ( 'NONE', #1767, #13062, #12017 ) ;
#53864=ORIENTED_EDGE ( 'NONE', *, *, #28864, .F. ) ;
#53866=AXIS2_PLACEMENT_3D ( 'NONE', #50545, #22971, #38555 ) ;
#53867=CIRCLE ( 'NONE', #24517, 4.500000000000191847 ) ;
#53870=CARTESIAN_POINT ( 'NONE',  ( -13.00000000000000178, -15.50000000000000000, 20.05051025721700242 ) ) ;
#53879=DIRECTION ( 'NONE',  ( -0.000000000000000000, 1.000000000000000000, -0.000000000000000000 ) ) ;
#53880=VECTOR ( 'NONE', #14546, 1000.000000000000000 ) ;
#53884=DIRECTION ( 'NONE',  ( 0.3479852726768751237, 0.000000000000000000, -0.9375000000000004441 ) ) ;
#53888=DIRECTION ( 'NONE',  ( 0.000000000000000000, 1.000000000000000000, 0.000000000000000000 ) ) ;
#53894=DIRECTION ( 'NONE',  ( 0.000000000000000000, 0.000000000000000000, 1.000000000000000000 ) ) ;
#53908=DIRECTION ( 'NONE',  ( -1.000000000000000000, 0.000000000000000000, 0.000000000000000000 ) ) ;
#53909=CIRCLE ( 'NONE', #35869, 0.4000000000000600298 ) ;
#53916=ORIENTED_EDGE ( 'NONE', *, *, #43843, .F. ) ;
#53925=AXIS2_PLACEMENT_3D ( 'NONE', #15912, #21230, #36791 ) ;
#53934=DIRECTION ( 'NONE',  ( 0.000000000000000000, 0.000000000000000000, 1.000000000000000000 ) ) ;
#53941=ORIENTED_EDGE ( 'NONE', *, *, #50977, .F. ) ;
#53943=ORIENTED_EDGE ( 'NONE', *, *, #64061, .T. ) ;
#53948=EDGE_CURVE ( 'NONE', #47752, #19062, #44277, .T. ) ;
#53952=AXIS2_PLACEMENT_3D ( 'NONE', #43955, #65534, #38660 ) ;
#53955=AXIS2_PLACEMENT_3D ( 'NONE', #9496, #68554, #37082 ) ;
#53963=VECTOR ( 'NONE', #55847, 1000.000000000000114 ) ;
#53967=CIRCLE ( 'NONE', #62990, 0.5000000000079362072 ) ;
#53987=DIRECTION ( 'NONE',  ( 0.000000000000000000, 1.000000000000000000, 0.000000000000000000 ) ) ;
#53990=DIRECTION ( 'NONE',  ( 0.4999999999989371835, 0.000000000000000000, -0.8660254037850523279 ) ) ;
#53993=ORIENTED_EDGE ( 'NONE', *, *, #25405, .T. ) ;
#53998=EDGE_CURVE ( 'NONE', #12276, #5787, #1844, .T. ) ;
#54044=FACE_OUTER_BOUND ( 'NONE', #8611, .T. ) ;
#54048=LINE ( 'NONE', #27168, #33981 ) ;
#54057=AXIS2_PLACEMENT_3D ( 'NONE', #63560, #31737, #3457 ) ;
#54058=EDGE_CURVE ( 'NONE', #25620, #17134, #20350, .T. ) ;
#54066=CARTESIAN_POINT ( 'NONE',  ( -15.50000000000000000, -1.037157890325000054, 26.00000000000000000 ) ) ;
#54072=LINE ( 'NONE', #32146, #32272 ) ;
#54079=VERTEX_POINT ( 'NONE', #8184 ) ;
#54088=DIRECTION ( 'NONE',  ( 1.000000000000000000, 0.000000000000000000, 0.000000000000000000 ) ) ;
#54090=VERTEX_POINT ( 'NONE', #67949 ) ;
#54093=ORIENTED_EDGE ( 'NONE', *, *, #16355, .F. ) ;
#54101=EDGE_LOOP ( 'NONE', ( #42791, #28092, #67822, #50060 ) ) ;
#54102=VERTEX_POINT ( 'NONE', #46370 ) ;
#54109=CIRCLE ( 'NONE', #31549, 3.499999999999855227 ) ;
#54117=DIRECTION ( 'NONE',  ( 0.000000000000000000, 0.000000000000000000, -1.000000000000000000 ) ) ;
#54122=LINE ( 'NONE', #5682, #6420 ) ;
#54126=CIRCLE ( 'NONE', #27016, 4.000000000000000888 ) ;
#54138=CARTESIAN_POINT ( 'NONE',  ( 11.00000000000000000, -5.200000000000001066, 26.59999999999999432 ) ) ;
#54141=DIRECTION ( 'NONE',  ( 1.000000000000000000, 0.000000000000000000, 0.000000000000000000 ) ) ;
#54145=FACE_OUTER_BOUND ( 'NONE', #13289, .T. ) ;
#54149=CARTESIAN_POINT ( 'NONE',  ( 14.25000000000000000, -0.2038245569916330158, -23.22168783648699986 ) ) ;
#54154=CYLINDRICAL_SURFACE ( 'NONE', #39588, 3.499999999999055866 ) ;
#54160=DIRECTION ( 'NONE',  ( 0.000000000000000000, 0.000000000000000000, -1.000000000000000000 ) ) ;
#54165=EDGE_CURVE ( 'NONE', #45304, #10852, #24465, .T. ) ;
#54170=VECTOR ( 'NONE', #36841, 1000.000000000000000 ) ;
#54173=AXIS2_PLACEMENT_3D ( 'NONE', #11686, #27620, #59798 ) ;
#54177=EDGE_LOOP ( 'NONE', ( #51407, #34236, #59160, #36160 ) ) ;
#54178=DIRECTION ( 'NONE',  ( 0.000000000000000000, 0.000000000000000000, -1.000000000000000000 ) ) ;
#54180=ORIENTED_EDGE ( 'NONE', *, *, #53602, .F. ) ;
#54192=EDGE_LOOP ( 'NONE', ( #25198, #55814, #15235, #63558 ) ) ;
#54200=ORIENTED_EDGE ( 'NONE', *, *, #15687, .T. ) ;
#54207=EDGE_CURVE ( 'NONE', #28131, #53754, #37870, .T. ) ;
#54214=VECTOR ( 'NONE', #34892, 1000.000000000000000 ) ;
#54218=ORIENTED_EDGE ( 'NONE', *, *, #38870, .T. ) ;
#54233=FACE_OUTER_BOUND ( 'NONE', #16492, .T. ) ;
#54241=PLANE ( 'NONE',  #27725 ) ;
#54248=LINE ( 'NONE', #33017, #55020 ) ;
#54254=LINE ( 'NONE', #874, #41887 ) ;
#54264=EDGE_LOOP ( 'NONE', ( #14802, #59812, #40535, #38721, #13978, #9770, #67380, #5500, #17458, #1643, #62550, #26332, #8954, #28650, #61838, #7267, #37976, #43374, #65997, #56042 ) ) ;
#54266=DIRECTION ( 'NONE',  ( 1.000000000000000000, 0.000000000000000000, 0.000000000000000000 ) ) ;
#54269=ORIENTED_EDGE ( 'NONE', *, *, #27905, .F. ) ;
#54270=CIRCLE ( 'NONE', #23701, 4.500000000000190958 ) ;
#54271=ORIENTED_EDGE ( 'NONE', *, *, #41193, .F. ) ;
#54276=ORIENTED_EDGE ( 'NONE', *, *, #39420, .F. ) ;
#54279=DIRECTION ( 'NONE',  ( 1.000000000000000000, -0.000000000000000000, -0.000000000000000000 ) ) ;
#54280=AXIS2_PLACEMENT_3D ( 'NONE', #57042, #24171, #17829 ) ;
#54288=DIRECTION ( 'NONE',  ( 0.000000000000000000, 0.6857142857142869419, -0.7278708115918273158 ) ) ;
#54295=EDGE_CURVE ( 'NONE', #47155, #63841, #15620, .T. ) ;
#54299=VERTEX_POINT ( 'NONE', #58745 ) ;
#54313=CYLINDRICAL_SURFACE ( 'NONE', #58456, 0.4999999999991868727 ) ;
#54320=ORIENTED_EDGE ( 'NONE', *, *, #39086, .T. ) ;
#54325=CARTESIAN_POINT ( 'NONE',  ( -11.00000000000000000, -11.50000000000100009, 19.50000000000103739 ) ) ;
#54326=LINE ( 'NONE', #48323, #33034 ) ;
#54337=VERTEX_POINT ( 'NONE', #10995 ) ;
#54339=EDGE_LOOP ( 'NONE', ( #40619, #55275, #65095, #24804 ) ) ;
#54344=VERTEX_POINT ( 'NONE', #6712 ) ;
#54368=CARTESIAN_POINT ( 'NONE',  ( 14.10805890929250062, -5.000000000000000000, 26.25000000000000000 ) ) ;
#54374=EDGE_LOOP ( 'NONE', ( #64761, #8706, #45535, #68010 ) ) ;
#54377=ORIENTED_EDGE ( 'NONE', *, *, #54207, .F. ) ;
#54383=DIRECTION ( 'NONE',  ( -1.000000000000000000, 0.000000000000000000, 0.000000000000000000 ) ) ;
#54384=EDGE_CURVE ( 'NONE', #42854, #27322, #23772, .T. ) ;
#54394=ADVANCED_FACE ( 'NONE', ( #28626 ), #17678, .T. ) ;
#54401=EDGE_CURVE ( 'NONE', #54664, #24168, #1414, .T. ) ;
#54410=LINE ( 'NONE', #11935, #6042 ) ;
#54413=CARTESIAN_POINT ( 'NONE',  ( -11.00000000000000000, -8.959999999999999076, 12.95475478405700009 ) ) ;
#54433=ORIENTED_EDGE ( 'NONE', *, *, #19391, .F. ) ;
#54447=VERTEX_POINT ( 'NONE', #43859 ) ;
#54448=CARTESIAN_POINT ( 'NONE',  ( 11.50000000000000000, -11.70000000000012008, -11.00000000000000000 ) ) ;
#54449=ORIENTED_EDGE ( 'NONE', *, *, #27329, .T. ) ;
#54458=ORIENTED_EDGE ( 'NONE', *, *, #21771, .T. ) ;
#54460=AXIS2_PLACEMENT_3D ( 'NONE', #29720, #1810, #62246 ) ;
#54462=ADVANCED_FACE ( 'NONE', ( #34969 ), #45941, .T. ) ;
#54467=DIRECTION ( 'NONE',  ( 0.000000000000000000, 1.000000000000000000, 0.000000000000000000 ) ) ;
#54492=EDGE_CURVE ( 'NONE', #69773, #12080, #39554, .T. ) ;
#54498=CARTESIAN_POINT ( 'NONE',  ( 14.25000000000000178, -0.2714405302574905421, -22.01253933645463690 ) ) ;
#54510=EDGE_CURVE ( 'NONE', #31847, #32441, #14108, .T. ) ;
#54512=CARTESIAN_POINT ( 'NONE',  ( 30.00000000000000000, -11.50000000000000000, 15.00000000000000000 ) ) ;
#54516=DIRECTION ( 'NONE',  ( 1.000000000000000000, 0.000000000000000000, 0.000000000000000000 ) ) ;
#54520=VERTEX_POINT ( 'NONE', #8813 ) ;
#54531=DIRECTION ( 'NONE',  ( 0.000000000000000000, 0.000000000000000000, 1.000000000000000000 ) ) ;
#54534=CARTESIAN_POINT ( 'NONE',  ( -30.00000000000000000, -11.50000000000000000, 11.00000000000000000 ) ) ;
#54535=ORIENTED_EDGE ( 'NONE', *, *, #18194, .T. ) ;
#54537=ORIENTED_EDGE ( 'NONE', *, *, #15712, .T. ) ;
#54545=ORIENTED_EDGE ( 'NONE', *, *, #38285, .T. ) ;
#54552=EDGE_CURVE ( 'NONE', #52657, #34054, #40786, .T. ) ;
#54553=ORIENTED_EDGE ( 'NONE', *, *, #40958, .F. ) ;
#54559=DIRECTION ( 'NONE',  ( -1.000000000000000000, 0.000000000000000000, 0.000000000000000000 ) ) ;
#54571=ORIENTED_EDGE ( 'NONE', *, *, #63078, .F. ) ;
#54572=DIRECTION ( 'NONE',  ( 0.000000000000000000, -0.7046037717859445770, 0.7096009616573392131 ) ) ;
#54579=AXIS2_PLACEMENT_3D ( 'NONE', #47878, #63806, #63102 ) ;
#54582=CARTESIAN_POINT ( 'NONE',  ( 13.00000000000000178, -16.64230188589299786, 14.64519951917100116 ) ) ;
#54584=VERTEX_POINT ( 'NONE', #31450 ) ;
#54593=EDGE_CURVE ( 'NONE', #27508, #53596, #36740, .T. ) ;
#54595=DIRECTION ( 'NONE',  ( 1.000000000000000000, 0.000000000000000000, 0.000000000000000000 ) ) ;
#54601=ADVANCED_FACE ( 'NONE', ( #48039 ), #64479, .T. ) ;
#54603=LINE ( 'NONE', #27719, #65950 ) ;
#54610=CARTESIAN_POINT ( 'NONE',  ( 14.25000000000000000, -0.2038245569916330158, -21.77831216351300014 ) ) ;
#54614=CARTESIAN_POINT ( 'NONE',  ( 29.50000000000000355, -11.50000000000100009, 10.50000000000065903 ) ) ;
#54618=VERTEX_POINT ( 'NONE', #48391 ) ;
#54632=ORIENTED_EDGE ( 'NONE', *, *, #44149, .F. ) ;
#54636=CIRCLE ( 'NONE', #48983, 4.000000000000000888 ) ;
#54644=EDGE_CURVE ( 'NONE', #7139, #21874, #22719, .T. ) ;
#54648=ORIENTED_EDGE ( 'NONE', *, *, #14551, .T. ) ;
#54654=CARTESIAN_POINT ( 'NONE',  ( 30.00000000000000000, -11.70000000000000284, 12.50000000000000000 ) ) ;
#54657=PLANE ( 'NONE',  #64775 ) ;
#54663=AXIS2_PLACEMENT_3D ( 'NONE', #17822, #13552, #18493 ) ;
#54664=VERTEX_POINT ( 'NONE', #15535 ) ;
#54669=EDGE_CURVE ( 'NONE', #13935, #1121, #67840, .T. ) ;
#54672=AXIS2_PLACEMENT_3D ( 'NONE', #41094, #62312, #35434 ) ;
#54688=VECTOR ( 'NONE', #29455, 1000.000000000000000 ) ;
#54693=ORIENTED_EDGE ( 'NONE', *, *, #48686, .F. ) ;
#54698=DIRECTION ( 'NONE',  ( 0.000000000000000000, -0.7046037717806115097, -0.7096009616626348659 ) ) ;
#54699=ORIENTED_EDGE ( 'NONE', *, *, #64485, .T. ) ;
#54701=LINE ( 'NONE', #27829, #21101 ) ;
#54708=DIRECTION ( 'NONE',  ( 0.000000000000000000, 1.000000000000000000, 0.000000000000000000 ) ) ;
#54710=ORIENTED_EDGE ( 'NONE', *, *, #58978, .F. ) ;
#54712=LINE ( 'NONE', #48714, #2870 ) ;
#54714=AXIS2_PLACEMENT_3D ( 'NONE', #33650, #45282, #23730 ) ;
#54721=VECTOR ( 'NONE', #50639, 1000.000000000000000 ) ;
#54722=EDGE_CURVE ( 'NONE', #63841, #8038, #50919, .T. ) ;
#54737=DIRECTION ( 'NONE',  ( 0.000000000000000000, -1.000000000000000000, 0.000000000000000000 ) ) ;
#54759=DIRECTION ( 'NONE',  ( 0.000000000000000000, -1.000000000000000000, 0.000000000000000000 ) ) ;
#54762=ORIENTED_EDGE ( 'NONE', *, *, #11581, .F. ) ;
#54766=LINE ( 'NONE', #28230, #37053 ) ;
#54770=VECTOR ( 'NONE', #30869, 1000.000000000000000 ) ;
#54774=ORIENTED_EDGE ( 'NONE', *, *, #15378, .F. ) ;
#54782=EDGE_CURVE ( 'NONE', #11406, #67088, #16586, .T. ) ;
#54783=ORIENTED_EDGE ( 'NONE', *, *, #17444, .F. ) ;
#54792=ORIENTED_EDGE ( 'NONE', *, *, #16730, .F. ) ;
#54793=EDGE_CURVE ( 'NONE', #38888, #66296, #2368, .T. ) ;
#54797=ORIENTED_EDGE ( 'NONE', *, *, #505, .F. ) ;
#54800=CARTESIAN_POINT ( 'NONE',  ( 11.00000000000000000, -11.50000000000100009, -19.50000000000103739 ) ) ;
#54808=ORIENTED_EDGE ( 'NONE', *, *, #47533, .T. ) ;
#54812=AXIS2_PLACEMENT_3D ( 'NONE', #15500, #58627, #37411 ) ;
#54820=AXIS2_PLACEMENT_3D ( 'NONE', #67116, #2072, #2761 ) ;
#54823=ADVANCED_FACE ( 'NONE', ( #645 ), #1002, .F. ) ;
#54824=CARTESIAN_POINT ( 'NONE',  ( -16.74999999999999289, -0.3152037684892597946, -22.25410949791978510 ) ) ;
#54825=CARTESIAN_POINT ( 'NONE',  ( 16.75000000000000000, -0.2038245569916320166, 21.77831216351300014 ) ) ;
#54826=DIRECTION ( 'NONE',  ( 0.000000000000000000, 1.000000000000000000, 0.000000000000000000 ) ) ;
#54842=CARTESIAN_POINT ( 'NONE',  ( -15.50000000000129852, -17.50000000000000000, -22.50000000000000000 ) ) ;
#54849=PLANE ( 'NONE',  #44052 ) ;
#54851=AXIS2_PLACEMENT_3D ( 'NONE', #14007, #57150, #8718 ) ;
#54864=DIRECTION ( 'NONE',  ( 0.000000000000000000, -0.1249999999999996531, -0.9921567416492215186 ) ) ;
#54868=VECTOR ( 'NONE', #1262, 1000.000000000000114 ) ;
#54873=ADVANCED_FACE ( 'NONE', ( #4407 ), #46121, .F. ) ;
#54876=CIRCLE ( 'NONE', #16464, 0.3499999999998879008 ) ;
#54884=ORIENTED_EDGE ( 'NONE', *, *, #33756, .F. ) ;
#54886=ADVANCED_FACE ( 'NONE', ( #57076 ), #30913, .F. ) ;
#54887=ADVANCED_FACE ( 'NONE', ( #63794 ), #41519, .T. ) ;
#54889=CARTESIAN_POINT ( 'NONE',  ( -28.00000000000000000, -17.00000000000000000, -15.70499999999969809 ) ) ;
#54903=APPLICATION_CONTEXT ( 'automotive_design' ) ;
#54914=DIRECTION ( 'NONE',  ( -1.000000000000000000, 0.000000000000000000, 0.000000000000000000 ) ) ;
#54936=VERTEX_POINT ( 'NONE', #20644 ) ;
#54941=AXIS2_PLACEMENT_3D ( 'NONE', #52590, #36666, #8743 ) ;
#54960=DIRECTION ( 'NONE',  ( -1.000000000000000000, 0.000000000000000000, 0.000000000000000000 ) ) ;
#54965=CARTESIAN_POINT ( 'NONE',  ( 25.50000000000000355, -5.200000000000001066, -20.24999999999999645 ) ) ;
#54966=VECTOR ( 'NONE', #57723, 1000.000000000000000 ) ;
#54976=VECTOR ( 'NONE', #28134, 1000.000000000000114 ) ;
#54977=VECTOR ( 'NONE', #27532, 1000.000000000000000 ) ;
#54980=ORIENTED_EDGE ( 'NONE', *, *, #17616, .T. ) ;
#54982=CARTESIAN_POINT ( 'NONE',  ( -22.14589803375000088, -15.50000000000000000, -21.50000000000000000 ) ) ;
#54984=AXIS2_PLACEMENT_3D ( 'NONE', #58179, #46860, #20003 ) ;
#54985=ORIENTED_EDGE ( 'NONE', *, *, #25708, .T. ) ;
#54990=CARTESIAN_POINT ( 'NONE',  ( 15.50000000000000000, -1.037157890325000054, -22.50000000000000000 ) ) ;
#54994=LINE ( 'NONE', #1235, #35670 ) ;
#55001=CARTESIAN_POINT ( 'NONE',  ( 29.25000000000000000, -5.000000000000000000, 11.75000000000000000 ) ) ;
#55007=LINE ( 'NONE', #6558, #17574 ) ;
#55015=VECTOR ( 'NONE', #44783, 1000.000000000000000 ) ;
#55020=VECTOR ( 'NONE', #27372, 1000.000000000000000 ) ;
#55034=ADVANCED_FACE ( 'NONE', ( #42912 ), #52097, .F. ) ;
#55037=CARTESIAN_POINT ( 'NONE',  ( -25.50000000000000355, 0.000000000000000000, -24.12099999999999866 ) ) ;
#55039=CARTESIAN_POINT ( 'NONE',  ( -25.50000000000000355, -15.50000000000000000, 24.50000000000000000 ) ) ;
#55042=VECTOR ( 'NONE', #42034, 1000.000000000000000 ) ;
#55062=EDGE_LOOP ( 'NONE', ( #39312, #33661, #7900, #20072 ) ) ;
#55064=VERTEX_POINT ( 'NONE', #22047 ) ;
#55069=ORIENTED_EDGE ( 'NONE', *, *, #36771, .F. ) ;
#55076=EDGE_LOOP ( 'NONE', ( #61634, #60310, #31914, #31242, #44399, #65894 ) ) ;
#55088=ORIENTED_EDGE ( 'NONE', *, *, #45725, .T. ) ;
#55103=DIRECTION ( 'NONE',  ( 0.000000000000000000, 0.000000000000000000, 1.000000000000000000 ) ) ;
#55113=ORIENTED_EDGE ( 'NONE', *, *, #27013, .T. ) ;
#55120=AXIS2_PLACEMENT_3D ( 'NONE', #34489, #56080, #7630 ) ;
#55124=ORIENTED_EDGE ( 'NONE', *, *, #45019, .F. ) ;
#55125=LINE ( 'NONE', #66753, #45401 ) ;
#55126=ADVANCED_FACE ( 'NONE', ( #31624 ), #53201, .F. ) ;
#55127=ORIENTED_EDGE ( 'NONE', *, *, #28371, .F. ) ;
#55132=CARTESIAN_POINT ( 'NONE',  ( 11.00000000000000000, -9.487228132326899654, 12.50000000000000000 ) ) ;
#55135=CARTESIAN_POINT ( 'NONE',  ( -11.00000000000000000, -11.70000000000000284, -12.50000000000000000 ) ) ;
#55144=LINE ( 'NONE', #7373, #3179 ) ;
#55148=CYLINDRICAL_SURFACE ( 'NONE', #11981, 0.5000000000001357803 ) ;
#55152=CYLINDRICAL_SURFACE ( 'NONE', #63971, 0.4999999999991850963 ) ;
#55158=FACE_OUTER_BOUND ( 'NONE', #58538, .T. ) ;
#55162=EDGE_LOOP ( 'NONE', ( #45314, #17734 ) ) ;
#55166=CARTESIAN_POINT ( 'NONE',  ( 15.50000000000000000, -5.000000000000000000, 22.50000000000000000 ) ) ;
#55186=DIRECTION ( 'NONE',  ( 1.000000000000000000, 0.000000000000000000, 0.000000000000000000 ) ) ;
#55188=EDGE_CURVE ( 'NONE', #1760, #51933, #29080, .T. ) ;
#55194=EDGE_CURVE ( 'NONE', #23202, #4292, #39655, .T. ) ;
#55197=CARTESIAN_POINT ( 'NONE',  ( 24.00000000000000000, -16.28999999999710369, -14.50000000000000000 ) ) ;
#55199=FACE_OUTER_BOUND ( 'NONE', #24513, .T. ) ;
#55202=EDGE_CURVE ( 'NONE', #46144, #27925, #1861, .T. ) ;
#55204=DIRECTION ( 'NONE',  ( 0.000000000000000000, -0.7096009616570518874, -0.7046037717862339012 ) ) ;
#55205=VERTEX_POINT ( 'NONE', #44985 ) ;
#55219=ORIENTED_EDGE ( 'NONE', *, *, #15237, .F. ) ;
#55228=ORIENTED_EDGE ( 'NONE', *, *, #56051, .F. ) ;
#55233=ORIENTED_EDGE ( 'NONE', *, *, #27239, .T. ) ;
#55238=ORIENTED_EDGE ( 'NONE', *, *, #10860, .F. ) ;
#55244=CARTESIAN_POINT ( 'NONE',  ( 11.00000000000000000, -17.50000000000000000, -15.70500000000000007 ) ) ;
#55246=CARTESIAN_POINT ( 'NONE',  ( 11.00000000000000000, -11.50000000000000000, -15.00000000000000000 ) ) ;
#55251=EDGE_CURVE ( 'NONE', #34031, #68975, #53275, .T. ) ;
#55252=VERTEX_POINT ( 'NONE', #7842 ) ;
#55262=DIRECTION ( 'NONE',  ( 1.000000000000000000, -0.000000000000000000, -0.000000000000000000 ) ) ;
#55263=CIRCLE ( 'NONE', #45094, 0.4999999999991868727 ) ;
#55265=EDGE_CURVE ( 'NONE', #52459, #48929, #56646, .T. ) ;
#55271=CYLINDRICAL_SURFACE ( 'NONE', #18950, 4.000000000000000000 ) ;
#55275=ORIENTED_EDGE ( 'NONE', *, *, #29548, .F. ) ;
#55280=EDGE_CURVE ( 'NONE', #4772, #29478, #35774, .T. ) ;
#55281=DIRECTION ( 'NONE',  ( 0.000000000000000000, -0.1249999999999996531, -0.9921567416492215186 ) ) ;
#55282=AXIS2_PLACEMENT_3D ( 'NONE', #9478, #67825, #62867 ) ;
#55284=ORIENTED_EDGE ( 'NONE', *, *, #25524, .F. ) ;
#55302=VERTEX_POINT ( 'NONE', #63007 ) ;
#55332=EDGE_CURVE ( 'NONE', #59233, #30962, #68309, .T. ) ;
#55336=DIRECTION ( 'NONE',  ( 0.000000000000000000, 0.000000000000000000, 1.000000000000000000 ) ) ;
#55338=FACE_OUTER_BOUND ( 'NONE', #64821, .T. ) ;
#55340=VERTEX_POINT ( 'NONE', #14920 ) ;
#55345=VERTEX_POINT ( 'NONE', #19508 ) ;
#55349=EDGE_CURVE ( 'NONE', #24441, #611, #9619, .T. ) ;
#55351=CARTESIAN_POINT ( 'NONE',  ( -15.50000000000000000, -0.2000000000000000111, 19.20000000000052509 ) ) ;
#55358=DIRECTION ( 'NONE',  ( -1.000000000000000000, 0.000000000000000000, 0.000000000000000000 ) ) ;
#55369=CARTESIAN_POINT ( 'NONE',  ( -11.00000000000000000, -5.599999999999999645, 9.400000000000000355 ) ) ;
#55373=ORIENTED_EDGE ( 'NONE', *, *, #12831, .F. ) ;
#55378=ORIENTED_EDGE ( 'NONE', *, *, #52465, .T. ) ;
#55383=LINE ( 'NONE', #5557, #62783 ) ;
#55384=ORIENTED_EDGE ( 'NONE', *, *, #63152, .T. ) ;
#55392=ORIENTED_EDGE ( 'NONE', *, *, #63085, .T. ) ;
#55408=ORIENTED_EDGE ( 'NONE', *, *, #53948, .F. ) ;
#55415=FACE_OUTER_BOUND ( 'NONE', #24079, .T. ) ;
#55421=CARTESIAN_POINT ( 'NONE',  ( -23.75054448485400016, -15.50000000000000000, 25.53140320652400064 ) ) ;
#55427=AXIS2_PLACEMENT_3D ( 'NONE', #16906, #21858, #299 ) ;
#55436=CARTESIAN_POINT ( 'NONE',  ( -25.50000000000000355, -15.50000000000000000, 22.50000000000000000 ) ) ;
#55440=DIRECTION ( 'NONE',  ( 0.000000000000000000, -1.000000000000000000, -6.036837696397607468E-13 ) ) ;
#55441=ORIENTED_EDGE ( 'NONE', *, *, #62221, .F. ) ;
#55446=CARTESIAN_POINT ( 'NONE',  ( -23.75054448485400016, -15.50000000000000000, 25.53140320652400064 ) ) ;
#55452=LINE ( 'NONE', #27888, #9291 ) ;
#55465=DIRECTION ( 'NONE',  ( -1.000000000000000000, 0.000000000000000000, 0.000000000000000000 ) ) ;
#55466=ORIENTED_EDGE ( 'NONE', *, *, #5792, .T. ) ;
#55471=ORIENTED_EDGE ( 'NONE', *, *, #12040, .F. ) ;
#55476=EDGE_LOOP ( 'NONE', ( #28164, #7161, #43363, #25785 ) ) ;
#55490=ORIENTED_EDGE ( 'NONE', *, *, #13448, .T. ) ;
#55502=EDGE_CURVE ( 'NONE', #38480, #10983, #58658, .T. ) ;
#55511=DIRECTION ( 'NONE',  ( -1.000000000000000000, 0.000000000000000000, 0.000000000000000000 ) ) ;
#55517=DIRECTION ( 'NONE',  ( -1.000000000000000000, 0.000000000000000000, 0.000000000000000000 ) ) ;
#55518=DIRECTION ( 'NONE',  ( -1.000000000000000000, 0.000000000000000000, 0.000000000000000000 ) ) ;
#55520=DIRECTION ( 'NONE',  ( 0.000000000000000000, 0.000000000000000000, -1.000000000000000000 ) ) ;
#55529=DIRECTION ( 'NONE',  ( 1.000000000000000000, -0.000000000000000000, -0.000000000000000000 ) ) ;
#55531=CARTESIAN_POINT ( 'NONE',  ( 15.50000000000000000, -0.2000000000000000111, 22.50000000000000000 ) ) ;
#55537=ORIENTED_EDGE ( 'NONE', *, *, #19809, .T. ) ;
#55540=DIRECTION ( 'NONE',  ( 0.000000000000000000, 1.000000000000000000, 0.000000000000000000 ) ) ;
#55542=EDGE_CURVE ( 'NONE', #21874, #7139, #61151, .T. ) ;
#55555=DIRECTION ( 'NONE',  ( 0.000000000000000000, -1.000000000000000000, 0.000000000000000000 ) ) ;
#55558=CARTESIAN_POINT ( 'NONE',  ( -15.50000000000000000, -5.000000000000000000, -19.00000000000000000 ) ) ;
#55559=ORIENTED_EDGE ( 'NONE', *, *, #54593, .F. ) ;
#55561=VERTEX_POINT ( 'NONE', #65445 ) ;
#55565=DIRECTION ( 'NONE',  ( 1.000000000000000000, 0.000000000000000000, 0.000000000000000000 ) ) ;
#55576=VERTEX_POINT ( 'NONE', #22321 ) ;
#55578=CARTESIAN_POINT ( 'NONE',  ( -11.00000000000000000, -11.50000000000082068, -10.20500000000000007 ) ) ;
#55580=ADVANCED_FACE ( 'NONE', ( #6723 ), #18364, .T. ) ;
#55585=VERTEX_POINT ( 'NONE', #1093 ) ;
#55586=DIRECTION ( 'NONE',  ( 1.000000000000000000, 0.000000000000000000, 0.000000000000000000 ) ) ;
#55589=CARTESIAN_POINT ( 'NONE',  ( -25.50000000000000355, -5.200000000000001066, 22.50000000000000000 ) ) ;
#55590=CIRCLE ( 'NONE', #25108, 1.620999999999997332 ) ;
#55604=CARTESIAN_POINT ( 'NONE',  ( 28.00000000000000000, -17.50000000000000000, -20.05051025721700242 ) ) ;
#55605=DIRECTION ( 'NONE',  ( 0.000000000000000000, 0.000000000000000000, 1.000000000000000000 ) ) ;
#55606=CARTESIAN_POINT ( 'NONE',  ( 30.00000000000000000, -17.00000000000000000, -15.70499999999969809 ) ) ;
#55611=LINE ( 'NONE', #1871, #61251 ) ;
#55635=CARTESIAN_POINT ( 'NONE',  ( -15.50000000000000000, -5.000000000000000000, 22.50000000000000000 ) ) ;
#55640=ORIENTED_EDGE ( 'NONE', *, *, #9308, .F. ) ;
#55641=ORIENTED_EDGE ( 'NONE', *, *, #41838, .T. ) ;
#55642=EDGE_CURVE ( 'NONE', #22061, #39495, #39709, .T. ) ;
#55645=CARTESIAN_POINT ( 'NONE',  ( 25.50000000000000355, -5.200000000000001066, 24.75000000000000000 ) ) ;
#55653=ORIENTED_EDGE ( 'NONE', *, *, #35500, .F. ) ;
#55664=ADVANCED_FACE ( 'NONE', ( #55863 ), #7414, .F. ) ;
#55668=VECTOR ( 'NONE', #19779, 1000.000000000000000 ) ;
#55669=CIRCLE ( 'NONE', #64714, 4.000000000000000888 ) ;
#55672=CARTESIAN_POINT ( 'NONE',  ( 30.00000000000000000, -5.200000000000001066, 9.400000000000000355 ) ) ;
#55684=CARTESIAN_POINT ( 'NONE',  ( -11.00000000000000000, -15.46862696659690073, 14.50000000000000000 ) ) ;
#55694=DIRECTION ( 'NONE',  ( 0.000000000000000000, 0.000000000000000000, -1.000000000000000000 ) ) ;
#55712=DIRECTION ( 'NONE',  ( 1.000000000000000000, -0.000000000000000000, -0.000000000000000000 ) ) ;
#55716=AXIS2_PLACEMENT_3D ( 'NONE', #36956, #25990, #69114 ) ;
#55728=CARTESIAN_POINT ( 'NONE',  ( -30.00000000000000000, -8.959999999999999076, -17.04524521594300523 ) ) ;
#55739=EDGE_CURVE ( 'NONE', #2965, #35460, #36341, .T. ) ;
#55741=VERTEX_POINT ( 'NONE', #29677 ) ;
#55742=DIRECTION ( 'NONE',  ( -1.000000000000000000, 0.000000000000000000, 0.000000000000000000 ) ) ;
#55747=LINE ( 'NONE', #16885, #12516 ) ;
#55749=ORIENTED_EDGE ( 'NONE', *, *, #14152, .T. ) ;
#55761=DIRECTION ( 'NONE',  ( 0.000000000000000000, 1.000000000000000000, 0.000000000000000000 ) ) ;
#55762=VECTOR ( 'NONE', #17101, 1000.000000000000000 ) ;
#55766=DIRECTION ( 'NONE',  ( 1.000000000000000000, 0.000000000000000000, 0.000000000000000000 ) ) ;
#55772=DIRECTION ( 'NONE',  ( 0.000000000000000000, 0.000000000000000000, 1.000000000000000000 ) ) ;
#55773=DIRECTION ( 'NONE',  ( 0.000000000000000000, -0.7046037717859445770, 0.7096009616573392131 ) ) ;
#55778=CARTESIAN_POINT ( 'NONE',  ( 29.50000000000000355, -12.00000000000000000, -11.03137303340310282 ) ) ;
#55779=ORIENTED_EDGE ( 'NONE', *, *, #10655, .T. ) ;
#55792=LINE ( 'NONE', #51545, #68379 ) ;
#55798=AXIS2_PLACEMENT_3D ( 'NONE', #68933, #9538, #57269 ) ;
#55804=ORIENTED_EDGE ( 'NONE', *, *, #43537, .T. ) ;
#55805=EDGE_CURVE ( 'NONE', #9113, #27438, #10454, .T. ) ;
#55806=LINE ( 'NONE', #60755, #21709 ) ;
#55807=EDGE_LOOP ( 'NONE', ( #49795, #7305, #19144, #11631 ) ) ;
#55810=DIRECTION ( 'NONE',  ( 0.8660254037844482555, 0.000000000000000000, 0.4999999999999831801 ) ) ;
#55814=ORIENTED_EDGE ( 'NONE', *, *, #64453, .F. ) ;
#55818=AXIS2_PLACEMENT_3D ( 'NONE', #21699, #32654, #64490 ) ;
#55826=ORIENTED_EDGE ( 'NONE', *, *, #54722, .T. ) ;
#55828=DIRECTION ( 'NONE',  ( 1.000000000000000000, -0.000000000000000000, -0.000000000000000000 ) ) ;
#55840=CARTESIAN_POINT ( 'NONE',  ( -30.00000000000000000, -10.85999999999999943, 9.000000000000001776 ) ) ;
#55845=CARTESIAN_POINT ( 'NONE',  ( 29.50000000000000355, -11.50000000000000000, -15.00000000000000000 ) ) ;
#55847=DIRECTION ( 'NONE',  ( 0.000000000000000000, 0.7071067811865474617, -0.7071067811865474617 ) ) ;
#55859=AXIS2_PLACEMENT_3D ( 'NONE', #2893, #41428, #24477 ) ;
#55861=DIRECTION ( 'NONE',  ( 0.000000000000000000, 0.000000000000000000, 1.000000000000000000 ) ) ;
#55863=FACE_OUTER_BOUND ( 'NONE', #39739, .T. ) ;
#55864=VECTOR ( 'NONE', #65040, 1000.000000000000000 ) ;
#55871=VECTOR ( 'NONE', #1903, 1000.000000000000000 ) ;
#55875=CIRCLE ( 'NONE', #23114, 0.5000000000001386669 ) ;
#55889=EDGE_CURVE ( 'NONE', #7056, #67901, #44300, .T. ) ;
#55901=CARTESIAN_POINT ( 'NONE',  ( 30.00000000000000000, -11.50000000000000000, 19.00000000000000000 ) ) ;
#55915=AXIS2_PLACEMENT_3D ( 'NONE', #42698, #4530, #58270 ) ;
#55926=DIRECTION ( 'NONE',  ( 8.659560562354951347E-17, -0.7071067811865460184, 0.7071067811865489050 ) ) ;
#55928=ADVANCED_FACE ( 'NONE', ( #43429 ), #27371, .F. ) ;
#55929=EDGE_LOOP ( 'NONE', ( #57960, #41494, #63008, #24790, #48623, #25798, #26951, #63052 ) ) ;
#55933=CARTESIAN_POINT ( 'NONE',  ( -30.00000000000000000, -14.04000000000000092, -14.80000000000000071 ) ) ;
#55935=DIRECTION ( 'NONE',  ( 0.000000000000000000, -0.9921567416492215186, 0.1249999999999996531 ) ) ;
#55936=CARTESIAN_POINT ( 'NONE',  ( -28.00000000000000000, -15.50000000000000000, 20.05051025721700242 ) ) ;
#55943=LINE ( 'NONE', #50637, #7306 ) ;
#55950=VECTOR ( 'NONE', #12293, 1000.000000000000000 ) ;
#55960=FACE_BOUND ( 'NONE', #22931, .T. ) ;
#55968=CARTESIAN_POINT ( 'NONE',  ( 11.00000000000000000, -11.70000000000000284, -12.50000000000000000 ) ) ;
#55978=AXIS2_PLACEMENT_3D ( 'NONE', #5627, #1020, #16587 ) ;
#55984=EDGE_CURVE ( 'NONE', #41462, #1475, #1674, .T. ) ;
#55987=CARTESIAN_POINT ( 'NONE',  ( 30.00000000000000000, -11.10796162543699950, -9.102987789146602893 ) ) ;
#55994=DIRECTION ( 'NONE',  ( 0.000000000000000000, -0.9921567416492215186, 0.1249999999999996531 ) ) ;
#56027=CIRCLE ( 'NONE', #31219, 4.500000000000190958 ) ;
#56028=VERTEX_POINT ( 'NONE', #1345 ) ;
#56030=AXIS2_PLACEMENT_3D ( 'NONE', #20400, #68501, #25008 ) ;
#56032=DIRECTION ( 'NONE',  ( 0.000000000000000000, 0.000000000000000000, -1.000000000000000000 ) ) ;
#56042=ORIENTED_EDGE ( 'NONE', *, *, #5917, .F. ) ;
#56051=EDGE_CURVE ( 'NONE', #32857, #278, #1013, .T. ) ;
#56052=CARTESIAN_POINT ( 'NONE',  ( 25.50000000000000355, -15.50000000000000000, -20.49999999999999645 ) ) ;
#56058=CARTESIAN_POINT ( 'NONE',  ( 15.50000000000000000, -0.2038245569916610489, -23.94337567297399971 ) ) ;
#56059=ORIENTED_EDGE ( 'NONE', *, *, #35073, .T. ) ;
#56069=EDGE_CURVE ( 'NONE', #5667, #62784, #59703, .T. ) ;
#56071=AXIS2_PLACEMENT_3D ( 'NONE', #20885, #54467, #46446 ) ;
#56076=EDGE_CURVE ( 'NONE', #27235, #27455, #12643, .T. ) ;
#56080=DIRECTION ( 'NONE',  ( 0.000000000000000000, 1.000000000000000000, 0.000000000000000000 ) ) ;
#56084=DIRECTION ( 'NONE',  ( -0.000000000000000000, 1.000000000000000000, -0.000000000000000000 ) ) ;
#56091=EDGE_LOOP ( 'NONE', ( #69485, #56319, #9311, #33127 ) ) ;
#56093=CARTESIAN_POINT ( 'NONE',  ( 11.50000000000000000, -11.50000000000000000, -11.00000000000000000 ) ) ;
#56098=EDGE_CURVE ( 'NONE', #8072, #32931, #62455, .T. ) ;
#56102=CIRCLE ( 'NONE', #57268, 0.3499999999999285905 ) ;
#56122=ORIENTED_EDGE ( 'NONE', *, *, #14652, .T. ) ;
#56126=CARTESIAN_POINT ( 'NONE',  ( 29.50000000000000355, -11.50000000000000000, -19.00000000000000000 ) ) ;
#56135=DIRECTION ( 'NONE',  ( 1.000000000000000000, -0.000000000000000000, -0.000000000000000000 ) ) ;
#56136=EDGE_CURVE ( 'NONE', #41307, #21951, #18632, .T. ) ;
#56139=EDGE_CURVE ( 'NONE', #60418, #37432, #14030, .T. ) ;
#56143=DIRECTION ( 'NONE',  ( -1.000000000000000000, 0.000000000000000000, 0.000000000000000000 ) ) ;
#56144=CARTESIAN_POINT ( 'NONE',  ( 24.00000000000000000, -17.35230188589299871, 15.35019951917099945 ) ) ;
#56153=DIRECTION ( 'NONE',  ( 0.000000000000000000, 0.000000000000000000, -1.000000000000000000 ) ) ;
#56157=CARTESIAN_POINT ( 'NONE',  ( 29.50000000000000355, -11.50000000000000000, -15.00000000000000000 ) ) ;
#56160=CARTESIAN_POINT ( 'NONE',  ( -17.24945551514599984, -17.50000000000000000, 25.53140320652400064 ) ) ;
#56168=CARTESIAN_POINT ( 'NONE',  ( 25.49999999999869971, -17.50000000000000000, -22.50000000000000000 ) ) ;
#56179=DIRECTION ( 'NONE',  ( -0.000000000000000000, 1.000000000000000000, -0.000000000000000000 ) ) ;
#56189=FACE_OUTER_BOUND ( 'NONE', #65261, .T. ) ;
#56194=VECTOR ( 'NONE', #37629, 1000.000000000000000 ) ;
#56197=CARTESIAN_POINT ( 'NONE',  ( -15.50000000000000000, -0.2038245569916614930, 21.05662432702600029 ) ) ;
#56198=ORIENTED_EDGE ( 'NONE', *, *, #5868, .T. ) ;
#56208=ORIENTED_EDGE ( 'NONE', *, *, #64318, .F. ) ;
#56210=CARTESIAN_POINT ( 'NONE',  ( -30.00000000000000000, -17.50000000000000000, -15.70500000000000007 ) ) ;
#56216=CARTESIAN_POINT ( 'NONE',  ( 30.00000000000000000, -17.50000000000000000, 26.64999999999999858 ) ) ;
#56220=ORIENTED_EDGE ( 'NONE', *, *, #67508, .F. ) ;
#56232=DIRECTION ( 'NONE',  ( -0.9375000000000004441, 0.000000000000000000, -0.3479852726768752902 ) ) ;
#56235=CARTESIAN_POINT ( 'NONE',  ( 29.25000000000000000, -5.200000000000001066, 11.75000000000000000 ) ) ;
#56239=VERTEX_POINT ( 'NONE', #4494 ) ;
#56241=DIRECTION ( 'NONE',  ( 0.000000000000000000, 0.000000000000000000, 1.000000000000000000 ) ) ;
#56243=EDGE_LOOP ( 'NONE', ( #45804, #30044, #7715, #56059 ) ) ;
#56248=VECTOR ( 'NONE', #54160, 1000.000000000000000 ) ;
#56251=PLANE ( 'NONE',  #67133 ) ;
#56255=ORIENTED_EDGE ( 'NONE', *, *, #37787, .F. ) ;
#56257=ORIENTED_EDGE ( 'NONE', *, *, #34088, .T. ) ;
#56258=PLANE ( 'NONE',  #11789 ) ;
#56267=ORIENTED_EDGE ( 'NONE', *, *, #3089, .F. ) ;
#56271=AXIS2_PLACEMENT_3D ( 'NONE', #55606, #39675, #29081 ) ;
#56284=EDGE_CURVE ( 'NONE', #38291, #50590, #58927, .T. ) ;
#56287=EDGE_CURVE ( 'NONE', #43516, #41912, #52244, .T. ) ;
#56288=EDGE_CURVE ( 'NONE', #33465, #14877, #46575, .T. ) ;
#56292=LINE ( 'NONE', #50984, #66066 ) ;
#56311=ORIENTED_EDGE ( 'NONE', *, *, #65856, .T. ) ;
#56315=VERTEX_POINT ( 'NONE', #20739 ) ;
#56319=ORIENTED_EDGE ( 'NONE', *, *, #67947, .T. ) ;
#56329=CARTESIAN_POINT ( 'NONE',  ( -16.75000000000000000, -2.500000000000000000, -21.77831216351300014 ) ) ;
#56342=( NAMED_UNIT ( * ) SI_UNIT ( $, .STERADIAN. ) SOLID_ANGLE_UNIT ( ) );
#56353=FACE_OUTER_BOUND ( 'NONE', #63505, .T. ) ;
#56357=AXIS2_PLACEMENT_3D ( 'NONE', #20940, #10000, #69382 ) ;
#56364=VECTOR ( 'NONE', #29411, 1000.000000000000000 ) ;
#56365=DIRECTION ( 'NONE',  ( 1.000000000000000000, -0.000000000000000000, -0.000000000000000000 ) ) ;
#56370=ORIENTED_EDGE ( 'NONE', *, *, #16469, .T. ) ;
#56374=DIRECTION ( 'NONE',  ( -1.000000000000000000, 0.000000000000000000, 0.000000000000000000 ) ) ;
#56378=AXIS2_PLACEMENT_3D ( 'NONE', #41765, #63350, #69343 ) ;
#56383=CARTESIAN_POINT ( 'NONE',  ( 15.50000000000000000, -1.037157890325000054, 22.50000000000000000 ) ) ;
#56384=FACE_OUTER_BOUND ( 'NONE', #36917, .T. ) ;
#56396=DIRECTION ( 'NONE',  ( 8.659560562354951347E-17, -0.7071067811865460184, 0.7071067811865489050 ) ) ;
#56398=CARTESIAN_POINT ( 'NONE',  ( 13.00000000000000178, -17.50000000000000000, 20.05051025721700242 ) ) ;
#56403=CIRCLE ( 'NONE', #25950, 4.000000000000000888 ) ;
#56422=EDGE_LOOP ( 'NONE', ( #68621, #61963, #67572, #57526 ) ) ;
#56434=CARTESIAN_POINT ( 'NONE',  ( 30.00000000000000000, -17.00000000000000000, -15.70499999999969809 ) ) ;
#56439=DIRECTION ( 'NONE',  ( 0.000000000000000000, 0.000000000000000000, -1.000000000000000000 ) ) ;
#56443=VECTOR ( 'NONE', #49094, 1000.000000000000000 ) ;
#56447=EDGE_CURVE ( 'NONE', #38888, #60780, #6903, .T. ) ;
#56457=EDGE_CURVE ( 'NONE', #69443, #49539, #26306, .T. ) ;
#56459=DIRECTION ( 'NONE',  ( 1.000000000000000000, -0.000000000000000000, -0.000000000000000000 ) ) ;
#56462=CARTESIAN_POINT ( 'NONE',  ( -25.50000000000000355, -5.200000000000001066, -22.50000000000000000 ) ) ;
#56466=DIRECTION ( 'NONE',  ( 0.000000000000000000, 0.000000000000000000, 1.000000000000000000 ) ) ;
#56469=VECTOR ( 'NONE', #11417, 1000.000000000000000 ) ;
#56470=VECTOR ( 'NONE', #48702, 1000.000000000000000 ) ;
#56472=VERTEX_POINT ( 'NONE', #6579 ) ;
#56489=ORIENTED_EDGE ( 'NONE', *, *, #22999, .T. ) ;
#56490=EDGE_CURVE ( 'NONE', #65734, #8948, #11508, .T. ) ;
#56495=ORIENTED_EDGE ( 'NONE', *, *, #10964, .T. ) ;
#56498=ORIENTED_EDGE ( 'NONE', *, *, #41030, .F. ) ;
#56501=LINE ( 'NONE', #25039, #45974 ) ;
#56507=FACE_OUTER_BOUND ( 'NONE', #19653, .T. ) ;
#56518=CARTESIAN_POINT ( 'NONE',  ( 30.00000000000000000, -12.00000000000000000, -11.03137303340310282 ) ) ;
#56519=CARTESIAN_POINT ( 'NONE',  ( -28.00000000000000000, -15.50000000000000000, -20.05051025721700242 ) ) ;
#56521=EDGE_CURVE ( 'NONE', #25535, #1031, #3351, .T. ) ;
#56524=VECTOR ( 'NONE', #13910, 1000.000000000000000 ) ;
#56539=DIRECTION ( 'NONE',  ( 0.000000000000000000, 0.000000000000000000, 1.000000000000000000 ) ) ;
#56542=CARTESIAN_POINT ( 'NONE',  ( -11.00000000000000000, -11.50000000000082068, 10.20500000000000007 ) ) ;
#56548=ORIENTED_EDGE ( 'NONE', *, *, #22999, .F. ) ;
#56549=CARTESIAN_POINT ( 'NONE',  ( -15.50000000000000000, -5.000000000000000000, -22.50000000000000000 ) ) ;
#56553=EDGE_CURVE ( 'NONE', #50555, #12586, #8654, .T. ) ;
#56554=DIRECTION ( 'NONE',  ( 1.000000000000000000, 0.000000000000000000, 0.000000000000000000 ) ) ;
#56557=CIRCLE ( 'NONE', #45236, 0.5000000000079362072 ) ;
#56566=EDGE_LOOP ( 'NONE', ( #25675, #30597, #57152, #54762, #34826, #53095 ) ) ;
#56569=CARTESIAN_POINT ( 'NONE',  ( 30.00000000000000000, -16.28999999999710369, -15.00000000000794920 ) ) ;
#56578=EDGE_CURVE ( 'NONE', #122, #52042, #46479, .T. ) ;
#56583=LINE ( 'NONE', #8132, #62318 ) ;
#56598=DIRECTION ( 'NONE',  ( 1.000000000000000000, -0.000000000000000000, -0.000000000000000000 ) ) ;
#56606=AXIS2_PLACEMENT_3D ( 'NONE', #64820, #16733, #26991 ) ;
#56607=VERTEX_POINT ( 'NONE', #62381 ) ;
#56621=EDGE_LOOP ( 'NONE', ( #16008, #20627, #35393, #1076 ) ) ;
#56625=CARTESIAN_POINT ( 'NONE',  ( -30.00000000000000000, -12.00000000000000000, 11.03137303340310282 ) ) ;
#56628=VECTOR ( 'NONE', #3608, 1000.000000000000000 ) ;
#56632=CARTESIAN_POINT ( 'NONE',  ( -24.00000000000000000, -17.50000000000000000, 15.70499999999969809 ) ) ;
#56636=EDGE_CURVE ( 'NONE', #40609, #13055, #770, .T. ) ;
#56640=EDGE_CURVE ( 'NONE', #55340, #32467, #9357, .T. ) ;
#56642=PLANE ( 'NONE',  #60303 ) ;
#56646=LINE ( 'NONE', #67611, #5825 ) ;
#56647=CARTESIAN_POINT ( 'NONE',  ( -11.00000000000000000, -13.54524521594299991, -17.53999999999999915 ) ) ;
#56649=CARTESIAN_POINT ( 'NONE',  ( 11.50000000000000000, -11.50000000000100009, -19.50000000000103739 ) ) ;
#56651=PLANE ( 'NONE',  #43788 ) ;
#56657=DIRECTION ( 'NONE',  ( -0.000000000000000000, 1.000000000000000000, -0.000000000000000000 ) ) ;
#56661=FACE_BOUND ( 'NONE', #15607, .T. ) ;
#56664=VECTOR ( 'NONE', #69829, 1000.000000000000000 ) ;
#56679=AXIS2_PLACEMENT_3D ( 'NONE', #28988, #51249, #47003 ) ;
#56681=DIRECTION ( 'NONE',  ( 0.000000000000000000, 0.000000000000000000, 1.000000000000000000 ) ) ;
#56682=EDGE_CURVE ( 'NONE', #60969, #14935, #25189, .T. ) ;
#56688=CARTESIAN_POINT ( 'NONE',  ( 15.50000000000000000, -5.000000000000000000, 19.00000000000000000 ) ) ;
#56692=CARTESIAN_POINT ( 'NONE',  ( -16.75000000000000000, -0.2038245569916330158, 23.22168783648699986 ) ) ;
#56696=LINE ( 'NONE', #44676, #11365 ) ;
#56707=EDGE_LOOP ( 'NONE', ( #3159, #16536, #59893, #20971 ) ) ;
#56723=CIRCLE ( 'NONE', #35296, 4.500000000000191847 ) ;
#56736=DIRECTION ( 'NONE',  ( 0.000000000000000000, -0.9921567416492215186, 0.1249999999999996531 ) ) ;
#56737=CARTESIAN_POINT ( 'NONE',  ( 11.00000000000000000, -9.199999999999999289, 12.69999999999986073 ) ) ;
#56741=VERTEX_POINT ( 'NONE', #41534 ) ;
#56742=CARTESIAN_POINT ( 'NONE',  ( -30.00000000000000000, -17.14999999999900027, -26.64999999999900027 ) ) ;
#56743=DIRECTION ( 'NONE',  ( -1.000000000000000000, 0.000000000000000000, 0.000000000000000000 ) ) ;
#56744=VECTOR ( 'NONE', #61334, 1000.000000000000000 ) ;
#56752=EDGE_CURVE ( 'NONE', #22939, #64180, #9394, .T. ) ;
#56759=ORIENTED_EDGE ( 'NONE', *, *, #23652, .T. ) ;
#56760=EDGE_LOOP ( 'NONE', ( #69368, #55559, #69012, #53339 ) ) ;
#56771=CARTESIAN_POINT ( 'NONE',  ( 14.25000000000000000, -2.500000000000000000, 23.22168783648699986 ) ) ;
#56772=VECTOR ( 'NONE', #29165, 1000.000000000000000 ) ;
#56778=FACE_OUTER_BOUND ( 'NONE', #37282, .T. ) ;
#56781=ORIENTED_EDGE ( 'NONE', *, *, #68623, .F. ) ;
#56786=ORIENTED_EDGE ( 'NONE', *, *, #4275, .T. ) ;
#56792=LINE ( 'NONE', #66708, #25474 ) ;
#56819=DIRECTION ( 'NONE',  ( 0.000000000000000000, 0.000000000000000000, -1.000000000000000000 ) ) ;
#56825=LINE ( 'NONE', #24662, #18400 ) ;
#56834=AXIS2_PLACEMENT_3D ( 'NONE', #48508, #20927, #27629 ) ;
#56842=ADVANCED_FACE ( 'NONE', ( #45253 ), #60137, .T. ) ;
#56851=CARTESIAN_POINT ( 'NONE',  ( 24.00000000000000000, -17.00000000000000000, 15.70499999999969809 ) ) ;
#56863=VECTOR ( 'NONE', #18025, 1000.000000000000000 ) ;
#56873=CARTESIAN_POINT ( 'NONE',  ( 30.00000000000000000, -5.000000000000000000, -11.75000000000000000 ) ) ;
#56874=CARTESIAN_POINT ( 'NONE',  ( 11.00000000000000000, -14.33999999999999986, 14.50000000000000000 ) ) ;
#56878=CARTESIAN_POINT ( 'NONE',  ( -30.00000000000000000, -9.200000000000120082, 17.30000000000000071 ) ) ;
#56881=ORIENTED_EDGE ( 'NONE', *, *, #4156, .F. ) ;
#56887=DIRECTION ( 'NONE',  ( 1.000000000000000000, -0.000000000000000000, -0.000000000000000000 ) ) ;
#56890=LINE ( 'NONE', #18354, #57220 ) ;
#56895=PLANE ( 'NONE',  #3060 ) ;
#56902=ORIENTED_EDGE ( 'NONE', *, *, #69231, .F. ) ;
#56908=AXIS2_PLACEMENT_3D ( 'NONE', #47355, #68928, #42401 ) ;
#56910=ORIENTED_EDGE ( 'NONE', *, *, #9244, .F. ) ;
#56912=ORIENTED_EDGE ( 'NONE', *, *, #48999, .T. ) ;
#56919=EDGE_CURVE ( 'NONE', #31900, #67199, #57274, .T. ) ;
#56926=ORIENTED_EDGE ( 'NONE', *, *, #62437, .T. ) ;
#56934=VERTEX_POINT ( 'NONE', #62933 ) ;
#56938=CARTESIAN_POINT ( 'NONE',  ( -16.75000000000000000, -0.2038245569916330158, 23.22168783648699986 ) ) ;
#56944=EDGE_CURVE ( 'NONE', #68720, #50148, #68937, .T. ) ;
#56945=CYLINDRICAL_SURFACE ( 'NONE', #33264, 4.500000000000188294 ) ;
#56957=PLANE ( 'NONE',  #5706 ) ;
#56958=ORIENTED_EDGE ( 'NONE', *, *, #13885, .T. ) ;
#56959=VECTOR ( 'NONE', #36575, 1000.000000000000000 ) ;
#56971=EDGE_CURVE ( 'NONE', #47849, #20965, #60207, .T. ) ;
#56973=VECTOR ( 'NONE', #48001, 1000.000000000000000 ) ;
#56974=DIRECTION ( 'NONE',  ( 0.000000000000000000, 0.000000000000000000, 1.000000000000000000 ) ) ;
#56977=EDGE_CURVE ( 'NONE', #9070, #69553, #52689, .T. ) ;
#56983=CARTESIAN_POINT ( 'NONE',  ( 29.25000000000000000, -5.200000000000001066, -26.25000000000000000 ) ) ;
#56992=ORIENTED_EDGE ( 'NONE', *, *, #41468, .F. ) ;
#56993=DIRECTION ( 'NONE',  ( -1.000000000000000000, 0.000000000000000000, 0.000000000000000000 ) ) ;
#56997=CARTESIAN_POINT ( 'NONE',  ( 30.00000000000000000, -13.54524521594299991, 17.53999999999999915 ) ) ;
#56999=EDGE_CURVE ( 'NONE', #22725, #19628, #12740, .T. ) ;
#57001=ORIENTED_EDGE ( 'NONE', *, *, #15594, .F. ) ;
#57003=CARTESIAN_POINT ( 'NONE',  ( 30.00000000000000000, -17.14999999999900027, -26.64999999999900027 ) ) ;
#57014=CARTESIAN_POINT ( 'NONE',  ( 30.00000000000000000, -5.200000000000001066, 26.59999999999999787 ) ) ;
#57021=LINE ( 'NONE', #8582, #54966 ) ;
#57022=AXIS2_PLACEMENT_3D ( 'NONE', #29716, #52354, #67202 ) ;
#57029=EDGE_LOOP ( 'NONE', ( #69363, #45029, #69081, #9466 ) ) ;
#57042=CARTESIAN_POINT ( 'NONE',  ( -30.00000000000000000, -16.28999999999710369, -15.00000000000794920 ) ) ;
#57055=CARTESIAN_POINT ( 'NONE',  ( -17.00000000000000000, -16.28999999999710369, -15.00000000000794920 ) ) ;
#57060=VECTOR ( 'NONE', #61081, 1000.000000000000000 ) ;
#57063=CARTESIAN_POINT ( 'NONE',  ( 11.00000000000000000, -5.200000000000001066, 9.400000000000000355 ) ) ;
#57074=DIRECTION ( 'NONE',  ( 0.000000000000000000, 0.000000000000000000, -1.000000000000000000 ) ) ;
#57075=EDGE_CURVE ( 'NONE', #39920, #18785, #34244, .T. ) ;
#57076=FACE_OUTER_BOUND ( 'NONE', #61129, .T. ) ;
#57090=CARTESIAN_POINT ( 'NONE',  ( -29.50000000000000355, -11.50000000000000000, -15.00000000000000000 ) ) ;
#57096=DIRECTION ( 'NONE',  ( 1.000000000000000000, -0.000000000000000000, -0.000000000000000000 ) ) ;
#57098=CARTESIAN_POINT ( 'NONE',  ( 29.50000000000000355, -11.50000000000000000, -19.00000000000000000 ) ) ;
#57101=CARTESIAN_POINT ( 'NONE',  ( -29.50000000000000355, -11.50000000000100009, 15.00000000000084910 ) ) ;
#57104=EDGE_LOOP ( 'NONE', ( #16893, #56489, #11437, #11322 ) ) ;
#57112=VERTEX_POINT ( 'NONE', #53038 ) ;
#57114=ORIENTED_EDGE ( 'NONE', *, *, #39815, .F. ) ;
#57117=ADVANCED_FACE ( 'NONE', ( #32150 ), #10931, .F. ) ;
#57128=CYLINDRICAL_SURFACE ( 'NONE', #5676, 0.5000000000001374456 ) ;
#57131=ORIENTED_EDGE ( 'NONE', *, *, #41069, .T. ) ;
#57136=CARTESIAN_POINT ( 'NONE',  ( 30.00000000000000000, -8.959999999999999076, 17.04524521594300523 ) ) ;
#57145=EDGE_LOOP ( 'NONE', ( #62769, #47984, #60179, #31593 ) ) ;
#57147=CARTESIAN_POINT ( 'NONE',  ( -15.50000000000129852, -15.50000000000000000, -22.50000000000000000 ) ) ;
#57150=DIRECTION ( 'NONE',  ( -0.000000000000000000, 1.000000000000000000, -0.000000000000000000 ) ) ;
#57152=ORIENTED_EDGE ( 'NONE', *, *, #27796, .T. ) ;
#57161=VECTOR ( 'NONE', #3358, 1000.000000000000000 ) ;
#57162=LINE ( 'NONE', #3083, #63619 ) ;
#57164=ORIENTED_EDGE ( 'NONE', *, *, #22784, .T. ) ;
#57167=CYLINDRICAL_SURFACE ( 'NONE', #30475, 4.000000000000000000 ) ;
#57175=DIRECTION ( 'NONE',  ( 0.000000000000000000, 0.000000000000000000, -1.000000000000000000 ) ) ;
#57186=CARTESIAN_POINT ( 'NONE',  ( -17.00000000000000000, -17.00000000000000000, -15.70499999999969809 ) ) ;
#57202=ORIENTED_EDGE ( 'NONE', *, *, #55542, .T. ) ;
#57211=EDGE_CURVE ( 'NONE', #28902, #21463, #51216, .T. ) ;
#57220=VECTOR ( 'NONE', #17682, 1000.000000000000000 ) ;
#57222=DIRECTION ( 'NONE',  ( 0.000000000000000000, 1.000000000000000000, 0.000000000000000000 ) ) ;
#57226=LINE ( 'NONE', #25054, #68705 ) ;
#57228=VERTEX_POINT ( 'NONE', #60057 ) ;
#57233=VERTEX_POINT ( 'NONE', #65378 ) ;
#57234=DIRECTION ( 'NONE',  ( -1.000000000000000000, 0.000000000000000000, 0.000000000000000000 ) ) ;
#57241=CARTESIAN_POINT ( 'NONE',  ( -25.50000000000000355, -5.578999999999999737, -20.87899999999999778 ) ) ;
#57245=EDGE_LOOP ( 'NONE', ( #69229, #53732, #19285, #7702, #7540, #61296, #11117, #43728, #63749, #44202, #34071 ) ) ;
#57250=DIRECTION ( 'NONE',  ( 0.000000000000000000, 0.000000000000000000, 1.000000000000000000 ) ) ;
#57256=DIRECTION ( 'NONE',  ( 0.000000000000000000, -1.000000000000000000, 0.000000000000000000 ) ) ;
#57263=ORIENTED_EDGE ( 'NONE', *, *, #35365, .F. ) ;
#57265=DIRECTION ( 'NONE',  ( 0.000000000000000000, 1.000000000000000000, 0.000000000000000000 ) ) ;
#57268=AXIS2_PLACEMENT_3D ( 'NONE', #56878, #58300, #9503 ) ;
#57269=DIRECTION ( 'NONE',  ( 0.000000000000000000, -0.7046037717806115097, -0.7096009616626348659 ) ) ;
#57270=DIRECTION ( 'NONE',  ( 1.000000000000000000, 0.000000000000000000, 0.000000000000000000 ) ) ;
#57272=AXIS2_PLACEMENT_3D ( 'NONE', #57003, #52061, #18126 ) ;
#57274=LINE ( 'NONE', #24749, #50056 ) ;
#57276=ORIENTED_EDGE ( 'NONE', *, *, #156, .F. ) ;
#57279=DIRECTION ( 'NONE',  ( 0.000000000000000000, 0.7084617869628681008, 0.7057491738665939707 ) ) ;
#57283=CIRCLE ( 'NONE', #53925, 4.500000000000190958 ) ;
#57288=CARTESIAN_POINT ( 'NONE',  ( 29.50000000000000355, -11.50000000000000000, 15.00000000000000000 ) ) ;
#57291=AXIS2_PLACEMENT_3D ( 'NONE', #44889, #62193, #13756 ) ;
#57297=CARTESIAN_POINT ( 'NONE',  ( -30.00000000000000000, -16.64230188589299786, 14.64519951917100116 ) ) ;
#57299=CARTESIAN_POINT ( 'NONE',  ( 11.00000000000000000, -9.454754784057099570, -17.53999999999999915 ) ) ;
#57316=CIRCLE ( 'NONE', #49411, 3.499999999999855227 ) ;
#57327=VERTEX_POINT ( 'NONE', #12290 ) ;
#57330=VECTOR ( 'NONE', #27006, 1000.000000000000000 ) ;
#57345=EDGE_CURVE ( 'NONE', #41911, #27132, #61421, .T. ) ;
#57349=CARTESIAN_POINT ( 'NONE',  ( -25.50000000000000355, -15.50000000000000000, 22.50000000000000000 ) ) ;
#57352=EDGE_CURVE ( 'NONE', #9744, #33676, #55452, .T. ) ;
#57358=CARTESIAN_POINT ( 'NONE',  ( -11.50000000000000000, -11.70000000000000284, -11.00000000000000000 ) ) ;
#57369=FACE_OUTER_BOUND ( 'NONE', #33717, .T. ) ;
#57372=VECTOR ( 'NONE', #21547, 1000.000000000000000 ) ;
#57374=CARTESIAN_POINT ( 'NONE',  ( -11.50000000000000000, -15.46862696659690073, -14.50000000000000000 ) ) ;
#57375=DIRECTION ( 'NONE',  ( 0.9583148474998870459, 0.000000000000000000, -0.2857142857143623593 ) ) ;
#57381=DIRECTION ( 'NONE',  ( -1.000000000000000000, 0.000000000000000000, 0.000000000000000000 ) ) ;
#57394=ORIENTED_EDGE ( 'NONE', *, *, #39265, .T. ) ;
#57403=CARTESIAN_POINT ( 'NONE',  ( 30.00000000000000000, -11.85423089348099879, -9.852125413066602277 ) ) ;
#57411=VERTEX_POINT ( 'NONE', #46222 ) ;
#57412=EDGE_CURVE ( 'NONE', #34054, #1375, #40915, .T. ) ;
#57413=ORIENTED_EDGE ( 'NONE', *, *, #60056, .F. ) ;
#57419=DIRECTION ( 'NONE',  ( 0.000000000000000000, -0.8206518066484758123, 0.5714285714283042772 ) ) ;
#57423=EDGE_CURVE ( 'NONE', #15308, #47849, #56723, .T. ) ;
#57427=ORIENTED_EDGE ( 'NONE', *, *, #57352, .T. ) ;
#57428=CARTESIAN_POINT ( 'NONE',  ( 11.00000000000000000, -8.959999999999999076, -17.04524521594300523 ) ) ;
#57433=EDGE_LOOP ( 'NONE', ( #30541, #13549, #51343, #39532 ) ) ;
#57436=DIRECTION ( 'NONE',  ( 0.000000000000000000, 1.000000000000000000, 0.000000000000000000 ) ) ;
#57441=CARTESIAN_POINT ( 'NONE',  ( 30.00000000000000000, -10.85999999999999943, 9.000000000000001776 ) ) ;
#57454=CARTESIAN_POINT ( 'NONE',  ( 30.00000000000000000, -14.33999999999999986, -14.50000000000000000 ) ) ;
#57461=AXIS2_PLACEMENT_3D ( 'NONE', #30260, #63836, #51822 ) ;
#57462=EDGE_CURVE ( 'NONE', #41126, #36987, #52236, .T. ) ;
#57463=EDGE_LOOP ( 'NONE', ( #21313, #50127, #5191, #53436, #3216, #16409, #18166, #57719 ) ) ;
#57474=VECTOR ( 'NONE', #29072, 1000.000000000000000 ) ;
#57481=VERTEX_POINT ( 'NONE', #62400 ) ;
#57485=ORIENTED_EDGE ( 'NONE', *, *, #16469, .F. ) ;
#57491=ORIENTED_EDGE ( 'NONE', *, *, #30593, .F. ) ;
#57498=DIRECTION ( 'NONE',  ( -1.000000000000000000, 0.000000000000000000, 0.000000000000000000 ) ) ;
#57511=LINE ( 'NONE', #52938, #53169 ) ;
#57518=DIRECTION ( 'NONE',  ( -1.000000000000000000, 0.000000000000000000, 0.000000000000000000 ) ) ;
#57526=ORIENTED_EDGE ( 'NONE', *, *, #27543, .F. ) ;
#57540=DIRECTION ( 'NONE',  ( 0.000000000000000000, 0.000000000000000000, 1.000000000000000000 ) ) ;
#57543=ORIENTED_EDGE ( 'NONE', *, *, #18125, .F. ) ;
#57554=AXIS2_PLACEMENT_3D ( 'NONE', #24077, #13469, #51661 ) ;
#57560=ORIENTED_EDGE ( 'NONE', *, *, #23491, .F. ) ;
#57574=FACE_OUTER_BOUND ( 'NONE', #28608, .T. ) ;
#57577=VERTEX_POINT ( 'NONE', #38682 ) ;
#57587=AXIS2_PLACEMENT_3D ( 'NONE', #17785, #56657, #66568 ) ;
#57596=CIRCLE ( 'NONE', #63257, 4.000000000000000000 ) ;
#57603=FACE_OUTER_BOUND ( 'NONE', #9229, .T. ) ;
#57605=CARTESIAN_POINT ( 'NONE',  ( 30.00000000000000000, -17.50000000000000000, -15.70500000000000007 ) ) ;
#57609=VECTOR ( 'NONE', #23556, 1000.000000000000000 ) ;
#57618=VERTEX_POINT ( 'NONE', #53231 ) ;
#57628=ORIENTED_EDGE ( 'NONE', *, *, #47893, .T. ) ;
#57629=VERTEX_POINT ( 'NONE', #69827 ) ;
#57633=DIRECTION ( 'NONE',  ( 0.000000000000000000, 1.000000000000000000, 0.000000000000000000 ) ) ;
#57639=ORIENTED_EDGE ( 'NONE', *, *, #14774, .F. ) ;
#57643=CARTESIAN_POINT ( 'NONE',  ( 25.50000000000000355, -5.200000000000001066, -22.50000000000000000 ) ) ;
#57644=DIRECTION ( 'NONE',  ( 0.000000000000000000, 0.000000000000000000, 1.000000000000000000 ) ) ;
#57647=AXIS2_PLACEMENT_3D ( 'NONE', #2797, #56887, #24376 ) ;
#57655=EDGE_CURVE ( 'NONE', #34366, #26875, #38708, .T. ) ;
#57660=CIRCLE ( 'NONE', #27186, 0.5000000000001362244 ) ;
#57665=ORIENTED_EDGE ( 'NONE', *, *, #26372, .T. ) ;
#57666=EDGE_LOOP ( 'NONE', ( #40691, #1220, #64630, #29331, #58035, #40271, #9238, #49935 ) ) ;
#57667=PLANE ( 'NONE',  #39810 ) ;
#57677=ORIENTED_EDGE ( 'NONE', *, *, #32474, .F. ) ;
#57681=DIRECTION ( 'NONE',  ( -1.000000000000000000, 0.000000000000000000, 0.000000000000000000 ) ) ;
#57683=CIRCLE ( 'NONE', #48656, 0.5000000000001386669 ) ;
#57685=DIRECTION ( 'NONE',  ( 0.000000000000000000, 0.7057491738665943037, -0.7084617869628675457 ) ) ;
#57686=VERTEX_POINT ( 'NONE', #42600 ) ;
#57695=ADVANCED_FACE ( 'NONE', ( #16776 ), #49949, .F. ) ;
#57696=AXIS2_PLACEMENT_3D ( 'NONE', #26834, #14821, #37782 ) ;
#57706=AXIS2_PLACEMENT_3D ( 'NONE', #49748, #982, #7291 ) ;
#57713=CARTESIAN_POINT ( 'NONE',  ( -30.00000000000000000, -5.599999999999999645, -9.400000000000000355 ) ) ;
#57717=CIRCLE ( 'NONE', #9170, 4.000000000000000888 ) ;
#57719=ORIENTED_EDGE ( 'NONE', *, *, #45588, .T. ) ;
#57723=DIRECTION ( 'NONE',  ( -1.000000000000000000, 0.000000000000000000, 0.000000000000000000 ) ) ;
#57731=ORIENTED_EDGE ( 'NONE', *, *, #10270, .F. ) ;
#57732=AXIS2_PLACEMENT_3D ( 'NONE', #58070, #31221, #25557 ) ;
#57735=FACE_OUTER_BOUND ( 'NONE', #67738, .T. ) ;
#57742=ORIENTED_EDGE ( 'NONE', *, *, #60020, .T. ) ;
#57745=AXIS2_PLACEMENT_3D ( 'NONE', #50642, #55262, #55605 ) ;
#57757=ORIENTED_EDGE ( 'NONE', *, *, #15449, .F. ) ;
#57758=ADVANCED_FACE ( 'NONE', ( #34753, #29451 ), #12824, .F. ) ;
#57760=FACE_OUTER_BOUND ( 'NONE', #46555, .T. ) ;
#57764=ORIENTED_EDGE ( 'NONE', *, *, #2853, .F. ) ;
#57766=DIRECTION ( 'NONE',  ( -1.000000000000000000, 0.000000000000000000, 0.000000000000000000 ) ) ;
#57773=DIRECTION ( 'NONE',  ( 0.000000000000000000, 0.000000000000000000, -1.000000000000000000 ) ) ;
#57774=VECTOR ( 'NONE', #34615, 1000.000000000000000 ) ;
#57784=DIRECTION ( 'NONE',  ( 0.000000000000000000, 1.000000000000000000, 0.000000000000000000 ) ) ;
#57787=PLANE ( 'NONE',  #20293 ) ;
#57797=DIRECTION ( 'NONE',  ( 0.000000000000000000, -2.854859206170826497E-12, -1.000000000000000000 ) ) ;
#57799=EDGE_CURVE ( 'NONE', #50438, #46957, #44657, .T. ) ;
#57801=VERTEX_POINT ( 'NONE', #1207 ) ;
#57817=CARTESIAN_POINT ( 'NONE',  ( 24.00000000000000000, -16.64230188589300141, 14.64519951917099583 ) ) ;
#57822=VERTEX_POINT ( 'NONE', #45012 ) ;
#57823=VECTOR ( 'NONE', #65819, 1000.000000000000000 ) ;
#57829=ORIENTED_EDGE ( 'NONE', *, *, #991, .T. ) ;
#57831=LINE ( 'NONE', #57136, #49682 ) ;
#57835=VERTEX_POINT ( 'NONE', #66588 ) ;
#57841=ORIENTED_EDGE ( 'NONE', *, *, #42294, .F. ) ;
#57852=DIRECTION ( 'NONE',  ( 0.000000000000000000, 1.000000000000000000, 0.000000000000000000 ) ) ;
#57859=ORIENTED_EDGE ( 'NONE', *, *, #19385, .F. ) ;
#57862=AXIS2_PLACEMENT_3D ( 'NONE', #24287, #4133, #67065 ) ;
#57873=CARTESIAN_POINT ( 'NONE',  ( 15.50000000000000000, -0.2038245569916604938, 23.94337567297399971 ) ) ;
#57881=DIRECTION ( 'NONE',  ( 0.000000000000000000, -1.000000000000000000, 0.000000000000000000 ) ) ;
#57913=ORIENTED_EDGE ( 'NONE', *, *, #17971, .F. ) ;
#57914=VECTOR ( 'NONE', #49622, 1000.000000000000000 ) ;
#57919=EDGE_CURVE ( 'NONE', #28197, #44220, #31962, .T. ) ;
#57924=CARTESIAN_POINT ( 'NONE',  ( -14.25000000000000000, -2.500000000000000000, 21.77831216351300014 ) ) ;
#57929=CARTESIAN_POINT ( 'NONE',  ( 18.85410196625000268, -15.50000000000000000, 21.50000000000000000 ) ) ;
#57931=CARTESIAN_POINT ( 'NONE',  ( -11.00000000000000000, -14.33999999999999986, -14.50000000000000000 ) ) ;
#57936=CARTESIAN_POINT ( 'NONE',  ( 30.00000000000000000, -5.200000000000001066, -26.25000000000000000 ) ) ;
#57937=VERTEX_POINT ( 'NONE', #41812 ) ;
#57944=LINE ( 'NONE', #20813, #12111 ) ;
#57958=EDGE_CURVE ( 'NONE', #57686, #14101, #20593, .T. ) ;
#57960=ORIENTED_EDGE ( 'NONE', *, *, #5087, .F. ) ;
#57961=FACE_OUTER_BOUND ( 'NONE', #44216, .T. ) ;
#57987=EDGE_LOOP ( 'NONE', ( #13719, #14456, #66529, #38788 ) ) ;
#57988=ORIENTED_EDGE ( 'NONE', *, *, #54669, .T. ) ;
#57990=CARTESIAN_POINT ( 'NONE',  ( 15.50000000000000000, -2.500000000000000000, -21.05662432702600029 ) ) ;
#58005=AXIS2_PLACEMENT_3D ( 'NONE', #6082, #27640, #794 ) ;
#58006=AXIS2_PLACEMENT_3D ( 'NONE', #23510, #12880, #45068 ) ;
#58010=DIRECTION ( 'NONE',  ( 1.000000000000000000, 0.000000000000000000, 0.000000000000000000 ) ) ;
#58012=VERTEX_POINT ( 'NONE', #4693 ) ;
#58013=EDGE_CURVE ( 'NONE', #18037, #45394, #6083, .T. ) ;
#58015=CARTESIAN_POINT ( 'NONE',  ( -29.50000000000000355, -15.46862696659690073, -14.50000000000000000 ) ) ;
#58019=CARTESIAN_POINT ( 'NONE',  ( -15.50000000000000000, -1.037157890325000054, -19.00000000000000000 ) ) ;
#58035=ORIENTED_EDGE ( 'NONE', *, *, #68978, .T. ) ;
#58037=CARTESIAN_POINT ( 'NONE',  ( 30.00000000000000000, -15.46862696659690073, 14.50000000000000000 ) ) ;
#58038=VERTEX_POINT ( 'NONE', #37570 ) ;
#58039=ADVANCED_FACE ( 'NONE', ( #53151 ), #35350, .F. ) ;
#58041=VECTOR ( 'NONE', #10229, 1000.000000000000000 ) ;
#58057=EDGE_CURVE ( 'NONE', #27455, #48929, #40964, .T. ) ;
#58063=ORIENTED_EDGE ( 'NONE', *, *, #60908, .F. ) ;
#58065=AXIS2_PLACEMENT_3D ( 'NONE', #61979, #56681, #8231 ) ;
#58070=CARTESIAN_POINT ( 'NONE',  ( -24.00000000000000000, -15.50000000000000000, -19.33772233983200195 ) ) ;
#58072=ORIENTED_EDGE ( 'NONE', *, *, #12557, .F. ) ;
#58083=ORIENTED_EDGE ( 'NONE', *, *, #23528, .T. ) ;
#58085=ORIENTED_EDGE ( 'NONE', *, *, #48965, .T. ) ;
#58086=ORIENTED_EDGE ( 'NONE', *, *, #11581, .T. ) ;
#58087=ORIENTED_EDGE ( 'NONE', *, *, #18112, .T. ) ;
#58091=AXIS2_PLACEMENT_3D ( 'NONE', #24923, #3708, #46483 ) ;
#58093=DIRECTION ( 'NONE',  ( 1.000000000000000000, 0.000000000000000000, 0.000000000000000000 ) ) ;
#58094=ORIENTED_EDGE ( 'NONE', *, *, #4549, .T. ) ;
#58106=EDGE_LOOP ( 'NONE', ( #62031, #27934, #30176, #19629 ) ) ;
#58109=AXIS2_PLACEMENT_3D ( 'NONE', #56168, #7708, #29267 ) ;
#58117=ORIENTED_EDGE ( 'NONE', *, *, #1372, .F. ) ;
#58118=VECTOR ( 'NONE', #9927, 1000.000000000000114 ) ;
#58120=CARTESIAN_POINT ( 'NONE',  ( 30.00000000000000000, -16.28999999999710369, -15.00000000000794920 ) ) ;
#58131=CARTESIAN_POINT ( 'NONE',  ( -30.00000000000000000, -5.200000000000001066, 26.59999999999999787 ) ) ;
#58142=EDGE_LOOP ( 'NONE', ( #23784, #63911, #10122, #57164 ) ) ;
#58143=DIRECTION ( 'NONE',  ( 0.000000000000000000, 1.000000000000000000, 0.000000000000000000 ) ) ;
#58158=VERTEX_POINT ( 'NONE', #50241 ) ;
#58164=DIRECTION ( 'NONE',  ( -1.000000000000000000, 0.000000000000000000, 0.000000000000000000 ) ) ;
#58165=CIRCLE ( 'NONE', #33329, 4.000000000000000888 ) ;
#58169=CYLINDRICAL_SURFACE ( 'NONE', #49168, 0.3999999999993835154 ) ;
#58173=ORIENTED_EDGE ( 'NONE', *, *, #28837, .T. ) ;
#58174=CARTESIAN_POINT ( 'NONE',  ( 11.00000000000000000, -13.54524521594299991, -17.53999999999999915 ) ) ;
#58179=CARTESIAN_POINT ( 'NONE',  ( 30.00000000000000000, -17.35230188589299871, 15.35019951917099945 ) ) ;
#58180=DIRECTION ( 'NONE',  ( 0.4999999999989410693, 0.000000000000000000, 0.8660254037850499964 ) ) ;
#58181=ORIENTED_EDGE ( 'NONE', *, *, #65783, .F. ) ;
#58182=VECTOR ( 'NONE', #14938, 1000.000000000000000 ) ;
#58203=ADVANCED_FACE ( 'NONE', ( #6432, #43898 ), #33296, .T. ) ;
#58214=LINE ( 'NONE', #41951, #43770 ) ;
#58233=EDGE_CURVE ( 'NONE', #18504, #47849, #28673, .T. ) ;
#58236=DIRECTION ( 'NONE',  ( 0.000000000000000000, -1.000000000000000000, -6.036837696397607468E-13 ) ) ;
#58243=AXIS2_PLACEMENT_3D ( 'NONE', #33438, #17864, #59955 ) ;
#58247=FACE_OUTER_BOUND ( 'NONE', #55807, .T. ) ;
#58249=CARTESIAN_POINT ( 'NONE',  ( 11.00000000000000000, -14.03999999999999915, 14.79999999999999893 ) ) ;
#58250=AXIS2_PLACEMENT_3D ( 'NONE', #66969, #18530, #57419 ) ;
#58255=AXIS2_PLACEMENT_3D ( 'NONE', #64980, #61030, #43394 ) ;
#58256=DIRECTION ( 'NONE',  ( 0.000000000000000000, -0.7057491738665938596, 0.7084617869628679898 ) ) ;
#58257=ORIENTED_EDGE ( 'NONE', *, *, #27975, .T. ) ;
#58261=CYLINDRICAL_SURFACE ( 'NONE', #41769, 4.500000000000189182 ) ;
#58264=LINE ( 'NONE', #45893, #20852 ) ;
#58270=DIRECTION ( 'NONE',  ( 0.000000000000000000, 0.000000000000000000, -1.000000000000000000 ) ) ;
#58277=CARTESIAN_POINT ( 'NONE',  ( 30.00000000000000000, -5.200000000000001066, -26.59999999999999787 ) ) ;
#58280=ADVANCED_FACE ( 'NONE', ( #2495 ), #2657, .T. ) ;
#58282=DIRECTION ( 'NONE',  ( 0.000000000000000000, 0.000000000000000000, -1.000000000000000000 ) ) ;
#58285=ORIENTED_EDGE ( 'NONE', *, *, #44320, .T. ) ;
#58286=EDGE_CURVE ( 'NONE', #16314, #20965, #32084, .T. ) ;
#58289=ORIENTED_EDGE ( 'NONE', *, *, #42180, .F. ) ;
#58290=DIRECTION ( 'NONE',  ( 0.000000000000000000, 1.000000000000000000, 0.000000000000000000 ) ) ;
#58291=CARTESIAN_POINT ( 'NONE',  ( -11.00000000000000000, -13.54524521594299991, -17.53999999999999915 ) ) ;
#58297=AXIS2_PLACEMENT_3D ( 'NONE', #36129, #20571, #42135 ) ;
#58300=DIRECTION ( 'NONE',  ( 1.000000000000000000, -0.000000000000000000, -0.000000000000000000 ) ) ;
#58310=AXIS2_PLACEMENT_3D ( 'NONE', #15585, #68257, #58707 ) ;
#58331=DIRECTION ( 'NONE',  ( 1.000000000000000000, -0.000000000000000000, -0.000000000000000000 ) ) ;
#58340=CARTESIAN_POINT ( 'NONE',  ( -30.00000000000000000, -5.000000000000000000, -27.00000000000000000 ) ) ;
#58341=EDGE_CURVE ( 'NONE', #8948, #15366, #36073, .T. ) ;
#58342=DIRECTION ( 'NONE',  ( 0.000000000000000000, 0.000000000000000000, -1.000000000000000000 ) ) ;
#58343=VERTEX_POINT ( 'NONE', #9215 ) ;
#58357=CYLINDRICAL_SURFACE ( 'NONE', #31864, 4.000000000000000000 ) ;
#58366=ORIENTED_EDGE ( 'NONE', *, *, #24130, .T. ) ;
#58369=VECTOR ( 'NONE', #263, 1000.000000000000000 ) ;
#58372=EDGE_LOOP ( 'NONE', ( #6984, #36499, #58940, #2076, #59638, #1383, #29669, #6261, #27259 ) ) ;
#58375=ORIENTED_EDGE ( 'NONE', *, *, #32837, .F. ) ;
#58382=PLANE ( 'NONE',  #65915 ) ;
#58384=CARTESIAN_POINT ( 'NONE',  ( 30.00000000000000000, -9.199999999999999289, -12.69999999999986073 ) ) ;
#58387=CARTESIAN_POINT ( 'NONE',  ( -22.14589803375000088, -15.50000000000000000, 21.50000000000000000 ) ) ;
#58388=EDGE_CURVE ( 'NONE', #51018, #22980, #16864, .T. ) ;
#58406=VECTOR ( 'NONE', #18002, 1000.000000000000000 ) ;
#58410=CARTESIAN_POINT ( 'NONE',  ( 23.50000000000000000, -5.200000000000001066, -22.50000000000000000 ) ) ;
#58412=CIRCLE ( 'NONE', #1951, 0.3999999999993835154 ) ;
#58428=ADVANCED_FACE ( 'NONE', ( #5225 ), #11536, .F. ) ;
#58455=AXIS2_PLACEMENT_3D ( 'NONE', #5250, #53688, #42368 ) ;
#58456=AXIS2_PLACEMENT_3D ( 'NONE', #64574, #43701, #11500 ) ;
#58458=DIRECTION ( 'NONE',  ( -0.000000000000000000, 1.000000000000000000, -0.000000000000000000 ) ) ;
#58467=ORIENTED_EDGE ( 'NONE', *, *, #9736, .F. ) ;
#58482=ORIENTED_EDGE ( 'NONE', *, *, #34729, .F. ) ;
#58486=EDGE_CURVE ( 'NONE', #37433, #27463, #49725, .T. ) ;
#58491=CARTESIAN_POINT ( 'NONE',  ( 17.00000000000000000, -16.28999999999999915, 14.50000000000000000 ) ) ;
#58492=FACE_OUTER_BOUND ( 'NONE', #39968, .T. ) ;
#58503=DIRECTION ( 'NONE',  ( 0.000000000000000000, 1.000000000000000000, 0.000000000000000000 ) ) ;
#58505=ORIENTED_EDGE ( 'NONE', *, *, #48970, .T. ) ;
#58510=CARTESIAN_POINT ( 'NONE',  ( 13.00000000000000178, -16.28999999999999915, 14.50000000000000000 ) ) ;
#58530=VERTEX_POINT ( 'NONE', #39454 ) ;
#58538=EDGE_LOOP ( 'NONE', ( #51960, #53116, #33035, #27903, #69836, #58083, #69874 ) ) ;
#58544=AXIS2_PLACEMENT_3D ( 'NONE', #55531, #12716, #8465 ) ;
#58545=ORIENTED_EDGE ( 'NONE', *, *, #63654, .T. ) ;
#58547=DIRECTION ( 'NONE',  ( -1.000000000000000000, 0.000000000000000000, 0.000000000000000000 ) ) ;
#58548=ORIENTED_EDGE ( 'NONE', *, *, #46632, .F. ) ;
#58555=DIRECTION ( 'NONE',  ( 1.000000000000000000, 0.000000000000000000, 0.000000000000000000 ) ) ;
#58558=DIRECTION ( 'NONE',  ( 1.000000000000000000, 0.000000000000000000, 0.000000000000000000 ) ) ;
#58583=VERTEX_POINT ( 'NONE', #55728 ) ;
#58588=DIRECTION ( 'NONE',  ( 0.000000000000000000, 0.7096009616570518874, 0.7046037717862339012 ) ) ;
#58591=CARTESIAN_POINT ( 'NONE',  ( -11.00000000000000000, -14.33999999999999986, -14.50000000000000000 ) ) ;
#58597=CARTESIAN_POINT ( 'NONE',  ( 25.50000000000000355, -15.50000000000000000, -25.99999999999985434 ) ) ;
#58599=VECTOR ( 'NONE', #41808, 1000.000000000000000 ) ;
#58601=CARTESIAN_POINT ( 'NONE',  ( 17.00000000000000000, -17.35230188589299871, -15.35019951917099945 ) ) ;
#58603=EDGE_LOOP ( 'NONE', ( #39220, #13704, #29199, #31139, #39194, #47716, #69690, #47061, #14424, #58285, #17687, #6913, #60931, #1794, #18389, #34982 ) ) ;
#58606=FACE_OUTER_BOUND ( 'NONE', #29191, .T. ) ;
#58608=AXIS2_PLACEMENT_3D ( 'NONE', #30761, #41001, #24751 ) ;
#58618=ORIENTED_EDGE ( 'NONE', *, *, #8142, .F. ) ;
#58623=ORIENTED_EDGE ( 'NONE', *, *, #51431, .F. ) ;
#58624=ORIENTED_EDGE ( 'NONE', *, *, #37493, .T. ) ;
#58627=DIRECTION ( 'NONE',  ( 0.000000000000000000, 0.000000000000000000, -1.000000000000000000 ) ) ;
#58641=CARTESIAN_POINT ( 'NONE',  ( -14.25000000000000000, -0.2038245569916330158, -23.22168783648699986 ) ) ;
#58642=CARTESIAN_POINT ( 'NONE',  ( -11.00000000000000000, -11.50000000000000000, 15.00000000000000000 ) ) ;
#58644=DIRECTION ( 'NONE',  ( -0.4999999999989410693, 0.000000000000000000, -0.8660254037850499964 ) ) ;
#58645=VERTEX_POINT ( 'NONE', #51467 ) ;
#58648=FACE_OUTER_BOUND ( 'NONE', #65400, .T. ) ;
#58653=ORIENTED_EDGE ( 'NONE', *, *, #26728, .T. ) ;
#58657=DIRECTION ( 'NONE',  ( -1.000000000000000000, 0.000000000000000000, 0.000000000000000000 ) ) ;
#58658=B_SPLINE_CURVE_WITH_KNOTS ( 'NONE', 3,
 ( #54149, #6053, #65105, #5712, #54498, #47435 ),
 .UNSPECIFIED., .F., .F.,
 ( 4, 2, 4 ),
 ( 1.820537833122031657, 2.555393473688635897, 3.290249114255240137 ),
 .UNSPECIFIED. ) ;
#58660=CARTESIAN_POINT ( 'NONE',  ( -13.00000000000000178, -15.50000000000000000, -14.50000000000000000 ) ) ;
#58662=DIRECTION ( 'NONE',  ( -1.000000000000000000, 0.000000000000000000, 0.000000000000000000 ) ) ;
#58667=ORIENTED_EDGE ( 'NONE', *, *, #60765, .F. ) ;
#58678=CARTESIAN_POINT ( 'NONE',  ( 29.25000000000000000, -5.000000000000000000, -11.75000000000000000 ) ) ;
#58680=PLANE ( 'NONE',  #38837 ) ;
#58681=LINE ( 'NONE', #10237, #67767 ) ;
#58695=VERTEX_POINT ( 'NONE', #30258 ) ;
#58697=CIRCLE ( 'NONE', #1149, 0.5000000000001357803 ) ;
#58706=AXIS2_PLACEMENT_3D ( 'NONE', #19758, #52306, #41336 ) ;
#58707=DIRECTION ( 'NONE',  ( 0.000000000000000000, 0.000000000000000000, 1.000000000000000000 ) ) ;
#58715=EDGE_CURVE ( 'NONE', #3267, #67437, #9488, .T. ) ;
#58721=ORIENTED_EDGE ( 'NONE', *, *, #64658, .T. ) ;
#58723=CARTESIAN_POINT ( 'NONE',  ( 15.50000000000000000, -5.000000000000000000, -22.50000000000000000 ) ) ;
#58727=CARTESIAN_POINT ( 'NONE',  ( 29.50000000000000355, -11.50000000000100009, 19.50000000000103739 ) ) ;
#58729=EDGE_CURVE ( 'NONE', #66591, #11358, #8685, .T. ) ;
#58731=ORIENTED_EDGE ( 'NONE', *, *, #34088, .F. ) ;
#58745=CARTESIAN_POINT ( 'NONE',  ( -15.50000000000000000, -2.500000000000000000, 21.05662432702600029 ) ) ;
#58748=PLANE ( 'NONE',  #53063 ) ;
#58752=FACE_OUTER_BOUND ( 'NONE', #50360, .T. ) ;
#58762=CARTESIAN_POINT ( 'NONE',  ( -29.50000000000000355, -11.50000000000100009, -15.00000000000084910 ) ) ;
#58765=AXIS2_PLACEMENT_3D ( 'NONE', #64423, #26241, #31899 ) ;
#58766=EDGE_CURVE ( 'NONE', #51393, #50235, #52896, .T. ) ;
#58769=CYLINDRICAL_SURFACE ( 'NONE', #58765, 4.000000000000000000 ) ;
#58770=VERTEX_POINT ( 'NONE', #58174 ) ;
#58773=DIRECTION ( 'NONE',  ( 0.000000000000000000, 0.7096009616570518874, -0.7046037717862339012 ) ) ;
#58774=VECTOR ( 'NONE', #4995, 1000.000000000000000 ) ;
#58775=CARTESIAN_POINT ( 'NONE',  ( 30.00000000000000000, -17.14999999999999858, -27.00000000000000000 ) ) ;
#58779=DIRECTION ( 'NONE',  ( -0.8660254037844482555, 0.000000000000000000, 0.4999999999999831801 ) ) ;
#58782=FACE_OUTER_BOUND ( 'NONE', #68376, .T. ) ;
#58792=DIRECTION ( 'NONE',  ( 0.000000000000000000, -0.1249999999999996531, -0.9921567416492215186 ) ) ;
#58795=VERTEX_POINT ( 'NONE', #22439 ) ;
#58800=DIRECTION ( 'NONE',  ( 1.000000000000000000, 0.000000000000000000, 0.000000000000000000 ) ) ;
#58810=ORIENTED_EDGE ( 'NONE', *, *, #34332, .T. ) ;
#58821=AXIS2_PLACEMENT_3D ( 'NONE', #68066, #62757, #15381 ) ;
#58825=ORIENTED_EDGE ( 'NONE', *, *, #51342, .F. ) ;
#58836=CARTESIAN_POINT ( 'NONE',  ( -30.00000000000000000, -9.200000000000120082, -17.30000000000000071 ) ) ;
#58839=DIRECTION ( 'NONE',  ( 0.000000000000000000, 0.000000000000000000, 1.000000000000000000 ) ) ;
#58841=CARTESIAN_POINT ( 'NONE',  ( 17.00000000000000000, -16.64230188589299786, 14.64519951917100116 ) ) ;
#58848=EDGE_LOOP ( 'NONE', ( #17965, #1985, #36334, #29207 ) ) ;
#58850=CARTESIAN_POINT ( 'NONE',  ( 25.50000000000000355, -15.50000000000000000, 20.49999999999999645 ) ) ;
#58853=ORIENTED_EDGE ( 'NONE', *, *, #38773, .T. ) ;
#58857=CARTESIAN_POINT ( 'NONE',  ( -16.75000000000000000, -2.500000000000000000, 23.22168783648699986 ) ) ;
#58858=CARTESIAN_POINT ( 'NONE',  ( 11.00000000000000000, -16.28999999999710369, -14.50000000000000000 ) ) ;
#58863=AXIS2_PLACEMENT_3D ( 'NONE', #37736, #9828, #10857 ) ;
#58872=AXIS2_PLACEMENT_3D ( 'NONE', #56542, #34619, #62905 ) ;
#58887=VERTEX_POINT ( 'NONE', #26699 ) ;
#58890=ORIENTED_EDGE ( 'NONE', *, *, #12557, .T. ) ;
#58901=LINE ( 'NONE', #21409, #24997 ) ;
#58904=VERTEX_POINT ( 'NONE', #1218 ) ;
#58905=VECTOR ( 'NONE', #19888, 1000.000000000000000 ) ;
#58909=ORIENTED_EDGE ( 'NONE', *, *, #9736, .T. ) ;
#58919=VERTEX_POINT ( 'NONE', #524 ) ;
#58927=LINE ( 'NONE', #10827, #7048 ) ;
#58929=DIRECTION ( 'NONE',  ( 1.000000000000000000, -0.000000000000000000, -0.000000000000000000 ) ) ;
#58930=ORIENTED_EDGE ( 'NONE', *, *, #15672, .T. ) ;
#58933=EDGE_CURVE ( 'NONE', #55576, #51933, #37706, .T. ) ;
#58935=CARTESIAN_POINT ( 'NONE',  ( 30.00000000000000000, -5.000000000000000000, 27.00000000000000000 ) ) ;
#58937=FACE_OUTER_BOUND ( 'NONE', #52167, .T. ) ;
#58940=ORIENTED_EDGE ( 'NONE', *, *, #3455, .T. ) ;
#58942=ADVANCED_FACE ( 'NONE', ( #61629 ), #23111, .T. ) ;
#58960=VERTEX_POINT ( 'NONE', #55645 ) ;
#58978=EDGE_CURVE ( 'NONE', #24086, #29722, #18497, .T. ) ;
#58983=CYLINDRICAL_SURFACE ( 'NONE', #58455, 4.000000000000000000 ) ;
#58992=VERTEX_POINT ( 'NONE', #6844 ) ;
#58995=DIRECTION ( 'NONE',  ( 0.000000000000000000, 1.000000000000000000, 0.000000000000000000 ) ) ;
#59000=ORIENTED_EDGE ( 'NONE', *, *, #33247, .F. ) ;
#59004=CARTESIAN_POINT ( 'NONE',  ( -30.00000000000000000, -15.97213595500069871, -14.50000000000000000 ) ) ;
#59010=LINE ( 'NONE', #10569, #52609 ) ;
#59011=VECTOR ( 'NONE', #69016, 1000.000000000000000 ) ;
#59020=DIRECTION ( 'NONE',  ( -1.000000000000000000, 0.000000000000000000, 0.000000000000000000 ) ) ;
#59023=B_SPLINE_CURVE_WITH_KNOTS ( 'NONE', 3,
 ( #16990, #33251, #16292, #54824, #32573, #6382 ),
 .UNSPECIFIED., .F., .F.,
 ( 4, 2, 4 ),
 ( 1.820537833122031213, 2.555393473688635453, 3.290249114255239693 ),
 .UNSPECIFIED. ) ;
#59027=LINE ( 'NONE', #27207, #31858 ) ;
#59031=CARTESIAN_POINT ( 'NONE',  ( -15.50000000000000000, -15.50000000000000000, -25.99999999999985079 ) ) ;
#59032=EDGE_CURVE ( 'NONE', #68712, #32441, #28763, .T. ) ;
#59035=ORIENTED_EDGE ( 'NONE', *, *, #48658, .F. ) ;
#59037=EDGE_LOOP ( 'NONE', ( #69840, #18952, #1922, #4848, #32789, #63728 ) ) ;
#59044=CARTESIAN_POINT ( 'NONE',  ( -11.50000000000000000, -11.50000000000100009, -15.00000000000084910 ) ) ;
#59046=ORIENTED_EDGE ( 'NONE', *, *, #42927, .F. ) ;
#59047=FACE_OUTER_BOUND ( 'NONE', #57029, .T. ) ;
#59054=DIRECTION ( 'NONE',  ( 0.000000000000000000, 0.000000000000000000, 1.000000000000000000 ) ) ;
#59062=EDGE_LOOP ( 'NONE', ( #7857, #46407, #17611, #2790 ) ) ;
#59063=ORIENTED_EDGE ( 'NONE', *, *, #34568, .T. ) ;
#59068=CARTESIAN_POINT ( 'NONE',  ( -30.00000000000000000, -5.000000000000000000, -27.00000000000000000 ) ) ;
#59075=CARTESIAN_POINT ( 'NONE',  ( -17.24945551514599984, -17.50000000000000000, -25.53140320652400064 ) ) ;
#59079=CARTESIAN_POINT ( 'NONE',  ( -11.00000000000000000, -13.79999999999979998, -17.30000000000000071 ) ) ;
#59084=EDGE_CURVE ( 'NONE', #55561, #63676, #69350, .T. ) ;
#59112=DIRECTION ( 'NONE',  ( 0.000000000000000000, -1.000000000000000000, -6.036837696397607468E-13 ) ) ;
#59118=VECTOR ( 'NONE', #28015, 1000.000000000000000 ) ;
#59119=LINE ( 'NONE', #43889, #37459 ) ;
#59120=ORIENTED_EDGE ( 'NONE', *, *, #15469, .T. ) ;
#59127=DIRECTION ( 'NONE',  ( 0.000000000000000000, 1.000000000000000000, 0.000000000000000000 ) ) ;
#59129=DIRECTION ( 'NONE',  ( 0.000000000000000000, 0.000000000000000000, 1.000000000000000000 ) ) ;
#59137=ORIENTED_EDGE ( 'NONE', *, *, #14717, .F. ) ;
#59140=CARTESIAN_POINT ( 'NONE',  ( -18.85410196625000268, -15.50000000000000000, 21.50000000000000000 ) ) ;
#59144=ORIENTED_EDGE ( 'NONE', *, *, #46784, .T. ) ;
#59146=DIRECTION ( 'NONE',  ( 0.000000000000000000, 1.000000000000000000, 0.000000000000000000 ) ) ;
#59154=EDGE_CURVE ( 'NONE', #14428, #28990, #46424, .T. ) ;
#59157=CARTESIAN_POINT ( 'NONE',  ( -11.75000000000000000, -5.200000000000001066, 11.75000000000000000 ) ) ;
#59160=ORIENTED_EDGE ( 'NONE', *, *, #68682, .T. ) ;
#59175=CYLINDRICAL_SURFACE ( 'NONE', #39399, 2.250000000000001776 ) ;
#59178=LINE ( 'NONE', #16388, #32345 ) ;
#59184=CYLINDRICAL_SURFACE ( 'NONE', #30289, 0.5000000000079367624 ) ;
#59196=ADVANCED_FACE ( 'NONE', ( #31584 ), #5418, .F. ) ;
#59204=CARTESIAN_POINT ( 'NONE',  ( -11.50000000000000000, -11.50000000000100009, 15.00000000000084910 ) ) ;
#59205=ADVANCED_FACE ( 'NONE', ( #4705 ), #26269, .T. ) ;
#59213=CARTESIAN_POINT ( 'NONE',  ( -30.00000000000000000, -11.50000000000100009, 10.50000000000065903 ) ) ;
#59216=LINE ( 'NONE', #10766, #48055 ) ;
#59219=AXIS2_PLACEMENT_3D ( 'NONE', #68305, #19160, #9261 ) ;
#59233=VERTEX_POINT ( 'NONE', #59140 ) ;
#59239=CARTESIAN_POINT ( 'NONE',  ( -28.00000000000000000, -17.35230188589299871, 15.35019951917099945 ) ) ;
#59242=AXIS2_PLACEMENT_3D ( 'NONE', #37474, #57633, #20505 ) ;
#59246=VECTOR ( 'NONE', #69544, 1000.000000000000000 ) ;
#59254=DIRECTION ( 'NONE',  ( 0.000000000000000000, 0.6857142857146703019, -0.7278708115914659382 ) ) ;
#59267=VECTOR ( 'NONE', #22137, 1000.000000000000000 ) ;
#59273=CARTESIAN_POINT ( 'NONE',  ( 25.50000000000000355, -5.578999999999999737, -22.50000000000000000 ) ) ;
#59280=DIRECTION ( 'NONE',  ( -1.000000000000000000, 0.000000000000000000, 0.000000000000000000 ) ) ;
#59285=DIRECTION ( 'NONE',  ( 0.000000000000000000, 1.000000000000000000, 0.000000000000000000 ) ) ;
#59286=DIRECTION ( 'NONE',  ( 0.000000000000000000, -1.000000000000000000, 0.000000000000000000 ) ) ;
#59291=AXIS2_PLACEMENT_3D ( 'NONE', #6503, #17791, #17436 ) ;
#59292=VERTEX_POINT ( 'NONE', #11047 ) ;
#59293=CARTESIAN_POINT ( 'NONE',  ( -14.25000000000000000, -2.500000000000000000, -21.77831216351300014 ) ) ;
#59295=ORIENTED_EDGE ( 'NONE', *, *, #21141, .F. ) ;
#59305=ORIENTED_EDGE ( 'NONE', *, *, #61539, .T. ) ;
#59310=VECTOR ( 'NONE', #38684, 1000.000000000000000 ) ;
#59316=ORIENTED_EDGE ( 'NONE', *, *, #9285, .F. ) ;
#59318=PLANE ( 'NONE',  #28853 ) ;
#59336=DIRECTION ( 'NONE',  ( -1.000000000000000000, 0.000000000000000000, 0.000000000000000000 ) ) ;
#59338=ORIENTED_EDGE ( 'NONE', *, *, #42359, .F. ) ;
#59342=DIRECTION ( 'NONE',  ( 1.000000000000000000, -0.000000000000000000, -0.000000000000000000 ) ) ;
#59362=CARTESIAN_POINT ( 'NONE',  ( 11.50000000000000000, -11.50000000000000000, -11.00000000000000000 ) ) ;
#59366=CARTESIAN_POINT ( 'NONE',  ( 11.75000000000000000, -5.000000000000000000, 26.25000000000000000 ) ) ;
#59373=VERTEX_POINT ( 'NONE', #7107 ) ;
#59374=EDGE_LOOP ( 'NONE', ( #12239, #19718, #65809, #60756 ) ) ;
#59379=DIRECTION ( 'NONE',  ( 0.000000000000000000, 1.000000000000000000, 0.000000000000000000 ) ) ;
#59380=EDGE_CURVE ( 'NONE', #30577, #35602, #2508, .T. ) ;
#59384=VERTEX_POINT ( 'NONE', #24076 ) ;
#59394=DIRECTION ( 'NONE',  ( 0.000000000000000000, 1.000000000000000000, 0.000000000000000000 ) ) ;
#59400=EDGE_LOOP ( 'NONE', ( #57543, #3687, #36423, #35549 ) ) ;
#59402=ORIENTED_EDGE ( 'NONE', *, *, #1372, .T. ) ;
#59406=VECTOR ( 'NONE', #18628, 1000.000000000000000 ) ;
#59409=EDGE_LOOP ( 'NONE', ( #12329, #34915, #10923, #16970 ) ) ;
#59412=VECTOR ( 'NONE', #34133, 1000.000000000000000 ) ;
#59418=CARTESIAN_POINT ( 'NONE',  ( -11.00000000000000000, -14.04000000000000092, -14.80000000000000071 ) ) ;
#59434=CARTESIAN_POINT ( 'NONE',  ( -15.50000000000000000, -2.500000000000000000, 23.94337567297399971 ) ) ;
#59440=EDGE_CURVE ( 'NONE', #59443, #8072, #512, .T. ) ;
#59441=VERTEX_POINT ( 'NONE', #1465 ) ;
#59443=VERTEX_POINT ( 'NONE', #40344 ) ;
#59444=LINE ( 'NONE', #37535, #48194 ) ;
#59450=CARTESIAN_POINT ( 'NONE',  ( -30.00000000000000000, -13.79999999999979998, -17.30000000000000071 ) ) ;
#59452=LINE ( 'NONE', #64419, #4097 ) ;
#59473=CARTESIAN_POINT ( 'NONE',  ( 13.00000000000000178, -17.35230188589299871, 15.35019951917099945 ) ) ;
#59481=ADVANCED_FACE ( 'NONE', ( #61540 ), #49568, .F. ) ;
#59484=EDGE_LOOP ( 'NONE', ( #6751, #56781, #4967, #47392 ) ) ;
#59489=ADVANCED_FACE ( 'NONE', ( #18409 ), #56258, .F. ) ;
#59495=VECTOR ( 'NONE', #61147, 1000.000000000000000 ) ;
#59498=CARTESIAN_POINT ( 'NONE',  ( -11.00000000000000000, -15.46862696659690073, -14.50000000000000000 ) ) ;
#59507=ORIENTED_EDGE ( 'NONE', *, *, #69589, .T. ) ;
#59518=AXIS2_PLACEMENT_3D ( 'NONE', #62098, #1413, #8005 ) ;
#59521=ADVANCED_FACE ( 'NONE', ( #41038 ), #56945, .F. ) ;
#59522=CARTESIAN_POINT ( 'NONE',  ( 30.00000000000000000, -15.97213595500069871, -14.50000000000000000 ) ) ;
#59532=AXIS2_PLACEMENT_3D ( 'NONE', #59691, #27173, #32814 ) ;
#59533=CARTESIAN_POINT ( 'NONE',  ( 30.00000000000000000, -17.35230188589299871, 15.35019951917099945 ) ) ;
#59539=DIRECTION ( 'NONE',  ( -1.000000000000000000, 0.000000000000000000, 0.000000000000000000 ) ) ;
#59542=DIRECTION ( 'NONE',  ( -1.000000000000000000, 0.000000000000000000, 0.000000000000000000 ) ) ;
#59555=CARTESIAN_POINT ( 'NONE',  ( 30.00000000000000000, -8.959999999999999076, 12.95475478405700009 ) ) ;
#59559=ORIENTED_EDGE ( 'NONE', *, *, #42359, .T. ) ;
#59562=CARTESIAN_POINT ( 'NONE',  ( -30.00000000000000000, -17.35230188589299871, 15.35019951917099945 ) ) ;
#59570=ORIENTED_EDGE ( 'NONE', *, *, #35073, .F. ) ;
#59599=CARTESIAN_POINT ( 'NONE',  ( -29.50000000000000355, -15.97213595500069871, 14.50000000000000000 ) ) ;
#59601=ADVANCED_FACE ( 'NONE', ( #37498 ), #15231, .F. ) ;
#59619=DIRECTION ( 'NONE',  ( 0.000000000000000000, 0.7096009616570518874, 0.7046037717862339012 ) ) ;
#59624=DIRECTION ( 'NONE',  ( 0.000000000000000000, 0.000000000000000000, -1.000000000000000000 ) ) ;
#59625=DIRECTION ( 'NONE',  ( 1.000000000000000000, 0.000000000000000000, 0.000000000000000000 ) ) ;
#59638=ORIENTED_EDGE ( 'NONE', *, *, #21431, .F. ) ;
#59643=ADVANCED_FACE ( 'NONE', ( #53414 ), #6007, .F. ) ;
#59657=ORIENTED_EDGE ( 'NONE', *, *, #21079, .T. ) ;
#59661=AXIS2_PLACEMENT_3D ( 'NONE', #18685, #8419, #29998 ) ;
#59663=CARTESIAN_POINT ( 'NONE',  ( -11.50000000000000000, -11.70000000000000284, -11.00000000000000000 ) ) ;
#59669=DIRECTION ( 'NONE',  ( -1.000000000000000000, 0.000000000000000000, 0.000000000000000000 ) ) ;
#59676=ORIENTED_EDGE ( 'NONE', *, *, #2989, .T. ) ;
#59679=CYLINDRICAL_SURFACE ( 'NONE', #35868, 3.499999999999999556 ) ;
#59687=ORIENTED_EDGE ( 'NONE', *, *, #24037, .T. ) ;
#59691=CARTESIAN_POINT ( 'NONE',  ( -15.50000000000000000, -5.000000000000000000, -22.50000000000000000 ) ) ;
#59703=LINE ( 'NONE', #23249, #42048 ) ;
#59723=EDGE_CURVE ( 'NONE', #57577, #4484, #3939, .T. ) ;
#59731=VERTEX_POINT ( 'NONE', #7369 ) ;
#59741=DIRECTION ( 'NONE',  ( -1.000000000000000000, 0.000000000000000000, 0.000000000000000000 ) ) ;
#59743=CARTESIAN_POINT ( 'NONE',  ( -11.00000000000000000, -5.599999999999379696, -27.00000000000000000 ) ) ;
#59746=DIRECTION ( 'NONE',  ( 0.000000000000000000, 3.989863994748342081E-13, 1.000000000000000000 ) ) ;
#59752=CARTESIAN_POINT ( 'NONE',  ( 25.50000000000000355, 0.000000000000000000, 20.24999999999999645 ) ) ;
#59757=CARTESIAN_POINT ( 'NONE',  ( -23.48000000000000043, -17.50000000000000000, -26.00000000000000355 ) ) ;
#59758=ORIENTED_EDGE ( 'NONE', *, *, #8083, .F. ) ;
#59759=AXIS2_PLACEMENT_3D ( 'NONE', #10805, #4815, #21767 ) ;
#59765=VECTOR ( 'NONE', #63782, 1000.000000000000000 ) ;
#59767=CARTESIAN_POINT ( 'NONE',  ( 17.24945551514599984, -15.50000000000000000, 25.53140320652400064 ) ) ;
#59777=CARTESIAN_POINT ( 'NONE',  ( -30.00000000000000000, -11.50000000000100009, -15.00000000000084910 ) ) ;
#59780=EDGE_CURVE ( 'NONE', #24071, #34366, #16352, .T. ) ;
#59784=LINE ( 'NONE', #44537, #15749 ) ;
#59798=DIRECTION ( 'NONE',  ( 0.000000000000000000, -0.9938079899998859545, 0.1111111111112941946 ) ) ;
#59804=ORIENTED_EDGE ( 'NONE', *, *, #63654, .F. ) ;
#59806=AXIS2_PLACEMENT_3D ( 'NONE', #8449, #50890, #8100 ) ;
#59812=ORIENTED_EDGE ( 'NONE', *, *, #32391, .T. ) ;
#59816=LINE ( 'NONE', #59473, #64519 ) ;
#59832=ORIENTED_EDGE ( 'NONE', *, *, #5901, .T. ) ;
#59836=VECTOR ( 'NONE', #29557, 1000.000000000000000 ) ;
#59839=CARTESIAN_POINT ( 'NONE',  ( -29.50000000000000355, -11.50000000000100009, 15.00000000000084910 ) ) ;
#59844=DIRECTION ( 'NONE',  ( 1.000000000000000000, -0.000000000000000000, -0.000000000000000000 ) ) ;
#59846=CARTESIAN_POINT ( 'NONE',  ( 11.00000000000000000, -17.50000000000000000, 60.00000000000000000 ) ) ;
#59850=DIRECTION ( 'NONE',  ( -1.000000000000000000, 0.000000000000000000, 0.000000000000000000 ) ) ;
#59852=VERTEX_POINT ( 'NONE', #46600 ) ;
#59864=ORIENTED_EDGE ( 'NONE', *, *, #28069, .T. ) ;
#59878=ORIENTED_EDGE ( 'NONE', *, *, #49141, .F. ) ;
#59879=VECTOR ( 'NONE', #63410, 1000.000000000000000 ) ;
#59880=CARTESIAN_POINT ( 'NONE',  ( -11.00000000000000000, -12.00000000000000000, -10.52786404500095863 ) ) ;
#59891=AXIS2_PLACEMENT_3D ( 'NONE', #34331, #63326, #67586 ) ;
#59893=ORIENTED_EDGE ( 'NONE', *, *, #34576, .T. ) ;
#59896=CARTESIAN_POINT ( 'NONE',  ( -13.00000000000000178, -17.50000000000000000, 15.70499999999969809 ) ) ;
#59899=DIRECTION ( 'NONE',  ( 0.000000000000000000, -1.000000000000000000, 0.000000000000000000 ) ) ;
#59903=LINE ( 'NONE', #32687, #16414 ) ;
#59909=EDGE_LOOP ( 'NONE', ( #50500, #23304 ) ) ;
#59916=ORIENTED_EDGE ( 'NONE', *, *, #47757, .T. ) ;
#59943=DIRECTION ( 'NONE',  ( 0.000000000000000000, 0.000000000000000000, 1.000000000000000000 ) ) ;
#59945=CARTESIAN_POINT ( 'NONE',  ( -15.50000000000000000, 0.000000000000000000, 26.50000000000000000 ) ) ;
#59948=CIRCLE ( 'NONE', #63506, 3.499999999999850342 ) ;
#59952=DIRECTION ( 'NONE',  ( 0.000000000000000000, 0.7046037717862339012, -0.7096009616570518874 ) ) ;
#59954=AXIS2_PLACEMENT_3D ( 'NONE', #42938, #6512, #10758 ) ;
#59955=DIRECTION ( 'NONE',  ( 0.000000000000000000, 0.7096009616570518874, 0.7046037717862339012 ) ) ;
#59957=FACE_OUTER_BOUND ( 'NONE', #4701, .T. ) ;
#59962=CARTESIAN_POINT ( 'NONE',  ( -16.75000000000000000, -2.500000000000000000, -23.22168783648699986 ) ) ;
#59966=EDGE_CURVE ( 'NONE', #8573, #51508, #52270, .T. ) ;
#59977=ORIENTED_EDGE ( 'NONE', *, *, #30136, .T. ) ;
#59981=LINE ( 'NONE', #33115, #18197 ) ;
#59992=CARTESIAN_POINT ( 'NONE',  ( 30.00000000000000000, -13.79999999999979998, 17.64999999999988844 ) ) ;
#59994=ADVANCED_FACE ( 'NONE', ( #4881 ), #32786, .F. ) ;
#59995=ORIENTED_EDGE ( 'NONE', *, *, #34576, .F. ) ;
#60000=CARTESIAN_POINT ( 'NONE',  ( -15.50000000000000000, -5.000000000000000000, 18.50000000000000000 ) ) ;
#60014=FACE_OUTER_BOUND ( 'NONE', #14147, .T. ) ;
#60016=AXIS2_PLACEMENT_3D ( 'NONE', #26286, #20973, #42549 ) ;
#60020=EDGE_CURVE ( 'NONE', #60253, #10983, #16181, .T. ) ;
#60028=ORIENTED_EDGE ( 'NONE', *, *, #55889, .F. ) ;
#60031=VECTOR ( 'NONE', #26916, 1000.000000000000000 ) ;
#60040=ADVANCED_FACE ( 'NONE', ( #63935 ), #25766, .F. ) ;
#60048=CIRCLE ( 'NONE', #69093, 4.000000000000000888 ) ;
#60049=EDGE_CURVE ( 'NONE', #27219, #9490, #47312, .T. ) ;
#60056=EDGE_CURVE ( 'NONE', #26381, #55064, #269, .T. ) ;
#60057=CARTESIAN_POINT ( 'NONE',  ( 25.50000000000000355, -5.200000000000001066, 20.24999999999999645 ) ) ;
#60058=ORIENTED_EDGE ( 'NONE', *, *, #37787, .T. ) ;
#60061=ORIENTED_EDGE ( 'NONE', *, *, #29292, .T. ) ;
#60062=DIRECTION ( 'NONE',  ( 0.000000000000000000, 0.000000000000000000, 1.000000000000000000 ) ) ;
#60069=ADVANCED_FACE ( 'NONE', ( #53334, #36710 ), #26450, .F. ) ;
#60082=DIRECTION ( 'NONE',  ( 0.000000000000000000, 0.000000000000000000, 1.000000000000000000 ) ) ;
#60086=DIRECTION ( 'NONE',  ( -1.000000000000000000, 0.000000000000000000, 0.000000000000000000 ) ) ;
#60088=DIRECTION ( 'NONE',  ( 0.000000000000000000, -5.800915303574361727E-12, 1.000000000000000000 ) ) ;
#60097=DIRECTION ( 'NONE',  ( 0.4998444328988824181, 0.000000000000000000, -0.8661152018640445593 ) ) ;
#60102=CARTESIAN_POINT ( 'NONE',  ( -15.50000000000000000, -15.50000000000000000, 22.50000000000000000 ) ) ;
#60110=LINE ( 'NONE', #33920, #14435 ) ;
#60112=ADVANCED_FACE ( 'NONE', ( #60337 ), #27834, .F. ) ;
#60114=DIRECTION ( 'NONE',  ( 0.000000000000000000, -1.000000000000000000, 0.000000000000000000 ) ) ;
#60117=CARTESIAN_POINT ( 'NONE',  ( 24.00000000000000000, -17.35230188589299871, 15.35019951917099945 ) ) ;
#60118=EDGE_LOOP ( 'NONE', ( #64653, #6275, #64603, #59676 ) ) ;
#60119=DIRECTION ( 'NONE',  ( 0.000000000000000000, 0.000000000000000000, 1.000000000000000000 ) ) ;
#60120=FACE_OUTER_BOUND ( 'NONE', #25066, .T. ) ;
#60126=ORIENTED_EDGE ( 'NONE', *, *, #39815, .T. ) ;
#60129=AXIS2_PLACEMENT_3D ( 'NONE', #9807, #58929, #32056 ) ;
#60134=DIRECTION ( 'NONE',  ( -1.000000000000000000, 0.000000000000000000, 0.000000000000000000 ) ) ;
#60137=CYLINDRICAL_SURFACE ( 'NONE', #26354, 0.5000000000079367624 ) ;
#60142=CARTESIAN_POINT ( 'NONE',  ( -11.50000000000000000, -11.50000000000000000, -15.00000000000000000 ) ) ;
#60145=CARTESIAN_POINT ( 'NONE',  ( -25.50000000000000355, -15.50000000000000000, -22.50000000000000000 ) ) ;
#60147=ORIENTED_EDGE ( 'NONE', *, *, #38773, .F. ) ;
#60149=ADVANCED_FACE ( 'NONE', ( #17212 ), #39128, .F. ) ;
#60150=VERTEX_POINT ( 'NONE', #38782 ) ;
#60165=ORIENTED_EDGE ( 'NONE', *, *, #58766, .F. ) ;
#60168=DIRECTION ( 'NONE',  ( 1.000000000000000000, -0.000000000000000000, -0.000000000000000000 ) ) ;
#60172=AXIS2_PLACEMENT_3D ( 'NONE', #48459, #64719, #43143 ) ;
#60173=DIRECTION ( 'NONE',  ( 0.000000000000000000, 1.000000000000000000, 0.000000000000000000 ) ) ;
#60179=ORIENTED_EDGE ( 'NONE', *, *, #62946, .F. ) ;
#60180=ORIENTED_EDGE ( 'NONE', *, *, #20456, .T. ) ;
#60182=AXIS2_PLACEMENT_3D ( 'NONE', #39634, #60173, #49910 ) ;
#60183=CARTESIAN_POINT ( 'NONE',  ( -15.50000000000000000, -0.2038245569916614930, -23.94337567297399971 ) ) ;
#60196=CARTESIAN_POINT ( 'NONE',  ( 16.33565937784172917, -0.3156604612126656106, 23.46090750622625976 ) ) ;
#60201=ORIENTED_EDGE ( 'NONE', *, *, #11451, .T. ) ;
#60202=PLANE ( 'NONE',  #26460 ) ;
#60205=EDGE_CURVE ( 'NONE', #29890, #53596, #13564, .T. ) ;
#60207=CIRCLE ( 'NONE', #16204, 4.500000000000191847 ) ;
#60214=CIRCLE ( 'NONE', #1510, 2.000000000000001776 ) ;
#60215=LINE ( 'NONE', #11768, #34736 ) ;
#60218=ORIENTED_EDGE ( 'NONE', *, *, #23652, .F. ) ;
#60221=VERTEX_POINT ( 'NONE', #60000 ) ;
#60222=DIRECTION ( 'NONE',  ( 0.000000000000000000, 0.000000000000000000, -1.000000000000000000 ) ) ;
#60225=LINE ( 'NONE', #49624, #1681 ) ;
#60226=VECTOR ( 'NONE', #43191, 1000.000000000000000 ) ;
#60235=DIRECTION ( 'NONE',  ( 0.000000000000000000, 0.000000000000000000, 1.000000000000000000 ) ) ;
#60237=ORIENTED_EDGE ( 'NONE', *, *, #17891, .T. ) ;
#60239=ADVANCED_FACE ( 'NONE', ( #67315 ), #8248, .F. ) ;
#60245=EDGE_CURVE ( 'NONE', #56934, #44584, #24876, .T. ) ;
#60253=VERTEX_POINT ( 'NONE', #8952 ) ;
#60262=LINE ( 'NONE', #6186, #51937 ) ;
#60264=VECTOR ( 'NONE', #29158, 1000.000000000000000 ) ;
#60277=EDGE_CURVE ( 'NONE', #58530, #1475, #26276, .T. ) ;
#60282=ORIENTED_EDGE ( 'NONE', *, *, #27800, .F. ) ;
#60283=CIRCLE ( 'NONE', #29802, 0.3999999999993835154 ) ;
#60284=CARTESIAN_POINT ( 'NONE',  ( 17.00000000000000000, -15.50000000000000000, -14.50000000000000000 ) ) ;
#60290=CARTESIAN_POINT ( 'NONE',  ( -25.50000000000000355, -15.50000000000000000, 22.50000000000000000 ) ) ;
#60292=FACE_OUTER_BOUND ( 'NONE', #63203, .T. ) ;
#60293=VECTOR ( 'NONE', #25805, 1000.000000000000000 ) ;
#60297=CARTESIAN_POINT ( 'NONE',  ( -30.00000000000000000, -11.50000000000000000, -15.00000000000000000 ) ) ;
#60303=AXIS2_PLACEMENT_3D ( 'NONE', #19505, #67957, #30470 ) ;
#60310=ORIENTED_EDGE ( 'NONE', *, *, #65282, .F. ) ;
#60314=DIRECTION ( 'NONE',  ( -0.4285714285711678118, 0.000000000000000000, -0.9035079029053749711 ) ) ;
#60321=EDGE_LOOP ( 'NONE', ( #2785, #62758, #8526, #8748 ) ) ;
#60323=VERTEX_POINT ( 'NONE', #4382 ) ;
#60333=CIRCLE ( 'NONE', #29856, 4.500000000000190958 ) ;
#60335=ORIENTED_EDGE ( 'NONE', *, *, #6856, .T. ) ;
#60337=FACE_OUTER_BOUND ( 'NONE', #16948, .T. ) ;
#60342=AXIS2_PLACEMENT_3D ( 'NONE', #49237, #33310, #10359 ) ;
#60343=CARTESIAN_POINT ( 'NONE',  ( 11.50000000000000000, -11.70000000000012008, -10.70000000000011831 ) ) ;
#60346=VECTOR ( 'NONE', #29699, 1000.000000000000114 ) ;
#60352=LINE ( 'NONE', #44434, #66249 ) ;
#60353=LINE ( 'NONE', #8000, #55015 ) ;
#60361=DIRECTION ( 'NONE',  ( 0.000000000000000000, 0.000000000000000000, 1.000000000000000000 ) ) ;
#60362=EDGE_CURVE ( 'NONE', #21951, #50851, #68725, .T. ) ;
#60363=FACE_OUTER_BOUND ( 'NONE', #54264, .T. ) ;
#60364=DIRECTION ( 'NONE',  ( 0.000000000000000000, 0.7096009616570518874, 0.7046037717862339012 ) ) ;
#60366=EDGE_CURVE ( 'NONE', #36688, #29870, #3307, .T. ) ;
#60370=DIRECTION ( 'NONE',  ( 0.000000000000000000, 0.000000000000000000, -1.000000000000000000 ) ) ;
#60376=DIRECTION ( 'NONE',  ( 0.000000000000000000, 1.000000000000000000, 0.000000000000000000 ) ) ;
#60378=CARTESIAN_POINT ( 'NONE',  ( -30.00000000000000000, -17.14999999999999858, 27.00000000000000000 ) ) ;
#60381=VECTOR ( 'NONE', #63376, 1000.000000000000000 ) ;
#60385=FACE_OUTER_BOUND ( 'NONE', #56422, .T. ) ;
#60397=VECTOR ( 'NONE', #10870, 1000.000000000000000 ) ;
#60418=VERTEX_POINT ( 'NONE', #5430 ) ;
#60426=ORIENTED_EDGE ( 'NONE', *, *, #36622, .F. ) ;
#60438=DIRECTION ( 'NONE',  ( -1.000000000000000000, 0.000000000000000000, 0.000000000000000000 ) ) ;
#60441=VERTEX_POINT ( 'NONE', #26983 ) ;
#60447=EDGE_CURVE ( 'NONE', #16870, #19628, #48541, .T. ) ;
#60457=FACE_OUTER_BOUND ( 'NONE', #10700, .T. ) ;
#60472=DIRECTION ( 'NONE',  ( -1.000000000000000000, 0.000000000000000000, 0.000000000000000000 ) ) ;
#60482=ORIENTED_EDGE ( 'NONE', *, *, #5561, .F. ) ;
#60489=VECTOR ( 'NONE', #23961, 1000.000000000000000 ) ;
#60507=AXIS2_PLACEMENT_3D ( 'NONE', #56157, #8043, #2402 ) ;
#60511=ORIENTED_EDGE ( 'NONE', *, *, #60205, .F. ) ;
#60512=ADVANCED_FACE ( 'NONE', ( #67222 ), #18415, .T. ) ;
#60516=ORIENTED_EDGE ( 'NONE', *, *, #63197, .T. ) ;
#60517=CIRCLE ( 'NONE', #41332, 0.3999999999993817390 ) ;
#60540=DIRECTION ( 'NONE',  ( 0.000000000000000000, -0.7071067811865460184, -0.7071067811865489050 ) ) ;
#60541=CIRCLE ( 'NONE', #39093, 3.499999999999056310 ) ;
#60556=LINE ( 'NONE', #139, #10885 ) ;
#60557=CARTESIAN_POINT ( 'NONE',  ( 30.00000000000000000, -5.200000000000001066, 26.25000000000000000 ) ) ;
#60561=CIRCLE ( 'NONE', #1806, 0.3500000000009988455 ) ;
#60575=ORIENTED_EDGE ( 'NONE', *, *, #54644, .T. ) ;
#60577=CARTESIAN_POINT ( 'NONE',  ( 30.00000000000000000, -13.79999999999979998, 17.30000000000000071 ) ) ;
#60584=CARTESIAN_POINT ( 'NONE',  ( 24.00000000000000000, -17.50000000000000000, -19.33772233983200195 ) ) ;
#60594=EDGE_CURVE ( 'NONE', #62987, #65652, #38862, .T. ) ;
#60596=EDGE_LOOP ( 'NONE', ( #40245, #34674 ) ) ;
#60598=VECTOR ( 'NONE', #33926, 1000.000000000000000 ) ;
#60599=VECTOR ( 'NONE', #55926, 1000.000000000000114 ) ;
#60603=EDGE_CURVE ( 'NONE', #14932, #40754, #1823, .T. ) ;
#60613=VECTOR ( 'NONE', #31181, 1000.000000000000000 ) ;
#60616=ORIENTED_EDGE ( 'NONE', *, *, #54058, .F. ) ;
#60617=ORIENTED_EDGE ( 'NONE', *, *, #66230, .T. ) ;
#60624=VECTOR ( 'NONE', #49851, 1000.000000000000000 ) ;
#60625=CARTESIAN_POINT ( 'NONE',  ( -11.00000000000000000, -10.85999999999999943, -9.000000000000001776 ) ) ;
#60627=EDGE_LOOP ( 'NONE', ( #48770, #5864, #10251, #68709 ) ) ;
#60633=EDGE_CURVE ( 'NONE', #41307, #37678, #66182, .T. ) ;
#60634=CARTESIAN_POINT ( 'NONE',  ( 11.75000000000000000, -5.000000000000000000, 11.75000000000000000 ) ) ;
#60635=DIRECTION ( 'NONE',  ( 0.000000000000000000, 0.000000000000000000, -1.000000000000000000 ) ) ;
#60645=CIRCLE ( 'NONE', #31353, 4.500000000000191847 ) ;
#60649=DIRECTION ( 'NONE',  ( -0.000000000000000000, 1.000000000000000000, -0.000000000000000000 ) ) ;
#60655=ORIENTED_EDGE ( 'NONE', *, *, #13190, .T. ) ;
#60659=VECTOR ( 'NONE', #22481, 1000.000000000000000 ) ;
#60669=ORIENTED_EDGE ( 'NONE', *, *, #19091, .F. ) ;
#60675=CARTESIAN_POINT ( 'NONE',  ( 25.50000000000000355, -5.200000000000001066, -22.50000000000000000 ) ) ;
#60679=ORIENTED_EDGE ( 'NONE', *, *, #50464, .T. ) ;
#60685=ADVANCED_FACE ( 'NONE', ( #62260 ), #3579, .F. ) ;
#60686=VECTOR ( 'NONE', #13516, 1000.000000000000000 ) ;
#60689=FACE_OUTER_BOUND ( 'NONE', #69242, .T. ) ;
#60701=AXIS2_PLACEMENT_3D ( 'NONE', #42846, #15982, #59112 ) ;
#60702=VECTOR ( 'NONE', #10716, 1000.000000000000000 ) ;
#60704=DIRECTION ( 'NONE',  ( 0.7142857142857395036, 0.000000000000000000, 0.6998542122237394469 ) ) ;
#60710=LINE ( 'NONE', #23223, #10056 ) ;
#60712=DIRECTION ( 'NONE',  ( -1.000000000000000000, 0.000000000000000000, 0.000000000000000000 ) ) ;
#60716=ORIENTED_EDGE ( 'NONE', *, *, #60362, .F. ) ;
#60726=CARTESIAN_POINT ( 'NONE',  ( 17.00000000000000000, -17.50000000000000000, 19.33772233983200195 ) ) ;
#60728=VECTOR ( 'NONE', #3617, 1000.000000000000000 ) ;
#60730=CARTESIAN_POINT ( 'NONE',  ( -24.00000000000000000, -15.50000000000000000, -19.33772233983200195 ) ) ;
#60743=AXIS2_PLACEMENT_3D ( 'NONE', #16601, #59379, #331 ) ;
#60746=DIRECTION ( 'NONE',  ( 0.000000000000000000, 1.000000000000000000, 0.000000000000000000 ) ) ;
#60747=VERTEX_POINT ( 'NONE', #25143 ) ;
#60752=LINE ( 'NONE', #12299, #28848 ) ;
#60755=CARTESIAN_POINT ( 'NONE',  ( -11.00000000000000000, -5.599999999999999645, -9.000000000000001776 ) ) ;
#60756=ORIENTED_EDGE ( 'NONE', *, *, #69077, .F. ) ;
#60764=EDGE_CURVE ( 'NONE', #60323, #5255, #51472, .T. ) ;
#60765=EDGE_CURVE ( 'NONE', #46144, #2815, #18701, .T. ) ;
#60768=DIRECTION ( 'NONE',  ( 0.000000000000000000, 1.000000000000000000, 0.000000000000000000 ) ) ;
#60774=EDGE_LOOP ( 'NONE', ( #67113, #36784, #17500, #1392 ) ) ;
#60779=EDGE_CURVE ( 'NONE', #11224, #1993, #63683, .T. ) ;
#60780=VERTEX_POINT ( 'NONE', #58015 ) ;
#60781=DIRECTION ( 'NONE',  ( -1.000000000000000000, 0.000000000000000000, 0.000000000000000000 ) ) ;
#60790=ORIENTED_EDGE ( 'NONE', *, *, #68385, .F. ) ;
#60795=EDGE_LOOP ( 'NONE', ( #40325, #43930, #42608, #29615, #32795, #65533, #30921, #13579, #29424, #13168, #9627, #55113, #64606, #15314, #58467, #6541, #2142, #24729 ) ) ;
#60798=CARTESIAN_POINT ( 'NONE',  ( 30.00000000000000000, -14.33999999999999986, 14.50000000000000000 ) ) ;
#60800=CARTESIAN_POINT ( 'NONE',  ( -11.00000000000000000, -12.00000000000000000, -12.20000000000000107 ) ) ;
#60801=DIRECTION ( 'NONE',  ( 0.4999999999999827360, 0.000000000000000000, 0.8660254037844485886 ) ) ;
#60802=DIRECTION ( 'NONE',  ( -1.000000000000000000, 0.000000000000000000, 0.000000000000000000 ) ) ;
#60805=DIRECTION ( 'NONE',  ( 0.000000000000000000, 1.000000000000000000, 0.000000000000000000 ) ) ;
#60814=ORIENTED_EDGE ( 'NONE', *, *, #21771, .F. ) ;
#60817=ORIENTED_EDGE ( 'NONE', *, *, #27543, .T. ) ;
#60825=LINE ( 'NONE', #66824, #37318 ) ;
#60827=EDGE_CURVE ( 'NONE', #23822, #4107, #36860, .T. ) ;
#60828=ORIENTED_EDGE ( 'NONE', *, *, #3804, .F. ) ;
#60829=DIRECTION ( 'NONE',  ( 0.000000000000000000, 1.000000000000000000, 0.000000000000000000 ) ) ;
#60837=FACE_OUTER_BOUND ( 'NONE', #10714, .T. ) ;
#60856=EDGE_CURVE ( 'NONE', #16696, #9744, #15600, .T. ) ;
#60866=EDGE_CURVE ( 'NONE', #44584, #24243, #21245, .T. ) ;
#60877=DIRECTION ( 'NONE',  ( 0.000000000000000000, 0.000000000000000000, 1.000000000000000000 ) ) ;
#60881=EDGE_CURVE ( 'NONE', #38679, #24526, #4974, .T. ) ;
#60884=DIRECTION ( 'NONE',  ( 0.000000000000000000, 0.000000000000000000, -1.000000000000000000 ) ) ;
#60886=EDGE_CURVE ( 'NONE', #46437, #42264, #16273, .T. ) ;
#60889=CARTESIAN_POINT ( 'NONE',  ( -11.00000000000000000, -5.200000000000001066, 60.00000000000000000 ) ) ;
#60893=CARTESIAN_POINT ( 'NONE',  ( 29.50000000000000355, -11.50000000000000000, -11.00000000000000000 ) ) ;
#60898=ORIENTED_EDGE ( 'NONE', *, *, #59723, .T. ) ;
#60908=EDGE_CURVE ( 'NONE', #28990, #62386, #53773, .T. ) ;
#60911=CYLINDRICAL_SURFACE ( 'NONE', #15504, 4.000000000000000000 ) ;
#60914=VERTEX_POINT ( 'NONE', #54800 ) ;
#60921=ORIENTED_EDGE ( 'NONE', *, *, #52477, .F. ) ;
#60924=DIRECTION ( 'NONE',  ( -1.000000000000000000, 0.000000000000000000, 0.000000000000000000 ) ) ;
#60926=DIRECTION ( 'NONE',  ( 0.000000000000000000, 1.000000000000000000, 0.000000000000000000 ) ) ;
#60931=ORIENTED_EDGE ( 'NONE', *, *, #7810, .T. ) ;
#60942=ORIENTED_EDGE ( 'NONE', *, *, #50117, .T. ) ;
#60945=CARTESIAN_POINT ( 'NONE',  ( -14.25000000000000000, -2.500000000000000000, 21.77831216351300014 ) ) ;
#60962=CARTESIAN_POINT ( 'NONE',  ( 28.00000000000000000, -16.64230188589300141, 14.64519951917099583 ) ) ;
#60968=LINE ( 'NONE', #68037, #5187 ) ;
#60969=VERTEX_POINT ( 'NONE', #6694 ) ;
#60971=EDGE_CURVE ( 'NONE', #65126, #11924, #34248, .T. ) ;
#60978=EDGE_CURVE ( 'NONE', #48159, #36748, #18758, .T. ) ;
#60989=AXIS2_PLACEMENT_3D ( 'NONE', #27434, #59952, #59619 ) ;
#60993=LINE ( 'NONE', #50042, #42283 ) ;
#61004=ORIENTED_EDGE ( 'NONE', *, *, #5608, .F. ) ;
#61005=VECTOR ( 'NONE', #60802, 1000.000000000000000 ) ;
#61007=DIRECTION ( 'NONE',  ( 0.000000000000000000, -1.000000000000000000, 0.000000000000000000 ) ) ;
#61010=EDGE_LOOP ( 'NONE', ( #34210, #5749, #8130, #37534, #25104, #30774, #51186, #59804, #3741, #61035, #17239, #10738, #2069, #64718, #42324, #39028, #63267, #25201 ) ) ;
#61015=DIRECTION ( 'NONE',  ( 0.000000000000000000, 0.000000000000000000, -1.000000000000000000 ) ) ;
#61016=EDGE_CURVE ( 'NONE', #27989, #65011, #18692, .T. ) ;
#61021=DIRECTION ( 'NONE',  ( -1.000000000000000000, 0.000000000000000000, 0.000000000000000000 ) ) ;
#61027=CIRCLE ( 'NONE', #2343, 4.000000000000000888 ) ;
#61030=DIRECTION ( 'NONE',  ( 1.000000000000000000, -0.000000000000000000, -0.000000000000000000 ) ) ;
#61033=EDGE_LOOP ( 'NONE', ( #63183, #18441, #42874, #29431 ) ) ;
#61035=ORIENTED_EDGE ( 'NONE', *, *, #10823, .F. ) ;
#61036=VECTOR ( 'NONE', #59280, 1000.000000000000000 ) ;
#61042=ADVANCED_FACE ( 'NONE', ( #65751 ), #55148, .T. ) ;
#61046=ORIENTED_EDGE ( 'NONE', *, *, #27990, .F. ) ;
#61048=PLANE ( 'NONE',  #38867 ) ;
#61057=DIRECTION ( 'NONE',  ( 0.000000000000000000, 0.000000000000000000, 1.000000000000000000 ) ) ;
#61059=DIRECTION ( 'NONE',  ( 0.000000000000000000, -0.1249999999999996531, -0.9921567416492215186 ) ) ;
#61064=CARTESIAN_POINT ( 'NONE',  ( 0.000000000000000000, -5.000000000000000000, 0.000000000000000000 ) ) ;
#61065=DIRECTION ( 'NONE',  ( 0.000000000000000000, -1.000000000000000000, 0.000000000000000000 ) ) ;
#61066=DIRECTION ( 'NONE',  ( -0.000000000000000000, 1.000000000000000000, -0.000000000000000000 ) ) ;
#61080=ORIENTED_EDGE ( 'NONE', *, *, #60764, .F. ) ;
#61081=DIRECTION ( 'NONE',  ( 0.000000000000000000, 0.000000000000000000, -1.000000000000000000 ) ) ;
#61088=DIRECTION ( 'NONE',  ( 0.000000000000000000, 1.000000000000000000, 0.000000000000000000 ) ) ;
#61089=ORIENTED_EDGE ( 'NONE', *, *, #23731, .T. ) ;
#61093=CIRCLE ( 'NONE', #22760, 4.000000000000000888 ) ;
#61098=VECTOR ( 'NONE', #51948, 999.9999999999998863 ) ;
#61101=EDGE_CURVE ( 'NONE', #14586, #20510, #61468, .T. ) ;
#61104=FACE_OUTER_BOUND ( 'NONE', #48492, .T. ) ;
#61106=ORIENTED_EDGE ( 'NONE', *, *, #12518, .F. ) ;
#61108=EDGE_LOOP ( 'NONE', ( #8320, #37724, #32621, #61165, #18734, #59878 ) ) ;
#61128=LINE ( 'NONE', #6030, #5756 ) ;
#61129=EDGE_LOOP ( 'NONE', ( #11473, #42958, #45724, #47865 ) ) ;
#61146=ORIENTED_EDGE ( 'NONE', *, *, #41686, .F. ) ;
#61147=DIRECTION ( 'NONE',  ( -1.000000000000000000, 0.000000000000000000, 0.000000000000000000 ) ) ;
#61151=CIRCLE ( 'NONE', #9248, 3.499999999999999556 ) ;
#61157=DIRECTION ( 'NONE',  ( -0.9583148474998870459, 0.000000000000000000, 0.2857142857143623593 ) ) ;
#61158=CARTESIAN_POINT ( 'NONE',  ( 29.50000000000000355, -15.97213595500069871, 14.50000000000000000 ) ) ;
#61165=ORIENTED_EDGE ( 'NONE', *, *, #60056, .T. ) ;
#61170=DIRECTION ( 'NONE',  ( 0.000000000000000000, 0.000000000000000000, -1.000000000000000000 ) ) ;
#61179=DIRECTION ( 'NONE',  ( 1.000000000000000000, 0.000000000000000000, 0.000000000000000000 ) ) ;
#61182=CARTESIAN_POINT ( 'NONE',  ( -11.00000000000000000, -11.10796162543699950, -9.102987789146602893 ) ) ;
#61183=CARTESIAN_POINT ( 'NONE',  ( -16.89194109070750116, -5.000000000000000000, 26.25000000000000000 ) ) ;
#61187=ORIENTED_EDGE ( 'NONE', *, *, #23731, .F. ) ;
#61189=ORIENTED_EDGE ( 'NONE', *, *, #32325, .F. ) ;
#61193=AXIS2_PLACEMENT_3D ( 'NONE', #2405, #28579, #33877 ) ;
#61196=FACE_OUTER_BOUND ( 'NONE', #48705, .T. ) ;
#61212=VERTEX_POINT ( 'NONE', #40612 ) ;
#61215=DIRECTION ( 'NONE',  ( 0.000000000000000000, 1.000000000000000000, 0.000000000000000000 ) ) ;
#61224=CARTESIAN_POINT ( 'NONE',  ( -17.00000000000000000, -16.64230188589300141, 14.64519951917099583 ) ) ;
#61227=DIRECTION ( 'NONE',  ( 0.000000000000000000, 1.000000000000000000, 0.000000000000000000 ) ) ;
#61238=ADVANCED_FACE ( 'NONE', ( #40957, #52641 ), #4208, .T. ) ;
#61242=ORIENTED_EDGE ( 'NONE', *, *, #23005, .F. ) ;
#61246=AXIS2_PLACEMENT_3D ( 'NONE', #41611, #41962, #26063 ) ;
#61251=VECTOR ( 'NONE', #8203, 1000.000000000000000 ) ;
#61272=DIRECTION ( 'NONE',  ( 0.000000000000000000, 1.000000000000000000, 0.000000000000000000 ) ) ;
#61273=CARTESIAN_POINT ( 'NONE',  ( -29.50000000000000355, -11.50000000000000000, 15.00000000000000000 ) ) ;
#61280=DIRECTION ( 'NONE',  ( 0.000000000000000000, 1.000000000000000000, 0.000000000000000000 ) ) ;
#61289=ORIENTED_EDGE ( 'NONE', *, *, #44149, .T. ) ;
#61292=DIRECTION ( 'NONE',  ( 1.060575238724893480E-16, 0.5000000000000189848, -0.8660254037844277164 ) ) ;
#61296=ORIENTED_EDGE ( 'NONE', *, *, #6561, .F. ) ;
#61306=DIRECTION ( 'NONE',  ( 0.000000000000000000, 0.000000000000000000, 1.000000000000000000 ) ) ;
#61321=AXIS2_PLACEMENT_3D ( 'NONE', #41452, #41092, #25903 ) ;
#61322=ORIENTED_EDGE ( 'NONE', *, *, #46608, .T. ) ;
#61334=DIRECTION ( 'NONE',  ( 0.000000000000000000, 0.000000000000000000, 1.000000000000000000 ) ) ;
#61335=EDGE_LOOP ( 'NONE', ( #44800, #63644, #1724, #42636 ) ) ;
#61344=AXIS2_PLACEMENT_3D ( 'NONE', #47786, #68311, #20215 ) ;
#61348=ORIENTED_EDGE ( 'NONE', *, *, #9247, .T. ) ;
#61354=AXIS2_PLACEMENT_3D ( 'NONE', #4129, #51145, #13667 ) ;
#61355=EDGE_LOOP ( 'NONE', ( #21365, #20874, #9392, #10873 ) ) ;
#61358=FACE_OUTER_BOUND ( 'NONE', #27921, .T. ) ;
#61362=FACE_OUTER_BOUND ( 'NONE', #59037, .T. ) ;
#61366=CARTESIAN_POINT ( 'NONE',  ( 15.50000000000000000, -15.50000000000000000, -22.50000000000000000 ) ) ;
#61379=ORIENTED_EDGE ( 'NONE', *, *, #62749, .T. ) ;
#61381=DIRECTION ( 'NONE',  ( 0.000000000000000000, -0.9938079899998859545, -0.1111111111112941946 ) ) ;
#61382=FACE_OUTER_BOUND ( 'NONE', #63137, .T. ) ;
#61387=DIRECTION ( 'NONE',  ( -0.3479852726768748461, 0.000000000000000000, 0.9375000000000006661 ) ) ;
#61400=DIRECTION ( 'NONE',  ( -1.000000000000000000, 0.000000000000000000, 0.000000000000000000 ) ) ;
#61405=EDGE_CURVE ( 'NONE', #32707, #29553, #19982, .T. ) ;
#61414=VERTEX_POINT ( 'NONE', #10278 ) ;
#61417=CARTESIAN_POINT ( 'NONE',  ( -23.48000000000000043, -15.50000000000000000, -26.00000000000000355 ) ) ;
#61418=CARTESIAN_POINT ( 'NONE',  ( -29.50000000000000355, -12.00000000000000000, -11.03137303340310282 ) ) ;
#61421=LINE ( 'NONE', #33867, #29605 ) ;
#61424=ORIENTED_EDGE ( 'NONE', *, *, #48362, .T. ) ;
#61426=DIRECTION ( 'NONE',  ( -1.000000000000000000, 0.000000000000000000, 0.000000000000000000 ) ) ;
#61441=EDGE_LOOP ( 'NONE', ( #52275, #34111, #16462, #346, #17203, #53232, #62725 ) ) ;
#61444=CARTESIAN_POINT ( 'NONE',  ( 25.50000000000000355, 0.000000000000000000, 20.24999999999999645 ) ) ;
#61468=LINE ( 'NONE', #13026, #715 ) ;
#61469=ORIENTED_EDGE ( 'NONE', *, *, #759, .T. ) ;
#61484=CARTESIAN_POINT ( 'NONE',  ( 30.00000000000000000, -17.14999999999900027, -26.64999999999900027 ) ) ;
#61487=DIRECTION ( 'NONE',  ( 0.3479852726768751237, 0.000000000000000000, -0.9375000000000004441 ) ) ;
#61505=DIRECTION ( 'NONE',  ( 0.000000000000000000, -0.9921567416492215186, 0.1249999999999996531 ) ) ;
#61509=DIRECTION ( 'NONE',  ( 0.000000000000000000, 0.7046037717862339012, 0.7096009616570518874 ) ) ;
#61512=EDGE_LOOP ( 'NONE', ( #11121, #61625, #56902, #57742 ) ) ;
#61513=DIRECTION ( 'NONE',  ( 0.000000000000000000, 1.000000000000000000, 0.000000000000000000 ) ) ;
#61520=CARTESIAN_POINT ( 'NONE',  ( 18.85410196625000268, -15.50000000000000000, 21.50000000000000000 ) ) ;
#61521=ORIENTED_EDGE ( 'NONE', *, *, #15383, .F. ) ;
#61523=CARTESIAN_POINT ( 'NONE',  ( -25.50000000000000355, -5.578999999999999737, -24.12099999999999511 ) ) ;
#61524=AXIS2_PLACEMENT_3D ( 'NONE', #35945, #57852, #52567 ) ;
#61532=ORIENTED_EDGE ( 'NONE', *, *, #15914, .T. ) ;
#61536=ORIENTED_EDGE ( 'NONE', *, *, #52887, .T. ) ;
#61539=EDGE_CURVE ( 'NONE', #49372, #69377, #1731, .T. ) ;
#61540=FACE_OUTER_BOUND ( 'NONE', #68967, .T. ) ;
#61548=ORIENTED_EDGE ( 'NONE', *, *, #27320, .T. ) ;
#61556=CIRCLE ( 'NONE', #2820, 3.499999999999056310 ) ;
#61558=VERTEX_POINT ( 'NONE', #33906 ) ;
#61566=DIRECTION ( 'NONE',  ( 0.000000000000000000, 0.000000000000000000, 1.000000000000000000 ) ) ;
#61570=CARTESIAN_POINT ( 'NONE',  ( 14.25000000000000000, -2.500000000000000000, 21.77831216351300014 ) ) ;
#61573=ORIENTED_EDGE ( 'NONE', *, *, #12518, .T. ) ;
#61575=DIRECTION ( 'NONE',  ( 0.000000000000000000, 1.000000000000000000, 0.000000000000000000 ) ) ;
#61577=CARTESIAN_POINT ( 'NONE',  ( -16.75000000000000000, -2.500000000000000000, 21.77831216351300014 ) ) ;
#61580=DIRECTION ( 'NONE',  ( 0.000000000000000000, -1.000000000000000000, 0.000000000000000000 ) ) ;
#61582=CYLINDRICAL_SURFACE ( 'NONE', #56271, 0.5000000000001374456 ) ;
#61583=CIRCLE ( 'NONE', #41256, 4.000000000000000888 ) ;
#61591=CIRCLE ( 'NONE', #4044, 2.250000000000001776 ) ;
#61596=ORIENTED_EDGE ( 'NONE', *, *, #26840, .F. ) ;
#61598=CARTESIAN_POINT ( 'NONE',  ( -15.50000000000000000, -0.1999999999999999556, 21.05000000000000071 ) ) ;
#61607=CARTESIAN_POINT ( 'NONE',  ( -25.50000000000000355, 0.000000000000000000, 24.75000000000000000 ) ) ;
#61625=ORIENTED_EDGE ( 'NONE', *, *, #69075, .F. ) ;
#61629=FACE_OUTER_BOUND ( 'NONE', #17955, .T. ) ;
#61633=EDGE_CURVE ( 'NONE', #27877, #26707, #15505, .T. ) ;
#61634=ORIENTED_EDGE ( 'NONE', *, *, #18671, .T. ) ;
#61639=DIRECTION ( 'NONE',  ( 0.000000000000000000, 1.000000000000000000, 0.000000000000000000 ) ) ;
#61640=ORIENTED_EDGE ( 'NONE', *, *, #36280, .F. ) ;
#61651=ORIENTED_EDGE ( 'NONE', *, *, #32474, .T. ) ;
#61653=ORIENTED_EDGE ( 'NONE', *, *, #60366, .F. ) ;
#61654=CARTESIAN_POINT ( 'NONE',  ( 25.50000000000000355, -5.200000000000001066, 24.50000000000000000 ) ) ;
#61658=LINE ( 'NONE', #41141, #47613 ) ;
#61659=DIRECTION ( 'NONE',  ( -1.000000000000000000, 0.000000000000000000, 0.000000000000000000 ) ) ;
#61662=ORIENTED_EDGE ( 'NONE', *, *, #46039, .F. ) ;
#61677=CARTESIAN_POINT ( 'NONE',  ( -29.50000000000000355, -12.00000000000000000, 10.52786404500095863 ) ) ;
#61681=DIRECTION ( 'NONE',  ( 1.000000000000000000, 0.000000000000000000, 0.000000000000000000 ) ) ;
#61684=ORIENTED_EDGE ( 'NONE', *, *, #18278, .F. ) ;
#61691=ORIENTED_EDGE ( 'NONE', *, *, #37552, .F. ) ;
#61692=DIRECTION ( 'NONE',  ( -1.000000000000000000, 0.000000000000000000, 0.000000000000000000 ) ) ;
#61696=VECTOR ( 'NONE', #41054, 1000.000000000000000 ) ;
#61699=CARTESIAN_POINT ( 'NONE',  ( 14.10805890929250062, -5.000000000000000000, 26.25000000000000000 ) ) ;
#61704=VECTOR ( 'NONE', #23259, 1000.000000000000000 ) ;
#61712=AXIS2_PLACEMENT_3D ( 'NONE', #56771, #1627, #23901 ) ;
#61714=EDGE_CURVE ( 'NONE', #50247, #21845, #16109, .T. ) ;
#61716=EDGE_CURVE ( 'NONE', #51933, #11521, #13205, .T. ) ;
#61725=DIRECTION ( 'NONE',  ( 0.000000000000000000, 1.000000000000000000, 0.000000000000000000 ) ) ;
#61727=EDGE_CURVE ( 'NONE', #29478, #67299, #53258, .T. ) ;
#61730=FACE_OUTER_BOUND ( 'NONE', #54339, .T. ) ;
#61732=CARTESIAN_POINT ( 'NONE',  ( 17.00000000000000000, -15.50000000000000000, -19.33772233983200195 ) ) ;
#61744=ORIENTED_EDGE ( 'NONE', *, *, #49994, .T. ) ;
#61748=CARTESIAN_POINT ( 'NONE',  ( -14.25000000000000000, -2.500000000000000000, -21.77831216351300014 ) ) ;
#61750=VECTOR ( 'NONE', #20817, 1000.000000000000000 ) ;
#61755=LINE ( 'NONE', #41230, #6341 ) ;
#61765=LINE ( 'NONE', #68477, #19500 ) ;
#61771=LINE ( 'NONE', #51155, #1946 ) ;
#61777=DIRECTION ( 'NONE',  ( 0.000000000000000000, 1.000000000000000000, 0.000000000000000000 ) ) ;
#61786=FACE_OUTER_BOUND ( 'NONE', #2299, .T. ) ;
#61788=CARTESIAN_POINT ( 'NONE',  ( 30.00000000000000000, -13.54524521594299991, 17.53999999999999915 ) ) ;
#61793=CARTESIAN_POINT ( 'NONE',  ( 30.00000000000000000, -11.50000000000100009, -15.00000000000084910 ) ) ;
#61796=COLOUR_RGB ( '', 0.09019608, 0.27058824, 0.51372549) ;
#61804=CARTESIAN_POINT ( 'NONE',  ( 17.00000000000000000, -16.28999999999999915, -14.50000000000000000 ) ) ;
#61811=VERTEX_POINT ( 'NONE', #48634 ) ;
#61814=AXIS2_PLACEMENT_3D ( 'NONE', #33957, #60829, #12378 ) ;
#61815=CIRCLE ( 'NONE', #69763, 3.499999999999999556 ) ;
#61816=LINE ( 'NONE', #51556, #31653 ) ;
#61824=FACE_OUTER_BOUND ( 'NONE', #64902, .T. ) ;
#61825=DIRECTION ( 'NONE',  ( -1.000000000000000000, 0.000000000000000000, 0.000000000000000000 ) ) ;
#61828=ORIENTED_EDGE ( 'NONE', *, *, #6899, .F. ) ;
#61838=ORIENTED_EDGE ( 'NONE', *, *, #42442, .F. ) ;
#61852=ORIENTED_EDGE ( 'NONE', *, *, #59032, .T. ) ;
#61855=DIRECTION ( 'NONE',  ( 0.000000000000000000, -1.000000000000000000, 0.000000000000000000 ) ) ;
#61864=CARTESIAN_POINT ( 'NONE',  ( 29.50000000000000355, -11.50000000000000000, -15.00000000000000000 ) ) ;
#61866=CARTESIAN_POINT ( 'NONE',  ( 30.00000000000000000, -11.10796162543699950, 9.102987789146602893 ) ) ;
#61867=DIRECTION ( 'NONE',  ( 0.4998444328988824181, 0.000000000000000000, -0.8661152018640445593 ) ) ;
#61873=CARTESIAN_POINT ( 'NONE',  ( 29.25000000000000000, -5.000000000000000000, -11.75000000000000000 ) ) ;
#61877=ORIENTED_EDGE ( 'NONE', *, *, #13082, .F. ) ;
#61886=ORIENTED_EDGE ( 'NONE', *, *, #50946, .T. ) ;
#61892=DIRECTION ( 'NONE',  ( -1.000000000000000000, 0.000000000000000000, 0.000000000000000000 ) ) ;
#61893=ORIENTED_EDGE ( 'NONE', *, *, #52133, .F. ) ;
#61894=CARTESIAN_POINT ( 'NONE',  ( 30.00000000000000000, -9.199999999999999289, -12.69999999999986073 ) ) ;
#61904=CARTESIAN_POINT ( 'NONE',  ( 30.00000000000000000, -13.79999999999979998, 17.30000000000000071 ) ) ;
#61907=ORIENTED_EDGE ( 'NONE', *, *, #3063, .F. ) ;
#61910=EDGE_CURVE ( 'NONE', #43603, #44628, #17753, .T. ) ;
#61913=ORIENTED_EDGE ( 'NONE', *, *, #19685, .F. ) ;
#61919=CARTESIAN_POINT ( 'NONE',  ( 30.00000000000000000, -5.200000000000001066, -11.75000000000000000 ) ) ;
#61921=EDGE_LOOP ( 'NONE', ( #34870, #2446, #23594, #4462 ) ) ;
#61934=DIRECTION ( 'NONE',  ( 1.000000000000000000, -0.000000000000000000, -0.000000000000000000 ) ) ;
#61941=DIRECTION ( 'NONE',  ( 0.000000000000000000, 0.000000000000000000, -1.000000000000000000 ) ) ;
#61944=DIRECTION ( 'NONE',  ( 0.000000000000000000, 0.000000000000000000, -1.000000000000000000 ) ) ;
#61945=ORIENTED_EDGE ( 'NONE', *, *, #3612, .T. ) ;
#61956=VERTEX_POINT ( 'NONE', #2971 ) ;
#61963=ORIENTED_EDGE ( 'NONE', *, *, #7164, .T. ) ;
#61964=DIRECTION ( 'NONE',  ( -0.000000000000000000, 1.000000000000000000, -0.000000000000000000 ) ) ;
#61965=VECTOR ( 'NONE', #66370, 1000.000000000000000 ) ;
#61972=ORIENTED_EDGE ( 'NONE', *, *, #13824, .F. ) ;
#61975=DIRECTION ( 'NONE',  ( -1.000000000000000000, 0.000000000000000000, 0.000000000000000000 ) ) ;
#61979=CARTESIAN_POINT ( 'NONE',  ( 30.00000000000000000, -5.200000000000001066, 11.75000000000000000 ) ) ;
#61994=ORIENTED_EDGE ( 'NONE', *, *, #580, .F. ) ;
#62002=ORIENTED_EDGE ( 'NONE', *, *, #9407, .F. ) ;
#62012=DIRECTION ( 'NONE',  ( 0.000000000000000000, -0.9921567416492215186, 0.1249999999999996531 ) ) ;
#62013=DIRECTION ( 'NONE',  ( 0.000000000000000000, 0.000000000000000000, 1.000000000000000000 ) ) ;
#62014=CONICAL_SURFACE ( 'NONE', #59759, 1.621000000000000885, 0.7853981633974518317 ) ;
#62017=CARTESIAN_POINT ( 'NONE',  ( -30.00000000000000000, -14.33999999999999986, -14.50000000000000000 ) ) ;
#62019=CARTESIAN_POINT ( 'NONE',  ( -15.50000000000000000, -0.1999999999999999556, 23.94999999999999929 ) ) ;
#62026=ORIENTED_EDGE ( 'NONE', *, *, #17497, .T. ) ;
#62028=CARTESIAN_POINT ( 'NONE',  ( -25.50000000000000355, -5.200000000000001066, 24.50000000000000000 ) ) ;
#62031=ORIENTED_EDGE ( 'NONE', *, *, #60827, .T. ) ;
#62041=EDGE_CURVE ( 'NONE', #66059, #18896, #34697, .T. ) ;
#62048=VECTOR ( 'NONE', #62398, 1000.000000000000000 ) ;
#62056=CARTESIAN_POINT ( 'NONE',  ( 30.00000000000000000, -11.50000000000000000, -11.00000000000000000 ) ) ;
#62058=VECTOR ( 'NONE', #18032, 1000.000000000000000 ) ;
#62075=CARTESIAN_POINT ( 'NONE',  ( 29.25000000000000000, -5.200000000000001066, 11.75000000000000000 ) ) ;
#62082=ORIENTED_EDGE ( 'NONE', *, *, #35118, .F. ) ;
#62088=VECTOR ( 'NONE', #42597, 1000.000000000000114 ) ;
#62094=VERTEX_POINT ( 'NONE', #20623 ) ;
#62096=DIRECTION ( 'NONE',  ( -0.8660254037844482555, 0.000000000000000000, 0.4999999999999831801 ) ) ;
#62098=CARTESIAN_POINT ( 'NONE',  ( -25.50000000000000355, 0.000000000000000000, 22.50000000000000000 ) ) ;
#62102=VECTOR ( 'NONE', #44471, 1000.000000000000000 ) ;
#62109=AXIS2_PLACEMENT_3D ( 'NONE', #33280, #6065, #73 ) ;
#62116=DIRECTION ( 'NONE',  ( 0.000000000000000000, 1.000000000000000000, 0.000000000000000000 ) ) ;
#62117=ORIENTED_EDGE ( 'NONE', *, *, #21496, .T. ) ;
#62118=PLANE ( 'NONE',  #68230 ) ;
#62126=CARTESIAN_POINT ( 'NONE',  ( -17.51999999999999957, -15.50000000000000000, -26.00000000000000355 ) ) ;
#62129=CARTESIAN_POINT ( 'NONE',  ( 30.00000000000000000, -17.14999999999999858, -27.00000000000000000 ) ) ;
#62137=VERTEX_POINT ( 'NONE', #36188 ) ;
#62149=VECTOR ( 'NONE', #62619, 1000.000000000000000 ) ;
#62153=DIRECTION ( 'NONE',  ( -1.000000000000000000, 0.000000000000000000, 0.000000000000000000 ) ) ;
#62160=AXIS2_PLACEMENT_3D ( 'NONE', #15801, #63897, #43013 ) ;
#62161=EDGE_CURVE ( 'NONE', #41930, #52180, #61815, .T. ) ;
#62164=ORIENTED_EDGE ( 'NONE', *, *, #65506, .T. ) ;
#62166=FACE_OUTER_BOUND ( 'NONE', #65413, .T. ) ;
#62168=ORIENTED_EDGE ( 'NONE', *, *, #58341, .F. ) ;
#62175=EDGE_LOOP ( 'NONE', ( #32807, #32578, #37040, #41297 ) ) ;
#62181=LINE ( 'NONE', #48382, #10942 ) ;
#62188=ORIENTED_EDGE ( 'NONE', *, *, #30918, .T. ) ;
#62193=DIRECTION ( 'NONE',  ( 1.000000000000000000, 0.000000000000000000, 0.000000000000000000 ) ) ;
#62199=CARTESIAN_POINT ( 'NONE',  ( 17.51999999999999957, -17.50000000000000000, 26.00000000000000355 ) ) ;
#62220=CARTESIAN_POINT ( 'NONE',  ( 17.00000000000000000, -17.50000000000000000, 15.70499999999969809 ) ) ;
#62221=EDGE_CURVE ( 'NONE', #60780, #14841, #12142, .T. ) ;
#62225=DIRECTION ( 'NONE',  ( 0.000000000000000000, 1.000000000000000000, 0.000000000000000000 ) ) ;
#62228=AXIS2_PLACEMENT_3D ( 'NONE', #61484, #13052, #34622 ) ;
#62231=ORIENTED_EDGE ( 'NONE', *, *, #33828, .F. ) ;
#62232=ORIENTED_EDGE ( 'NONE', *, *, #65791, .T. ) ;
#62237=DIRECTION ( 'NONE',  ( 0.000000000000000000, 1.000000000000000000, 0.000000000000000000 ) ) ;
#62246=DIRECTION ( 'NONE',  ( 0.000000000000000000, 0.000000000000000000, -1.000000000000000000 ) ) ;
#62260=FACE_OUTER_BOUND ( 'NONE', #43953, .T. ) ;
#62264=LINE ( 'NONE', #35745, #12707 ) ;
#62269=CARTESIAN_POINT ( 'NONE',  ( -11.00000000000000000, -17.50000000000000000, 26.64999999999999858 ) ) ;
#62282=CYLINDRICAL_SURFACE ( 'NONE', #34909, 4.500000000000188294 ) ;
#62290=DIRECTION ( 'NONE',  ( 0.000000000000000000, 0.000000000000000000, 1.000000000000000000 ) ) ;
#62297=DIRECTION ( 'NONE',  ( 0.000000000000000000, 0.000000000000000000, -1.000000000000000000 ) ) ;
#62298=EDGE_CURVE ( 'NONE', #42454, #52350, #28025, .T. ) ;
#62308=PLANE ( 'NONE',  #21828 ) ;
#62312=DIRECTION ( 'NONE',  ( 0.000000000000000000, 1.000000000000000000, 0.000000000000000000 ) ) ;
#62314=VERTEX_POINT ( 'NONE', #125 ) ;
#62316=DIRECTION ( 'NONE',  ( 0.000000000000000000, 0.000000000000000000, 1.000000000000000000 ) ) ;
#62318=VECTOR ( 'NONE', #56241, 1000.000000000000000 ) ;
#62320=DIRECTION ( 'NONE',  ( -0.4999999999999832356, 0.000000000000000000, -0.8660254037844483666 ) ) ;
#62321=CARTESIAN_POINT ( 'NONE',  ( 30.00000000000000000, -12.00000000000000000, 12.20000000000000107 ) ) ;
#62327=ORIENTED_EDGE ( 'NONE', *, *, #52934, .F. ) ;
#62333=EDGE_CURVE ( 'NONE', #20373, #38076, #16731, .T. ) ;
#62338=CARTESIAN_POINT ( 'NONE',  ( -29.50000000000000355, -15.46862696659690073, -14.50000000000000000 ) ) ;
#62351=VERTEX_POINT ( 'NONE', #62269 ) ;
#62360=EDGE_LOOP ( 'NONE', ( #63053, #66448, #9399, #51002 ) ) ;
#62368=AXIS2_PLACEMENT_3D ( 'NONE', #49308, #26337, #11454 ) ;
#62373=CARTESIAN_POINT ( 'NONE',  ( -25.50000000000000355, 0.000000000000000000, 22.50000000000000000 ) ) ;
#62377=LINE ( 'NONE', #36214, #52560 ) ;
#62381=CARTESIAN_POINT ( 'NONE',  ( -11.00000000000000000, -16.64230188589299786, 14.64519951917100116 ) ) ;
#62386=VERTEX_POINT ( 'NONE', #24091 ) ;
#62388=FACE_OUTER_BOUND ( 'NONE', #28051, .T. ) ;
#62395=ORIENTED_EDGE ( 'NONE', *, *, #23994, .T. ) ;
#62396=CARTESIAN_POINT ( 'NONE',  ( 15.70366306705350112, -0.2717122460102739390, -23.82579074638668004 ) ) ;
#62397=ORIENTED_EDGE ( 'NONE', *, *, #19977, .T. ) ;
#62398=DIRECTION ( 'NONE',  ( -1.000000000000000000, 0.000000000000000000, 0.000000000000000000 ) ) ;
#62400=CARTESIAN_POINT ( 'NONE',  ( 17.00000000000000000, -15.50000000000000000, -14.50000000000000000 ) ) ;
#62408=CARTESIAN_POINT ( 'NONE',  ( 15.50000000000000000, -0.4000000000000000222, 22.50000000000000000 ) ) ;
#62415=DIRECTION ( 'NONE',  ( 0.000000000000000000, 0.000000000000000000, 1.000000000000000000 ) ) ;
#62420=CARTESIAN_POINT ( 'NONE',  ( 17.00000000000000000, -16.64230188589299786, -14.64519951917100116 ) ) ;
#62430=ORIENTED_EDGE ( 'NONE', *, *, #41942, .F. ) ;
#62431=ORIENTED_EDGE ( 'NONE', *, *, #1602, .T. ) ;
#62435=VECTOR ( 'NONE', #14082, 1000.000000000000000 ) ;
#62437=EDGE_CURVE ( 'NONE', #26720, #23985, #39320, .T. ) ;
#62441=EDGE_LOOP ( 'NONE', ( #66168, #2880, #49379, #19152, #27889, #47882, #13726 ) ) ;
#62442=VERTEX_POINT ( 'NONE', #29741 ) ;
#62445=LINE ( 'NONE', #68116, #5934 ) ;
#62448=ORIENTED_EDGE ( 'NONE', *, *, #9509, .T. ) ;
#62449=CARTESIAN_POINT ( 'NONE',  ( 30.00000000000000000, -5.599999999999999645, 9.400000000000000355 ) ) ;
#62450=CARTESIAN_POINT ( 'NONE',  ( 11.50000000000000000, -11.50000000000000000, -15.00000000000000000 ) ) ;
#62452=FACE_OUTER_BOUND ( 'NONE', #36854, .T. ) ;
#62455=LINE ( 'NONE', #3778, #11544 ) ;
#62468=LINE ( 'NONE', #8027, #53419 ) ;
#62470=CARTESIAN_POINT ( 'NONE',  ( -15.50000000000000000, -0.1999999999999999556, 22.50000000000000000 ) ) ;
#62471=VERTEX_POINT ( 'NONE', #50272 ) ;
#62479=CIRCLE ( 'NONE', #39864, 0.3499999999999611200 ) ;
#62488=ORIENTED_EDGE ( 'NONE', *, *, #37894, .T. ) ;
#62490=DIRECTION ( 'NONE',  ( -1.000000000000000000, 0.000000000000000000, 0.000000000000000000 ) ) ;
#62507=DIRECTION ( 'NONE',  ( 0.000000000000000000, -5.800915303574361727E-12, -1.000000000000000000 ) ) ;
#62509=VECTOR ( 'NONE', #42254, 1000.000000000000000 ) ;
#62515=VECTOR ( 'NONE', #50660, 1000.000000000000000 ) ;
#62520=ADVANCED_FACE ( 'NONE', ( #24799 ), #9241, .F. ) ;
#62524=AXIS2_PLACEMENT_3D ( 'NONE', #1124, #22682, #17368 ) ;
#62530=DIRECTION ( 'NONE',  ( 0.000000000000000000, 0.000000000000000000, -1.000000000000000000 ) ) ;
#62533=ORIENTED_EDGE ( 'NONE', *, *, #16790, .T. ) ;
#62535=ORIENTED_EDGE ( 'NONE', *, *, #39298, .F. ) ;
#62537=DIRECTION ( 'NONE',  ( -1.000000000000000000, 0.000000000000000000, 0.000000000000000000 ) ) ;
#62545=CARTESIAN_POINT ( 'NONE',  ( -15.50000000000000000, -15.50000000000000000, 22.50000000000000000 ) ) ;
#62549=CARTESIAN_POINT ( 'NONE',  ( 15.50000000000000000, -15.50000000000000000, -22.50000000000000000 ) ) ;
#62550=ORIENTED_EDGE ( 'NONE', *, *, #50456, .F. ) ;
#62555=ADVANCED_FACE ( 'NONE', ( #46358 ), #9952, .F. ) ;
#62556=DIRECTION ( 'NONE',  ( -1.000000000000000000, 0.000000000000000000, 0.000000000000000000 ) ) ;
#62563=ORIENTED_EDGE ( 'NONE', *, *, #68978, .F. ) ;
#62564=DIRECTION ( 'NONE',  ( -1.000000000000000000, 0.000000000000000000, 0.000000000000000000 ) ) ;
#62566=VERTEX_POINT ( 'NONE', #62983 ) ;
#62582=DIRECTION ( 'NONE',  ( -1.000000000000000000, 0.000000000000000000, 0.000000000000000000 ) ) ;
#62587=EDGE_CURVE ( 'NONE', #36987, #28218, #37174, .T. ) ;
#62593=ORIENTED_EDGE ( 'NONE', *, *, #28485, .F. ) ;
#62611=CARTESIAN_POINT ( 'NONE',  ( 24.00000000000000000, -15.50000000000000000, -14.50000000000000000 ) ) ;
#62619=DIRECTION ( 'NONE',  ( -1.000000000000000000, 0.000000000000000000, 0.000000000000000000 ) ) ;
#62626=CARTESIAN_POINT ( 'NONE',  ( -29.50000000000000355, -11.50000000000000000, -11.00000000000000000 ) ) ;
#62633=VERTEX_POINT ( 'NONE', #59767 ) ;
#62635=CARTESIAN_POINT ( 'NONE',  ( -29.50000000000000355, -15.97213595500069871, 14.50000000000000000 ) ) ;
#62642=CARTESIAN_POINT ( 'NONE',  ( -11.00000000000000000, -12.00000000000000000, -10.20500000000000007 ) ) ;
#62643=DIRECTION ( 'NONE',  ( 0.000000000000000000, 0.000000000000000000, 1.000000000000000000 ) ) ;
#62653=ORIENTED_EDGE ( 'NONE', *, *, #18201, .F. ) ;
#62662=EDGE_CURVE ( 'NONE', #65337, #64069, #31865, .T. ) ;
#62663=LINE ( 'NONE', #68327, #58905 ) ;
#62666=FACE_OUTER_BOUND ( 'NONE', #48424, .T. ) ;
#62672=DIRECTION ( 'NONE',  ( 0.4999999999999827360, 0.000000000000000000, -0.8660254037844485886 ) ) ;
#62676=PLANE ( 'NONE',  #8512 ) ;
#62685=ORIENTED_EDGE ( 'NONE', *, *, #65606, .T. ) ;
#62687=DIRECTION ( 'NONE',  ( -1.000000000000000000, 0.000000000000000000, 0.000000000000000000 ) ) ;
#62688=CONICAL_SURFACE ( 'NONE', #4008, 2.000000000000001776, 0.7853981633974503884 ) ;
#62690=EDGE_LOOP ( 'NONE', ( #11304, #38432, #31096, #54985 ) ) ;
#62694=DIRECTION ( 'NONE',  ( -1.000000000000000000, 0.000000000000000000, 0.000000000000000000 ) ) ;
#62702=DIRECTION ( 'NONE',  ( -1.000000000000000000, 0.000000000000000000, 0.000000000000000000 ) ) ;
#62710=ORIENTED_EDGE ( 'NONE', *, *, #19821, .F. ) ;
#62714=CARTESIAN_POINT ( 'NONE',  ( -15.50000000000000000, 0.000000000000000000, -22.50000000000000000 ) ) ;
#62715=DIRECTION ( 'NONE',  ( 0.000000000000000000, 0.000000000000000000, 1.000000000000000000 ) ) ;
#62718=ORIENTED_EDGE ( 'NONE', *, *, #30756, .F. ) ;
#62719=CARTESIAN_POINT ( 'NONE',  ( -30.00000000000000000, -15.46862696659690073, -14.50000000000000000 ) ) ;
#62720=AXIS2_PLACEMENT_3D ( 'NONE', #45466, #50085, #44765 ) ;
#62725=ORIENTED_EDGE ( 'NONE', *, *, #22037, .T. ) ;
#62734=FACE_OUTER_BOUND ( 'NONE', #68954, .T. ) ;
#62740=CARTESIAN_POINT ( 'NONE',  ( -15.50000000000000000, -2.500000000000000000, -23.94337567297399971 ) ) ;
#62743=EDGE_CURVE ( 'NONE', #58530, #54344, #48204, .T. ) ;
#62744=CARTESIAN_POINT ( 'NONE',  ( -14.25000000000000000, -0.2038245569916330158, 23.22168783648699986 ) ) ;
#62747=DIRECTION ( 'NONE',  ( 0.000000000000000000, -1.000000000000000000, -2.854859206170826497E-12 ) ) ;
#62749=EDGE_CURVE ( 'NONE', #46404, #34424, #732, .T. ) ;
#62751=DIRECTION ( 'NONE',  ( 0.000000000000000000, -1.000000000000000000, 0.000000000000000000 ) ) ;
#62752=CARTESIAN_POINT ( 'NONE',  ( -11.00000000000000000, -9.199999999999999289, -12.69999999999986073 ) ) ;
#62757=DIRECTION ( 'NONE',  ( 0.000000000000000000, 1.000000000000000000, 0.000000000000000000 ) ) ;
#62758=ORIENTED_EDGE ( 'NONE', *, *, #15839, .F. ) ;
#62760=CARTESIAN_POINT ( 'NONE',  ( -13.00000000000000178, -15.50000000000000000, -20.05051025721700242 ) ) ;
#62766=VECTOR ( 'NONE', #63471, 1000.000000000000000 ) ;
#62767=VERTEX_POINT ( 'NONE', #12337 ) ;
#62769=ORIENTED_EDGE ( 'NONE', *, *, #68677, .F. ) ;
#62775=AXIS2_PLACEMENT_3D ( 'NONE', #59846, #54559, #27672 ) ;
#62780=CARTESIAN_POINT ( 'NONE',  ( -23.75054448485400016, -17.50000000000000000, 25.53140320652400064 ) ) ;
#62783=VECTOR ( 'NONE', #28488, 1000.000000000000000 ) ;
#62784=VERTEX_POINT ( 'NONE', #12000 ) ;
#62789=CYLINDRICAL_SURFACE ( 'NONE', #40643, 4.000000000000000000 ) ;
#62793=LINE ( 'NONE', #51489, #25507 ) ;
#62796=VECTOR ( 'NONE', #69070, 1000.000000000000000 ) ;
#62802=ADVANCED_FACE ( 'NONE', ( #28616 ), #28273, .F. ) ;
#62808=AXIS2_PLACEMENT_3D ( 'NONE', #66977, #56374, #7923 ) ;
#62810=VERTEX_POINT ( 'NONE', #1744 ) ;
#62835=CARTESIAN_POINT ( 'NONE',  ( -11.00000000000000000, -14.33999999999999986, 14.50000000000000000 ) ) ;
#62837=CYLINDRICAL_SURFACE ( 'NONE', #54941, 4.500000000000189182 ) ;
#62841=EDGE_CURVE ( 'NONE', #44065, #34045, #66096, .T. ) ;
#62849=DIRECTION ( 'NONE',  ( -1.000000000000000000, 0.000000000000000000, 0.000000000000000000 ) ) ;
#62850=CARTESIAN_POINT ( 'NONE',  ( -14.66434062215825840, -0.3156604612126666654, 23.46090750622624910 ) ) ;
#62851=EDGE_LOOP ( 'NONE', ( #27622, #6058, #31401, #61691 ) ) ;
#62852=DIRECTION ( 'NONE',  ( -1.000000000000000000, 0.000000000000000000, 0.000000000000000000 ) ) ;
#62867=DIRECTION ( 'NONE',  ( 0.000000000000000000, -0.7096009616570518874, 0.7046037717862339012 ) ) ;
#62869=ORIENTED_EDGE ( 'NONE', *, *, #64102, .T. ) ;
#62874=AXIS2_PLACEMENT_3D ( 'NONE', #45230, #60805, #66803 ) ;
#62881=CARTESIAN_POINT ( 'NONE',  ( -11.50000000000000000, -15.46862696659690073, -14.50000000000000000 ) ) ;
#62888=AXIS2_PLACEMENT_3D ( 'NONE', #24286, #44531, #14382 ) ;
#62893=CARTESIAN_POINT ( 'NONE',  ( -14.66242688423474227, -0.3152598339554795182, -23.45980260912095616 ) ) ;
#62899=CARTESIAN_POINT ( 'NONE',  ( 29.50000000000000355, -12.00000000000000000, -10.52786404500095863 ) ) ;
#62905=DIRECTION ( 'NONE',  ( 0.000000000000000000, -1.000000000000000000, 0.000000000000000000 ) ) ;
#62907=DIRECTION ( 'NONE',  ( 1.060575238724892987E-16, 0.5000000000000199840, -0.8660254037844271613 ) ) ;
#62909=EDGE_CURVE ( 'NONE', #51206, #4508, #56102, .T. ) ;
#62911=ORIENTED_EDGE ( 'NONE', *, *, #9425, .T. ) ;
#62912=LINE ( 'NONE', #19757, #10941 ) ;
#62926=VECTOR ( 'NONE', #63169, 1000.000000000000000 ) ;
#62928=DIRECTION ( 'NONE',  ( -0.000000000000000000, 1.000000000000000000, -0.000000000000000000 ) ) ;
#62929=DIRECTION ( 'NONE',  ( 0.000000000000000000, 0.000000000000000000, 1.000000000000000000 ) ) ;
#62930=EDGE_CURVE ( 'NONE', #58887, #32678, #8804, .T. ) ;
#62933=CARTESIAN_POINT ( 'NONE',  ( -14.25000000000000000, -2.500000000000000000, -21.77831216351300014 ) ) ;
#62938=ORIENTED_EDGE ( 'NONE', *, *, #13359, .T. ) ;
#62942=AXIS2_PLACEMENT_3D ( 'NONE', #44359, #65932, #59943 ) ;
#62946=EDGE_CURVE ( 'NONE', #43516, #31751, #31441, .T. ) ;
#62949=EDGE_CURVE ( 'NONE', #55252, #48042, #53867, .T. ) ;
#62950=ORIENTED_EDGE ( 'NONE', *, *, #19846, .F. ) ;
#62954=ORIENTED_EDGE ( 'NONE', *, *, #3308, .T. ) ;
#62961=DIRECTION ( 'NONE',  ( 0.000000000000000000, 0.000000000000000000, 1.000000000000000000 ) ) ;
#62969=CARTESIAN_POINT ( 'NONE',  ( -17.51999999999999957, -15.50000000000000000, -26.00000000000000355 ) ) ;
#62978=DIRECTION ( 'NONE',  ( 1.000000000000000000, 0.000000000000000000, 0.000000000000000000 ) ) ;
#62980=EDGE_LOOP ( 'NONE', ( #4048, #28633 ) ) ;
#62981=VECTOR ( 'NONE', #35000, 1000.000000000000000 ) ;
#62983=CARTESIAN_POINT ( 'NONE',  ( -15.50000000000000000, -0.1999999999999999556, -21.05000000000000071 ) ) ;
#62987=VERTEX_POINT ( 'NONE', #19400 ) ;
#62990=AXIS2_PLACEMENT_3D ( 'NONE', #17542, #39118, #54698 ) ;
#62994=DIRECTION ( 'NONE',  ( 0.000000000000000000, 0.000000000000000000, -1.000000000000000000 ) ) ;
#63000=ADVANCED_BREP_SHAPE_REPRESENTATION ( '', ( #20823, #45918 ), #34756 ) ;
#63007=CARTESIAN_POINT ( 'NONE',  ( 11.00000000000000000, -12.00000000000000000, 10.52786404500095863 ) ) ;
#63008=ORIENTED_EDGE ( 'NONE', *, *, #26940, .F. ) ;
#63010=FACE_OUTER_BOUND ( 'NONE', #50603, .T. ) ;
#63021=EDGE_LOOP ( 'NONE', ( #59559, #56122, #65244, #35753 ) ) ;
#63024=DIRECTION ( 'NONE',  ( -0.8660254037844482555, 0.000000000000000000, -0.4999999999999831801 ) ) ;
#63027=VERTEX_POINT ( 'NONE', #40622 ) ;
#63028=EDGE_CURVE ( 'NONE', #68712, #9129, #62181, .T. ) ;
#63031=ORIENTED_EDGE ( 'NONE', *, *, #9447, .T. ) ;
#63032=EDGE_CURVE ( 'NONE', #21463, #55205, #32804, .T. ) ;
#63034=VECTOR ( 'NONE', #5980, 1000.000000000000000 ) ;
#63035=CARTESIAN_POINT ( 'NONE',  ( -11.00000000000000000, -11.50000000000100009, -15.00000000000084910 ) ) ;
#63041=DIRECTION ( 'NONE',  ( 1.000000000000000000, 0.000000000000000000, 0.000000000000000000 ) ) ;
#63044=EDGE_LOOP ( 'NONE', ( #43983, #65878, #19736, #18866, #59137, #25394, #29340, #3291, #64163, #67300, #20242 ) ) ;
#63052=ORIENTED_EDGE ( 'NONE', *, *, #27329, .F. ) ;
#63053=ORIENTED_EDGE ( 'NONE', *, *, #18681, .F. ) ;
#63055=CARTESIAN_POINT ( 'NONE',  ( -25.50000000000000355, -15.50000000000000000, -24.50000000000000000 ) ) ;
#63067=DIRECTION ( 'NONE',  ( -1.000000000000000000, 0.000000000000000000, 0.000000000000000000 ) ) ;
#63068=DIRECTION ( 'NONE',  ( 1.000000000000000000, 0.000000000000000000, 0.000000000000000000 ) ) ;
#63078=EDGE_CURVE ( 'NONE', #56741, #18603, #26804, .T. ) ;
#63080=DIRECTION ( 'NONE',  ( 0.000000000000000000, 0.000000000000000000, 1.000000000000000000 ) ) ;
#63081=AXIS2_PLACEMENT_3D ( 'NONE', #29609, #34908, #24320 ) ;
#63082=CYLINDRICAL_SURFACE ( 'NONE', #8357, 3.499999999999850342 ) ;
#63085=EDGE_CURVE ( 'NONE', #50838, #9560, #30168, .T. ) ;
#63094=LINE ( 'NONE', #56383, #24333 ) ;
#63101=LINE ( 'NONE', #35506, #13953 ) ;
#63102=DIRECTION ( 'NONE',  ( 0.000000000000000000, 0.000000000000000000, 1.000000000000000000 ) ) ;
#63104=FACE_OUTER_BOUND ( 'NONE', #908, .T. ) ;
#63105=ORIENTED_EDGE ( 'NONE', *, *, #28229, .T. ) ;
#63110=CARTESIAN_POINT ( 'NONE',  ( -13.00000000000000178, -15.50000000000000000, -14.50000000000000000 ) ) ;
#63111=EDGE_CURVE ( 'NONE', #62094, #69773, #32479, .T. ) ;
#63115=EDGE_CURVE ( 'NONE', #22607, #58343, #5596, .T. ) ;
#63116=LINE ( 'NONE', #30943, #25994 ) ;
#63117=CARTESIAN_POINT ( 'NONE',  ( -17.00000000000000000, -17.50000000000000000, -15.70500000000000007 ) ) ;
#63124=AXIS2_PLACEMENT_3D ( 'NONE', #38014, #11804, #28087 ) ;
#63137=EDGE_LOOP ( 'NONE', ( #8632, #18271, #6857, #11334 ) ) ;
#63144=VECTOR ( 'NONE', #65674, 1000.000000000000000 ) ;
#63145=EDGE_CURVE ( 'NONE', #66744, #57618, #38134, .T. ) ;
#63152=EDGE_CURVE ( 'NONE', #26381, #63611, #67420, .T. ) ;
#63153=DIRECTION ( 'NONE',  ( 0.000000000000000000, -0.7096009616570518874, 0.7046037717862339012 ) ) ;
#63154=EDGE_CURVE ( 'NONE', #67917, #32193, #60353, .T. ) ;
#63155=EDGE_CURVE ( 'NONE', #39495, #57327, #12952, .T. ) ;
#63162=CARTESIAN_POINT ( 'NONE',  ( -30.00000000000000000, -17.14999999999900027, 26.64999999999900027 ) ) ;
#63169=DIRECTION ( 'NONE',  ( 0.000000000000000000, 1.000000000000000000, 0.000000000000000000 ) ) ;
#63170=DIRECTION ( 'NONE',  ( 0.000000000000000000, 0.000000000000000000, 1.000000000000000000 ) ) ;
#63183=ORIENTED_EDGE ( 'NONE', *, *, #43697, .F. ) ;
#63188=CARTESIAN_POINT ( 'NONE',  ( -11.00000000000000000, -11.50000000000000000, 15.00000000000000000 ) ) ;
#63190=ORIENTED_EDGE ( 'NONE', *, *, #28368, .T. ) ;
#63197=EDGE_CURVE ( 'NONE', #20570, #65126, #995, .T. ) ;
#63203=EDGE_LOOP ( 'NONE', ( #2576, #20265, #24952, #49783 ) ) ;
#63205=CARTESIAN_POINT ( 'NONE',  ( -28.00000000000000000, -17.50000000000000000, -15.70500000000000007 ) ) ;
#63206=ORIENTED_EDGE ( 'NONE', *, *, #45489, .T. ) ;
#63213=VERTEX_POINT ( 'NONE', #23574 ) ;
#63222=DIRECTION ( 'NONE',  ( -1.000000000000000000, 0.000000000000000000, 0.000000000000000000 ) ) ;
#63228=DIRECTION ( 'NONE',  ( 0.000000000000000000, 1.000000000000000000, 0.000000000000000000 ) ) ;
#63240=FACE_OUTER_BOUND ( 'NONE', #62441, .T. ) ;
#63249=DIRECTION ( 'NONE',  ( 0.000000000000000000, -0.9938079899998859545, 0.1111111111112941946 ) ) ;
#63257=AXIS2_PLACEMENT_3D ( 'NONE', #41208, #14358, #37325 ) ;
#63262=ORIENTED_EDGE ( 'NONE', *, *, #47761, .T. ) ;
#63266=DIRECTION ( 'NONE',  ( 0.000000000000000000, 0.000000000000000000, -1.000000000000000000 ) ) ;
#63267=ORIENTED_EDGE ( 'NONE', *, *, #69589, .F. ) ;
#63272=ORIENTED_EDGE ( 'NONE', *, *, #38386, .T. ) ;
#63277=LINE ( 'NONE', #46653, #53818 ) ;
#63278=FACE_OUTER_BOUND ( 'NONE', #14607, .T. ) ;
#63283=ORIENTED_EDGE ( 'NONE', *, *, #58286, .T. ) ;
#63294=VECTOR ( 'NONE', #46489, 1000.000000000000000 ) ;
#63308=AXIS2_PLACEMENT_3D ( 'NONE', #38563, #44194, #22641 ) ;
#63310=DIRECTION ( 'NONE',  ( 0.4285714285711672566, 0.000000000000000000, 0.9035079029053751931 ) ) ;
#63312=ORIENTED_EDGE ( 'NONE', *, *, #46080, .T. ) ;
#63313=CARTESIAN_POINT ( 'NONE',  ( -25.50000000000000355, -5.200000000000001066, 20.24999999999999645 ) ) ;
#63320=ORIENTED_EDGE ( 'NONE', *, *, #861, .T. ) ;
#63326=DIRECTION ( 'NONE',  ( 1.000000000000000000, 0.000000000000000000, 0.000000000000000000 ) ) ;
#63342=DIRECTION ( 'NONE',  ( -1.000000000000000000, 0.000000000000000000, 0.000000000000000000 ) ) ;
#63350=DIRECTION ( 'NONE',  ( 1.000000000000000000, -0.000000000000000000, -0.000000000000000000 ) ) ;
#63354=VECTOR ( 'NONE', #69117, 1000.000000000000000 ) ;
#63355=FACE_BOUND ( 'NONE', #18688, .T. ) ;
#63357=FACE_OUTER_BOUND ( 'NONE', #24655, .T. ) ;
#63362=ORIENTED_EDGE ( 'NONE', *, *, #2710, .F. ) ;
#63376=DIRECTION ( 'NONE',  ( -1.000000000000000000, 0.000000000000000000, 0.000000000000000000 ) ) ;
#63382=CIRCLE ( 'NONE', #6925, 4.000000000000000000 ) ;
#63392=EDGE_CURVE ( 'NONE', #19600, #67816, #40880, .T. ) ;
#63410=DIRECTION ( 'NONE',  ( 0.000000000000000000, 1.000000000000000000, 0.000000000000000000 ) ) ;
#63416=ORIENTED_EDGE ( 'NONE', *, *, #30936, .F. ) ;
#63417=CARTESIAN_POINT ( 'NONE',  ( -11.00000000000000000, -12.00000000000000000, -10.52786404500095863 ) ) ;
#63418=CARTESIAN_POINT ( 'NONE',  ( -15.50000000000000000, -5.000000000000000000, 26.50000000000000000 ) ) ;
#63422=CIRCLE ( 'NONE', #65630, 4.000000000000000000 ) ;
#63425=DIRECTION ( 'NONE',  ( 1.000000000000000000, -0.000000000000000000, -0.000000000000000000 ) ) ;
#63426=ORIENTED_EDGE ( 'NONE', *, *, #14236, .T. ) ;
#63428=CARTESIAN_POINT ( 'NONE',  ( -29.50000000000000355, -11.50000000000100009, 15.00000000000084910 ) ) ;
#63434=CIRCLE ( 'NONE', #18231, 0.3499999999998875677 ) ;
#63450=ORIENTED_EDGE ( 'NONE', *, *, #19333, .F. ) ;
#63456=DIRECTION ( 'NONE',  ( 0.000000000000000000, -0.9921567416492215186, 0.1249999999999996531 ) ) ;
#63466=PLANE ( 'NONE',  #39599 ) ;
#63471=DIRECTION ( 'NONE',  ( -1.000000000000000000, 0.000000000000000000, 0.000000000000000000 ) ) ;
#63475=DIRECTION ( 'NONE',  ( 0.000000000000000000, 0.000000000000000000, 1.000000000000000000 ) ) ;
#63479=ORIENTED_EDGE ( 'NONE', *, *, #31729, .F. ) ;
#63485=DIRECTION ( 'NONE',  ( -1.000000000000000000, 0.000000000000000000, 0.000000000000000000 ) ) ;
#63492=EDGE_CURVE ( 'NONE', #61811, #16870, #33594, .T. ) ;
#63496=ORIENTED_EDGE ( 'NONE', *, *, #19685, .T. ) ;
#63501=ORIENTED_EDGE ( 'NONE', *, *, #17890, .F. ) ;
#63505=EDGE_LOOP ( 'NONE', ( #68371, #54632, #51860, #41216 ) ) ;
#63506=AXIS2_PLACEMENT_3D ( 'NONE', #16245, #65044, #37134 ) ;
#63509=B_SPLINE_CURVE_WITH_KNOTS ( 'NONE', 3,
 ( #4953, #31837, #26519, #48088, #69667, #21229 ),
 .UNSPECIFIED., .F., .F.,
 ( 4, 2, 4 ),
 ( 0.0002380763768130567115, 0.7291065797294590256, 1.457975083082104995 ),
 .UNSPECIFIED. ) ;
#63529=CARTESIAN_POINT ( 'NONE',  ( -24.00000000000000000, -16.64230188589299786, -14.64519951917100116 ) ) ;
#63532=CARTESIAN_POINT ( 'NONE',  ( -11.75000000000000000, -5.200000000000001066, 26.25000000000000000 ) ) ;
#63551=CYLINDRICAL_SURFACE ( 'NONE', #33898, 0.3500000000009988455 ) ;
#63558=ORIENTED_EDGE ( 'NONE', *, *, #986, .T. ) ;
#63560=CARTESIAN_POINT ( 'NONE',  ( -15.50000000000000000, -5.000000000000000000, 22.50000000000000000 ) ) ;
#63576=ORIENTED_EDGE ( 'NONE', *, *, #30682, .F. ) ;
#63581=ORIENTED_EDGE ( 'NONE', *, *, #21558, .F. ) ;
#63600=LINE ( 'NONE', #55001, #28335 ) ;
#63606=DIRECTION ( 'NONE',  ( 1.000000000000000000, -0.000000000000000000, -0.000000000000000000 ) ) ;
#63608=EDGE_CURVE ( 'NONE', #21794, #35470, #19499, .T. ) ;
#63611=VERTEX_POINT ( 'NONE', #51695 ) ;
#63616=DIRECTION ( 'NONE',  ( -1.000000000000000000, 0.000000000000000000, 0.000000000000000000 ) ) ;
#63619=VECTOR ( 'NONE', #35223, 1000.000000000000000 ) ;
#63620=CARTESIAN_POINT ( 'NONE',  ( 23.48000000000000043, -17.50000000000000000, 26.00000000000000355 ) ) ;
#63621=ORIENTED_EDGE ( 'NONE', *, *, #56288, .T. ) ;
#63625=LINE ( 'NONE', #59004, #38999 ) ;
#63637=VECTOR ( 'NONE', #3092, 1000.000000000000000 ) ;
#63644=ORIENTED_EDGE ( 'NONE', *, *, #67640, .T. ) ;
#63646=VECTOR ( 'NONE', #3702, 1000.000000000000000 ) ;
#63650=EDGE_CURVE ( 'NONE', #46397, #51774, #22482, .T. ) ;
#63654=EDGE_CURVE ( 'NONE', #46800, #14694, #37181, .T. ) ;
#63658=ORIENTED_EDGE ( 'NONE', *, *, #33948, .F. ) ;
#63671=AXIS2_PLACEMENT_3D ( 'NONE', #18927, #41181, #18216 ) ;
#63676=VERTEX_POINT ( 'NONE', #46030 ) ;
#63683=LINE ( 'NONE', #19133, #28842 ) ;
#63693=ADVANCED_FACE ( 'NONE', ( #44975 ), #62282, .F. ) ;
#63701=CARTESIAN_POINT ( 'NONE',  ( 25.50000000000000355, -15.12100000000000044, 20.87900000000000134 ) ) ;
#63719=ORIENTED_EDGE ( 'NONE', *, *, #46226, .T. ) ;
#63721=AXIS2_PLACEMENT_3D ( 'NONE', #57643, #35720, #26178 ) ;
#63726=ORIENTED_EDGE ( 'NONE', *, *, #21484, .F. ) ;
#63728=ORIENTED_EDGE ( 'NONE', *, *, #60978, .T. ) ;
#63731=PLANE ( 'NONE',  #61321 ) ;
#63738=CYLINDRICAL_SURFACE ( 'NONE', #37415, 3.499999999999999556 ) ;
#63749=ORIENTED_EDGE ( 'NONE', *, *, #9106, .F. ) ;
#63759=PLANE ( 'NONE',  #13929 ) ;
#63765=AXIS2_PLACEMENT_3D ( 'NONE', #28316, #6746, #16690 ) ;
#63767=CARTESIAN_POINT ( 'NONE',  ( -11.00000000000000000, -14.04000000000000092, 14.80000000000000071 ) ) ;
#63769=ORIENTED_EDGE ( 'NONE', *, *, #32837, .T. ) ;
#63775=DIRECTION ( 'NONE',  ( 0.000000000000000000, -0.9938079899998859545, -0.1111111111112941946 ) ) ;
#63780=CIRCLE ( 'NONE', #52470, 4.500000000000190958 ) ;
#63782=DIRECTION ( 'NONE',  ( 0.000000000000000000, 1.000000000000000000, 0.000000000000000000 ) ) ;
#63790=ORIENTED_EDGE ( 'NONE', *, *, #3528, .T. ) ;
#63794=FACE_OUTER_BOUND ( 'NONE', #22661, .T. ) ;
#63795=FACE_OUTER_BOUND ( 'NONE', #69504, .T. ) ;
#63803=ORIENTED_EDGE ( 'NONE', *, *, #2175, .T. ) ;
#63806=DIRECTION ( 'NONE',  ( 0.000000000000000000, 1.000000000000000000, 0.000000000000000000 ) ) ;
#63808=CYLINDRICAL_SURFACE ( 'NONE', #50025, 3.499999999999055866 ) ;
#63813=CARTESIAN_POINT ( 'NONE',  ( 16.89194109070750116, -5.000000000000000000, -26.25000000000000000 ) ) ;
#63820=CARTESIAN_POINT ( 'NONE',  ( -29.50000000000000355, -11.50000000000100009, 10.50000000000065903 ) ) ;
#63821=EDGE_CURVE ( 'NONE', #24182, #62314, #28122, .T. ) ;
#63833=EDGE_CURVE ( 'NONE', #64346, #20240, #8893, .T. ) ;
#63836=DIRECTION ( 'NONE',  ( 1.000000000000000000, -0.000000000000000000, -0.000000000000000000 ) ) ;
#63838=ORIENTED_EDGE ( 'NONE', *, *, #57352, .F. ) ;
#63840=LINE ( 'NONE', #10100, #36140 ) ;
#63841=VERTEX_POINT ( 'NONE', #68298 ) ;
#63843=ORIENTED_EDGE ( 'NONE', *, *, #66446, .F. ) ;
#63847=DIRECTION ( 'NONE',  ( 0.000000000000000000, -0.7278708115916125987, 0.6857142857145147596 ) ) ;
#63848=CARTESIAN_POINT ( 'NONE',  ( -11.00000000000000000, -17.35230188589299871, 15.35019951917099945 ) ) ;
#63850=PLANE ( 'NONE',  #728 ) ;
#63852=AXIS2_PLACEMENT_3D ( 'NONE', #61864, #56554, #63266 ) ;
#63856=DIRECTION ( 'NONE',  ( 1.000000000000000000, 0.000000000000000000, 0.000000000000000000 ) ) ;
#63861=PLANE ( 'NONE',  #24371 ) ;
#63864=EDGE_LOOP ( 'NONE', ( #6153, #6386 ) ) ;
#63883=EDGE_CURVE ( 'NONE', #14976, #18063, #49574, .T. ) ;
#63894=DIRECTION ( 'NONE',  ( 0.000000000000000000, -0.7046037717806115097, 0.7096009616626348659 ) ) ;
#63896=DIRECTION ( 'NONE',  ( 0.8660254037850523279, 0.000000000000000000, 0.4999999999989371835 ) ) ;
#63897=DIRECTION ( 'NONE',  ( 0.000000000000000000, 1.000000000000000000, 0.000000000000000000 ) ) ;
#63902=ORIENTED_EDGE ( 'NONE', *, *, #24112, .T. ) ;
#63905=LINE ( 'NONE', #68510, #2902 ) ;
#63907=LINE ( 'NONE', #58249, #28055 ) ;
#63909=VECTOR ( 'NONE', #32767, 999.9999999999998863 ) ;
#63911=ORIENTED_EDGE ( 'NONE', *, *, #25616, .F. ) ;
#63915=ORIENTED_EDGE ( 'NONE', *, *, #57958, .F. ) ;
#63917=EDGE_CURVE ( 'NONE', #24393, #47170, #21612, .T. ) ;
#63925=ORIENTED_EDGE ( 'NONE', *, *, #11160, .T. ) ;
#63934=ORIENTED_EDGE ( 'NONE', *, *, #8142, .T. ) ;
#63935=FACE_OUTER_BOUND ( 'NONE', #17751, .T. ) ;
#63947=CARTESIAN_POINT ( 'NONE',  ( 30.00000000000000000, -12.00000000000000000, -10.20500000000000007 ) ) ;
#63948=DIRECTION ( 'NONE',  ( -1.000000000000000000, 0.000000000000000000, 0.000000000000000000 ) ) ;
#63951=ORIENTED_EDGE ( 'NONE', *, *, #5917, .T. ) ;
#63954=VECTOR ( 'NONE', #37541, 1000.000000000000000 ) ;
#63971=AXIS2_PLACEMENT_3D ( 'NONE', #49839, #60438, #39225 ) ;
#63981=FACE_OUTER_BOUND ( 'NONE', #36052, .T. ) ;
#63986=CARTESIAN_POINT ( 'NONE',  ( -11.50000000000000000, -11.50000000000100009, -15.00000000000084910 ) ) ;
#63988=LINE ( 'NONE', #26491, #60293 ) ;
#63990=ORIENTED_EDGE ( 'NONE', *, *, #43843, .T. ) ;
#63992=EDGE_CURVE ( 'NONE', #50235, #17310, #38564, .T. ) ;
#64037=CARTESIAN_POINT ( 'NONE',  ( -11.00000000000000000, -17.14999999999999858, 27.00000000000000000 ) ) ;
#64042=ORIENTED_EDGE ( 'NONE', *, *, #51773, .T. ) ;
#64045=CYLINDRICAL_SURFACE ( 'NONE', #15463, 0.5000000000001374456 ) ;
#64061=EDGE_CURVE ( 'NONE', #54337, #64273, #45577, .T. ) ;
#64065=VECTOR ( 'NONE', #49760, 1000.000000000000000 ) ;
#64069=VERTEX_POINT ( 'NONE', #2798 ) ;
#64075=DIRECTION ( 'NONE',  ( -0.000000000000000000, 1.000000000000000000, -0.000000000000000000 ) ) ;
#64082=CARTESIAN_POINT ( 'NONE',  ( -16.75000000000000000, -0.2714405302574894319, 22.98746066354538087 ) ) ;
#64083=DIRECTION ( 'NONE',  ( 0.000000000000000000, 0.7071067811865474617, -0.7071067811865474617 ) ) ;
#64091=ORIENTED_EDGE ( 'NONE', *, *, #46377, .T. ) ;
#64096=DIRECTION ( 'NONE',  ( -0.7142857142857395036, 0.000000000000000000, -0.6998542122237394469 ) ) ;
#64101=EDGE_LOOP ( 'NONE', ( #20935, #19616, #28431, #10325 ) ) ;
#64102=EDGE_CURVE ( 'NONE', #64845, #69297, #18013, .T. ) ;
#64113=ORIENTED_EDGE ( 'NONE', *, *, #55188, .T. ) ;
#64120=CIRCLE ( 'NONE', #31357, 0.3500000000009988455 ) ;
#64122=FACE_OUTER_BOUND ( 'NONE', #61512, .T. ) ;
#64133=ORIENTED_EDGE ( 'NONE', *, *, #35368, .F. ) ;
#64140=CARTESIAN_POINT ( 'NONE',  ( 15.50000000000000000, -1.037157890325000054, 26.50000000000000000 ) ) ;
#64163=ORIENTED_EDGE ( 'NONE', *, *, #36837, .F. ) ;
#64168=DIRECTION ( 'NONE',  ( 1.000000000000000000, -0.000000000000000000, -0.000000000000000000 ) ) ;
#64180=VERTEX_POINT ( 'NONE', #24378 ) ;
#64181=LINE ( 'NONE', #22076, #9140 ) ;
#64184=CARTESIAN_POINT ( 'NONE',  ( 14.25000000000000000, -2.500000000000000000, 23.22168783648699986 ) ) ;
#64189=EDGE_CURVE ( 'NONE', #63676, #24780, #66801, .T. ) ;
#64192=ORIENTED_EDGE ( 'NONE', *, *, #36245, .F. ) ;
#64193=ORIENTED_EDGE ( 'NONE', *, *, #18278, .T. ) ;
#64194=ADVANCED_FACE ( 'NONE', ( #46285 ), #26312, .F. ) ;
#64199=ORIENTED_EDGE ( 'NONE', *, *, #51497, .F. ) ;
#64214=VERTEX_POINT ( 'NONE', #68209 ) ;
#64217=CYLINDRICAL_SURFACE ( 'NONE', #1065, 0.5000000000001357803 ) ;
#64218=VERTEX_POINT ( 'NONE', #46993 ) ;
#64227=DIRECTION ( 'NONE',  ( 0.000000000000000000, -2.854859206170826497E-12, 1.000000000000000000 ) ) ;
#64228=DIRECTION ( 'NONE',  ( 0.000000000000000000, 0.000000000000000000, -1.000000000000000000 ) ) ;
#64231=DIRECTION ( 'NONE',  ( 0.000000000000000000, 0.000000000000000000, -1.000000000000000000 ) ) ;
#64240=ORIENTED_EDGE ( 'NONE', *, *, #5321, .T. ) ;
#64261=ORIENTED_EDGE ( 'NONE', *, *, #40569, .F. ) ;
#64262=AXIS2_PLACEMENT_3D ( 'NONE', #49196, #21287, #11692 ) ;
#64265=ORIENTED_EDGE ( 'NONE', *, *, #7512, .F. ) ;
#64273=VERTEX_POINT ( 'NONE', #58660 ) ;
#64275=DIRECTION ( 'NONE',  ( 0.000000000000000000, 1.000000000000000000, 0.000000000000000000 ) ) ;
#64280=VERTEX_POINT ( 'NONE', #63620 ) ;
#64306=LINE ( 'NONE', #31447, #8316 ) ;
#64309=CARTESIAN_POINT ( 'NONE',  ( -28.00000000000000000, -17.50000000000000000, 20.05051025721700242 ) ) ;
#64318=EDGE_CURVE ( 'NONE', #54520, #31859, #9351, .T. ) ;
#64321=EDGE_LOOP ( 'NONE', ( #1872, #31742, #58375, #3944 ) ) ;
#64323=PLANE ( 'NONE',  #67588 ) ;
#64325=CYLINDRICAL_SURFACE ( 'NONE', #64976, 4.500000000000188294 ) ;
#64330=CARTESIAN_POINT ( 'NONE',  ( -30.00000000000000000, 0.000000000000000000, 27.00000000000000000 ) ) ;
#64332=CARTESIAN_POINT ( 'NONE',  ( -25.50000000000000355, 0.000000000000000000, -22.50000000000000000 ) ) ;
#64335=ORIENTED_EDGE ( 'NONE', *, *, #64706, .T. ) ;
#64338=AXIS2_PLACEMENT_3D ( 'NONE', #62969, #53077, #58010 ) ;
#64340=ORIENTED_EDGE ( 'NONE', *, *, #35712, .T. ) ;
#64343=LINE ( 'NONE', #27544, #11840 ) ;
#64346=VERTEX_POINT ( 'NONE', #48393 ) ;
#64363=FACE_OUTER_BOUND ( 'NONE', #45629, .T. ) ;
#64368=DIRECTION ( 'NONE',  ( -1.000000000000000000, 0.000000000000000000, 0.000000000000000000 ) ) ;
#64379=ORIENTED_EDGE ( 'NONE', *, *, #43178, .F. ) ;
#64391=DIRECTION ( 'NONE',  ( 0.000000000000000000, 1.000000000000000000, 0.000000000000000000 ) ) ;
#64393=ORIENTED_EDGE ( 'NONE', *, *, #33230, .T. ) ;
#64408=ORIENTED_EDGE ( 'NONE', *, *, #32816, .F. ) ;
#64412=CARTESIAN_POINT ( 'NONE',  ( -29.50000000000000355, -11.50000000000000000, 15.00000000000000000 ) ) ;
#64419=CARTESIAN_POINT ( 'NONE',  ( -17.00000000000000000, -17.50000000000000000, -15.70500000000000007 ) ) ;
#64423=CARTESIAN_POINT ( 'NONE',  ( 11.50000000000000000, -11.50000000000000000, -15.00000000000000000 ) ) ;
#64424=ORIENTED_EDGE ( 'NONE', *, *, #15839, .T. ) ;
#64430=LINE ( 'NONE', #64776, #26155 ) ;
#64432=ORIENTED_EDGE ( 'NONE', *, *, #9044, .T. ) ;
#64438=FACE_OUTER_BOUND ( 'NONE', #40468, .T. ) ;
#64451=AXIS2_PLACEMENT_3D ( 'NONE', #20549, #32209, #10632 ) ;
#64452=CYLINDRICAL_SURFACE ( 'NONE', #22072, 3.499999999999999556 ) ;
#64453=EDGE_CURVE ( 'NONE', #62442, #18780, #10506, .T. ) ;
#64455=CIRCLE ( 'NONE', #37342, 0.4999999999991867061 ) ;
#64457=CARTESIAN_POINT ( 'NONE',  ( 14.25000000000000000, -2.500000000000000000, -21.77831216351300014 ) ) ;
#64460=ORIENTED_EDGE ( 'NONE', *, *, #3863, .F. ) ;
#64463=CARTESIAN_POINT ( 'NONE',  ( -28.00000000000000000, -16.28999999999710369, -15.00000000000794920 ) ) ;
#64469=ADVANCED_FACE ( 'NONE', ( #24289 ), #29225, .F. ) ;
#64479=TOROIDAL_SURFACE ( 'NONE', #57696, 3.299999999999470024, 0.2000000000005275058 ) ;
#64485=EDGE_CURVE ( 'NONE', #28718, #65641, #3744, .T. ) ;
#64490=DIRECTION ( 'NONE',  ( 0.000000000000000000, 0.000000000000000000, -1.000000000000000000 ) ) ;
#64519=VECTOR ( 'NONE', #11370, 1000.000000000000000 ) ;
#64520=EDGE_CURVE ( 'NONE', #44220, #44549, #40190, .T. ) ;
#64523=DIRECTION ( 'NONE',  ( -0.8660254037844485886, 0.000000000000000000, -0.4999999999999827360 ) ) ;
#64528=CARTESIAN_POINT ( 'NONE',  ( 30.00000000000000000, -5.599999999999379696, -26.60000000000059828 ) ) ;
#64538=FACE_OUTER_BOUND ( 'NONE', #23095, .T. ) ;
#64541=VECTOR ( 'NONE', #15064, 1000.000000000000000 ) ;
#64555=CARTESIAN_POINT ( 'NONE',  ( 30.00000000000000000, -9.199999999999999289, 12.69999999999986073 ) ) ;
#64562=ORIENTED_EDGE ( 'NONE', *, *, #68623, .T. ) ;
#64574=CARTESIAN_POINT ( 'NONE',  ( 30.00000000000000000, -11.50000000000082068, -10.20500000000000007 ) ) ;
#64582=DIRECTION ( 'NONE',  ( 0.000000000000000000, 1.000000000000000000, 0.000000000000000000 ) ) ;
#64585=LINE ( 'NONE', #47973, #23748 ) ;
#64590=VECTOR ( 'NONE', #24462, 1000.000000000000000 ) ;
#64592=ORIENTED_EDGE ( 'NONE', *, *, #18471, .T. ) ;
#64594=CARTESIAN_POINT ( 'NONE',  ( 30.00000000000000000, -5.200000000000001066, 26.59999999999999787 ) ) ;
#64596=CARTESIAN_POINT ( 'NONE',  ( -29.50000000000000355, -11.50000000000100009, 10.50000000000065903 ) ) ;
#64601=LINE ( 'NONE', #10854, #4104 ) ;
#64603=ORIENTED_EDGE ( 'NONE', *, *, #68120, .T. ) ;
#64606=ORIENTED_EDGE ( 'NONE', *, *, #3139, .T. ) ;
#64610=CARTESIAN_POINT ( 'NONE',  ( 25.50000000000000355, -15.50000000000000000, -22.50000000000000000 ) ) ;
#64612=ORIENTED_EDGE ( 'NONE', *, *, #56578, .T. ) ;
#64630=ORIENTED_EDGE ( 'NONE', *, *, #13448, .F. ) ;
#64631=DIRECTION ( 'NONE',  ( 0.000000000000000000, 0.000000000000000000, 1.000000000000000000 ) ) ;
#64642=DIRECTION ( 'NONE',  ( 0.000000000000000000, 1.000000000000000000, 0.000000000000000000 ) ) ;
#64645=DIRECTION ( 'NONE',  ( -1.000000000000000000, 0.000000000000000000, 0.000000000000000000 ) ) ;
#64653=ORIENTED_EDGE ( 'NONE', *, *, #41193, .T. ) ;
#64658=EDGE_CURVE ( 'NONE', #69392, #30786, #52207, .T. ) ;
#64659=DIRECTION ( 'NONE',  ( -1.000000000000000000, 0.000000000000000000, 0.000000000000000000 ) ) ;
#64662=CARTESIAN_POINT ( 'NONE',  ( -15.50000000000000000, -0.2038245569916614930, 21.05662432702600029 ) ) ;
#64670=DIRECTION ( 'NONE',  ( -0.000000000000000000, 1.000000000000000000, -0.000000000000000000 ) ) ;
#64689=DIRECTION ( 'NONE',  ( 0.000000000000000000, 0.000000000000000000, -1.000000000000000000 ) ) ;
#64698=CARTESIAN_POINT ( 'NONE',  ( -11.00000000000000000, -17.50000000000000000, 15.70499999999969809 ) ) ;
#64699=VERTEX_POINT ( 'NONE', #36647 ) ;
#64703=ORIENTED_EDGE ( 'NONE', *, *, #59780, .T. ) ;
#64706=EDGE_CURVE ( 'NONE', #35602, #44169, #57162, .T. ) ;
#64707=DIRECTION ( 'NONE',  ( 0.000000000000000000, 0.000000000000000000, -1.000000000000000000 ) ) ;
#64714=AXIS2_PLACEMENT_3D ( 'NONE', #63188, #67454, #2732 ) ;
#64718=ORIENTED_EDGE ( 'NONE', *, *, #23833, .F. ) ;
#64719=DIRECTION ( 'NONE',  ( -1.000000000000000000, 0.000000000000000000, 0.000000000000000000 ) ) ;
#64726=EDGE_CURVE ( 'NONE', #7495, #19227, #51175, .T. ) ;
#64729=VERTEX_POINT ( 'NONE', #35581 ) ;
#64735=CARTESIAN_POINT ( 'NONE',  ( 17.51999999999999957, -15.50000000000000000, -26.00000000000000355 ) ) ;
#64740=CONICAL_SURFACE ( 'NONE', #21832, 1732.050807568789651, 1.047197551196575871 ) ;
#64746=VERTEX_POINT ( 'NONE', #41243 ) ;
#64754=LINE ( 'NONE', #21964, #13096 ) ;
#64761=ORIENTED_EDGE ( 'NONE', *, *, #24197, .F. ) ;
#64765=AXIS2_PLACEMENT_3D ( 'NONE', #48067, #42060, #65030 ) ;
#64775=AXIS2_PLACEMENT_3D ( 'NONE', #6214, #39759, #50028 ) ;
#64776=CARTESIAN_POINT ( 'NONE',  ( 30.00000000000000000, -14.04000000000000092, 14.80000000000000071 ) ) ;
#64782=ORIENTED_EDGE ( 'NONE', *, *, #20014, .T. ) ;
#64801=EDGE_CURVE ( 'NONE', #6004, #24879, #42994, .T. ) ;
#64802=LINE ( 'NONE', #16017, #27512 ) ;
#64806=CIRCLE ( 'NONE', #35391, 0.3499999999999611200 ) ;
#64807=DIRECTION ( 'NONE',  ( 0.000000000000000000, -0.7046037717859411353, -0.7096009616573427659 ) ) ;
#64813=DIRECTION ( 'NONE',  ( -1.000000000000000000, 0.000000000000000000, 0.000000000000000000 ) ) ;
#64820=CARTESIAN_POINT ( 'NONE',  ( 25.50000000000000355, -15.12100000000000044, -22.50000000000000000 ) ) ;
#64821=EDGE_LOOP ( 'NONE', ( #28456, #19235, #55804, #27314 ) ) ;
#64826=VECTOR ( 'NONE', #6557, 1000.000000000000000 ) ;
#64837=FACE_OUTER_BOUND ( 'NONE', #62360, .T. ) ;
#64845=VERTEX_POINT ( 'NONE', #563 ) ;
#64850=DIRECTION ( 'NONE',  ( -1.000000000000000000, 0.000000000000000000, 0.000000000000000000 ) ) ;
#64851=CARTESIAN_POINT ( 'NONE',  ( -11.00000000000000000, -5.599999999999379696, -26.60000000000059828 ) ) ;
#64853=ADVANCED_FACE ( 'NONE', ( #32731 ), #27432, .F. ) ;
#64854=DIRECTION ( 'NONE',  ( 0.000000000000000000, 0.000000000000000000, 1.000000000000000000 ) ) ;
#64857=CARTESIAN_POINT ( 'NONE',  ( 15.50000000000000000, -15.50000000000000000, -22.50000000000000000 ) ) ;
#64866=ADVANCED_FACE ( 'NONE', ( #11499, #33080 ), #54657, .T. ) ;
#64886=EDGE_LOOP ( 'NONE', ( #4808, #29740, #65902, #36816 ) ) ;
#64890=CARTESIAN_POINT ( 'NONE',  ( 11.00000000000000000, -11.50000000000100009, 15.00000000000084910 ) ) ;
#64898=ORIENTED_EDGE ( 'NONE', *, *, #45372, .F. ) ;
#64899=DIRECTION ( 'NONE',  ( -1.000000000000000000, 0.000000000000000000, 0.000000000000000000 ) ) ;
#64902=EDGE_LOOP ( 'NONE', ( #27447, #1999, #6247, #30373 ) ) ;
#64903=CIRCLE ( 'NONE', #52488, 0.5000000000079362072 ) ;
#64907=CARTESIAN_POINT ( 'NONE',  ( 15.50000000000000000, -0.2038245569916610489, 21.05662432702600029 ) ) ;
#64917=FACE_OUTER_BOUND ( 'NONE', #35284, .T. ) ;
#64924=ADVANCED_FACE ( 'NONE', ( #1947 ), #38726, .F. ) ;
#64926=CARTESIAN_POINT ( 'NONE',  ( 30.00000000000000000, -13.79999999999979998, 17.64999999999988844 ) ) ;
#64934=PLANE ( 'NONE',  #40944 ) ;
#64939=CARTESIAN_POINT ( 'NONE',  ( 30.00000000000000000, -9.200000000000120082, 17.30000000000000071 ) ) ;
#64942=VERTEX_POINT ( 'NONE', #55351 ) ;
#64943=AXIS2_PLACEMENT_3D ( 'NONE', #63162, #15432, #64227 ) ;
#64945=CARTESIAN_POINT ( 'NONE',  ( -29.50000000000000355, -11.50000000000100009, 19.50000000000103739 ) ) ;
#64956=EDGE_LOOP ( 'NONE', ( #11156, #33385, #56912, #6237 ) ) ;
#64963=VECTOR ( 'NONE', #53677, 1000.000000000000000 ) ;
#64966=EDGE_CURVE ( 'NONE', #50438, #29049, #34448, .T. ) ;
#64967=LINE ( 'NONE', #48700, #58369 ) ;
#64971=CIRCLE ( 'NONE', #18654, 4.500000000000191847 ) ;
#64973=ORIENTED_EDGE ( 'NONE', *, *, #12046, .T. ) ;
#64976=AXIS2_PLACEMENT_3D ( 'NONE', #69274, #20481, #20827 ) ;
#64980=CARTESIAN_POINT ( 'NONE',  ( -11.00000000000000000, -5.599999999999999645, -9.400000000000000355 ) ) ;
#64982=DIRECTION ( 'NONE',  ( -0.000000000000000000, 1.000000000000000000, -0.000000000000000000 ) ) ;
#64983=ORIENTED_EDGE ( 'NONE', *, *, #18356, .F. ) ;
#64990=ORIENTED_EDGE ( 'NONE', *, *, #65783, .T. ) ;
#64994=AXIS2_PLACEMENT_3D ( 'NONE', #48031, #69940, #15165 ) ;
#64999=DIRECTION ( 'NONE',  ( 0.000000000000000000, 0.000000000000000000, 1.000000000000000000 ) ) ;
#65000=VECTOR ( 'NONE', #12988, 1000.000000000000000 ) ;
#65001=DIRECTION ( 'NONE',  ( -1.000000000000000000, 0.000000000000000000, 0.000000000000000000 ) ) ;
#65002=CARTESIAN_POINT ( 'NONE',  ( -15.50000000000000000, -0.2038245569916614930, 21.05662432702600029 ) ) ;
#65011=VERTEX_POINT ( 'NONE', #59498 ) ;
#65014=DIRECTION ( 'NONE',  ( 0.000000000000000000, 1.000000000000000000, 0.000000000000000000 ) ) ;
#65025=ORIENTED_EDGE ( 'NONE', *, *, #17412, .T. ) ;
#65030=DIRECTION ( 'NONE',  ( 0.000000000000000000, 0.000000000000000000, 1.000000000000000000 ) ) ;
#65032=VERTEX_POINT ( 'NONE', #1143 ) ;
#65033=EDGE_LOOP ( 'NONE', ( #68537, #40066, #41003, #394, #20466, #39636, #56311, #68483, #534, #53864, #24956, #27816, #52694, #19978, #31709 ) ) ;
#65040=DIRECTION ( 'NONE',  ( 0.000000000000000000, 0.000000000000000000, -1.000000000000000000 ) ) ;
#65044=DIRECTION ( 'NONE',  ( -0.000000000000000000, 1.000000000000000000, -0.000000000000000000 ) ) ;
#65045=ORIENTED_EDGE ( 'NONE', *, *, #47924, .F. ) ;
#65050=VECTOR ( 'NONE', #67685, 1000.000000000000000 ) ;
#65059=ORIENTED_EDGE ( 'NONE', *, *, #16558, .T. ) ;
#65068=AXIS2_PLACEMENT_3D ( 'NONE', #1063, #1394, #67135 ) ;
#65083=CARTESIAN_POINT ( 'NONE',  ( 30.00000000000000000, -5.200000000000001066, -26.59999999999999787 ) ) ;
#65084=CARTESIAN_POINT ( 'NONE',  ( -13.00000000000000178, -17.00000000000000000, 15.70499999999969809 ) ) ;
#65088=ORIENTED_EDGE ( 'NONE', *, *, #53036, .T. ) ;
#65091=CARTESIAN_POINT ( 'NONE',  ( -30.00000000000000000, -11.70000000000000284, -12.50000000000000000 ) ) ;
#65092=CARTESIAN_POINT ( 'NONE',  ( -25.50000000000000355, 0.000000000000000000, -24.75000000000000000 ) ) ;
#65095=ORIENTED_EDGE ( 'NONE', *, *, #19087, .T. ) ;
#65099=DIRECTION ( 'NONE',  ( 0.000000000000000000, 1.000000000000000000, 0.000000000000000000 ) ) ;
#65102=EDGE_CURVE ( 'NONE', #58960, #57228, #16210, .T. ) ;
#65104=CIRCLE ( 'NONE', #53801, 0.4999999999991867061 ) ;
#65105=CARTESIAN_POINT ( 'NONE',  ( 14.25000000000000000, -0.3156864504677152627, -22.74361999681790536 ) ) ;
#65107=VECTOR ( 'NONE', #31656, 1000.000000000000000 ) ;
#65108=ORIENTED_EDGE ( 'NONE', *, *, #60856, .F. ) ;
#65114=CIRCLE ( 'NONE', #62874, 4.000000000000001776 ) ;
#65115=VECTOR ( 'NONE', #11653, 1000.000000000000000 ) ;
#65118=EDGE_CURVE ( 'NONE', #7495, #42297, #22372, .T. ) ;
#65124=DIRECTION ( 'NONE',  ( -0.4999999999989371835, 0.000000000000000000, 0.8660254037850523279 ) ) ;
#65126=VERTEX_POINT ( 'NONE', #38627 ) ;
#65132=DIRECTION ( 'NONE',  ( 0.000000000000000000, 0.000000000000000000, 1.000000000000000000 ) ) ;
#65136=DIRECTION ( 'NONE',  ( -1.000000000000000000, 0.000000000000000000, 0.000000000000000000 ) ) ;
#65145=CARTESIAN_POINT ( 'NONE',  ( 30.00000000000000000, -17.50000000000000000, -26.64999999999999858 ) ) ;
#65146=CARTESIAN_POINT ( 'NONE',  ( 30.00000000000000000, -17.50000000000000000, 26.64999999999999858 ) ) ;
#65151=ORIENTED_EDGE ( 'NONE', *, *, #10968, .T. ) ;
#65158=ORIENTED_EDGE ( 'NONE', *, *, #30924, .T. ) ;
#65199=ORIENTED_EDGE ( 'NONE', *, *, #60908, .T. ) ;
#65206=CIRCLE ( 'NONE', #26793, 0.4000000000000600298 ) ;
#65217=DIRECTION ( 'NONE',  ( -0.000000000000000000, 1.000000000000000000, -0.000000000000000000 ) ) ;
#65223=AXIS2_PLACEMENT_3D ( 'NONE', #46796, #63068, #25241 ) ;
#65224=LINE ( 'NONE', #59562, #10183 ) ;
#65235=EDGE_LOOP ( 'NONE', ( #35886, #6946, #63581, #27304 ) ) ;
#65238=ADVANCED_FACE ( 'NONE', ( #33658 ), #45638, .F. ) ;
#65244=ORIENTED_EDGE ( 'NONE', *, *, #10361, .F. ) ;
#65252=DIRECTION ( 'NONE',  ( -1.000000000000000000, 0.000000000000000000, 0.000000000000000000 ) ) ;
#65255=ORIENTED_EDGE ( 'NONE', *, *, #2175, .F. ) ;
#65261=EDGE_LOOP ( 'NONE', ( #33723, #56910, #54808, #11127 ) ) ;
#65265=DIRECTION ( 'NONE',  ( 0.000000000000000000, 1.000000000000000000, 0.000000000000000000 ) ) ;
#65267=PLANE ( 'NONE',  #37110 ) ;
#65269=VECTOR ( 'NONE', #66828, 1000.000000000000000 ) ;
#65276=CIRCLE ( 'NONE', #20085, 0.5000000000001386669 ) ;
#65278=CARTESIAN_POINT ( 'NONE',  ( -29.50000000000000355, -11.50000000000100009, -15.00000000000084910 ) ) ;
#65279=DIRECTION ( 'NONE',  ( 0.000000000000000000, 0.000000000000000000, -1.000000000000000000 ) ) ;
#65282=EDGE_CURVE ( 'NONE', #278, #12416, #68633, .T. ) ;
#65284=DIRECTION ( 'NONE',  ( -1.000000000000000000, 0.000000000000000000, 0.000000000000000000 ) ) ;
#65285=ADVANCED_FACE ( 'NONE', ( #41745 ), #58382, .F. ) ;
#65286=VECTOR ( 'NONE', #53540, 1000.000000000000000 ) ;
#65296=DIRECTION ( 'NONE',  ( -1.000000000000000000, 0.000000000000000000, 0.000000000000000000 ) ) ;
#65310=EDGE_LOOP ( 'NONE', ( #37837, #21214, #31444, #22011 ) ) ;
#65311=DIRECTION ( 'NONE',  ( 0.000000000000000000, 1.000000000000000000, 0.000000000000000000 ) ) ;
#65318=ORIENTED_EDGE ( 'NONE', *, *, #39318, .T. ) ;
#65319=EDGE_LOOP ( 'NONE', ( #25071, #13834, #55640, #16018 ) ) ;
#65322=AXIS2_PLACEMENT_3D ( 'NONE', #38866, #60781, #44860 ) ;
#65335=CARTESIAN_POINT ( 'NONE',  ( -30.00000000000000000, -13.54524521594299991, -17.53999999999999915 ) ) ;
#65337=VERTEX_POINT ( 'NONE', #46349 ) ;
#65341=ORIENTED_EDGE ( 'NONE', *, *, #10471, .F. ) ;
#65342=CARTESIAN_POINT ( 'NONE',  ( 14.25000000000000000, -0.3156864504677177052, 22.25638000318208753 ) ) ;
#65354=PLANE ( 'NONE',  #66301 ) ;
#65355=CARTESIAN_POINT ( 'NONE',  ( -25.50000000000000355, -5.200000000000001066, -20.49999999999999645 ) ) ;
#65365=VECTOR ( 'NONE', #68742, 1000.000000000000000 ) ;
#65367=ORIENTED_EDGE ( 'NONE', *, *, #56069, .F. ) ;
#65368=PLANE ( 'NONE',  #18496 ) ;
#65369=CARTESIAN_POINT ( 'NONE',  ( 30.00000000000000000, -17.35230188589299871, 15.35019951917099945 ) ) ;
#65372=CARTESIAN_POINT ( 'NONE',  ( 25.50000000000000355, -15.50000000000000000, 20.49999999999999645 ) ) ;
#65378=CARTESIAN_POINT ( 'NONE',  ( -11.50000000000000000, -11.50000000000000000, 19.00000000000000000 ) ) ;
#65379=EDGE_LOOP ( 'NONE', ( #69218, #25366 ) ) ;
#65380=CARTESIAN_POINT ( 'NONE',  ( 15.91434062215688350, -0.3156604612129282894, -23.70415600323552852 ) ) ;
#65384=CARTESIAN_POINT ( 'NONE',  ( 28.00000000000000000, -16.28999999999999915, 14.50000000000000000 ) ) ;
#65387=ORIENTED_EDGE ( 'NONE', *, *, #24806, .T. ) ;
#65392=EDGE_CURVE ( 'NONE', #35877, #6775, #3226, .T. ) ;
#65395=CARTESIAN_POINT ( 'NONE',  ( 15.50000000000000000, -5.000000000000000000, -18.50000000000000000 ) ) ;
#65400=EDGE_LOOP ( 'NONE', ( #19501, #13464, #16571, #50815 ) ) ;
#65409=ADVANCED_FACE ( 'NONE', ( #29086 ), #44636, .T. ) ;
#65411=CARTESIAN_POINT ( 'NONE',  ( 25.50000000000000355, -5.200000000000001066, -24.75000000000000000 ) ) ;
#65413=EDGE_LOOP ( 'NONE', ( #3546, #51549, #11887, #66835 ) ) ;
#65417=DIRECTION ( 'NONE',  ( 0.000000000000000000, 0.000000000000000000, 1.000000000000000000 ) ) ;
#65423=VECTOR ( 'NONE', #43627, 1000.000000000000000 ) ;
#65426=CARTESIAN_POINT ( 'NONE',  ( -15.50000000000000000, -0.4000000000005236034, 25.79999999999947136 ) ) ;
#65432=DIRECTION ( 'NONE',  ( -1.000000000000000000, 0.000000000000000000, 0.000000000000000000 ) ) ;
#65445=CARTESIAN_POINT ( 'NONE',  ( 11.00000000000000000, -17.50000000000000000, -15.70500000000000007 ) ) ;
#65451=VERTEX_POINT ( 'NONE', #66226 ) ;
#65454=LINE ( 'NONE', #17012, #49493 ) ;
#65457=AXIS2_PLACEMENT_3D ( 'NONE', #35009, #61179, #46327 ) ;
#65478=CARTESIAN_POINT ( 'NONE',  ( -16.75000000000000000, -2.500000000000000000, -23.22168783648699986 ) ) ;
#65487=DIRECTION ( 'NONE',  ( 0.000000000000000000, 1.000000000000000000, 0.000000000000000000 ) ) ;
#65506=EDGE_CURVE ( 'NONE', #45889, #32328, #55611, .T. ) ;
#65517=DIRECTION ( 'NONE',  ( -1.000000000000000000, 0.000000000000000000, 0.000000000000000000 ) ) ;
#65523=LINE ( 'NONE', #31362, #37831 ) ;
#65526=CARTESIAN_POINT ( 'NONE',  ( -11.50000000000000000, -12.00000000000000000, -10.52786404500095863 ) ) ;
#65528=CARTESIAN_POINT ( 'NONE',  ( -15.50000000000000000, 998.9628421096749662, 22.50000000000000000 ) ) ;
#65533=ORIENTED_EDGE ( 'NONE', *, *, #39679, .T. ) ;
#65534=DIRECTION ( 'NONE',  ( 1.000000000000000000, 0.000000000000000000, 0.000000000000000000 ) ) ;
#65554=CARTESIAN_POINT ( 'NONE',  ( 29.50000000000000355, -12.00000000000000000, -10.69999999999999929 ) ) ;
#65559=LINE ( 'NONE', #17115, #59310 ) ;
#65563=EDGE_CURVE ( 'NONE', #18065, #63676, #52056, .T. ) ;
#65568=CARTESIAN_POINT ( 'NONE',  ( 11.50000000000000000, -11.50000000000000000, 19.00000000000000000 ) ) ;
#65572=ORIENTED_EDGE ( 'NONE', *, *, #56284, .F. ) ;
#65581=ORIENTED_EDGE ( 'NONE', *, *, #48647, .T. ) ;
#65582=DIRECTION ( 'NONE',  ( 0.000000000000000000, -0.7046037717806115097, 0.7096009616626348659 ) ) ;
#65587=DIRECTION ( 'NONE',  ( 0.000000000000000000, 0.7096009616570518874, 0.7046037717862339012 ) ) ;
#65594=VECTOR ( 'NONE', #30009, 1000.000000000000000 ) ;
#65601=ORIENTED_EDGE ( 'NONE', *, *, #54782, .T. ) ;
#65602=VECTOR ( 'NONE', #57265, 1000.000000000000000 ) ;
#65604=CARTESIAN_POINT ( 'NONE',  ( -13.00000000000000178, -17.35230188589299871, 15.35019951917099945 ) ) ;
#65606=EDGE_CURVE ( 'NONE', #2526, #51110, #52782, .T. ) ;
#65617=AXIS2_PLACEMENT_3D ( 'NONE', #8278, #30561, #52854 ) ;
#65627=EDGE_LOOP ( 'NONE', ( #19440, #34466, #8863, #50134, #40024, #52427, #23606, #39066, #5129 ) ) ;
#65630=AXIS2_PLACEMENT_3D ( 'NONE', #4466, #47584, #69152 ) ;
#65631=LINE ( 'NONE', #53645, #67313 ) ;
#65633=VERTEX_POINT ( 'NONE', #14931 ) ;
#65636=EDGE_CURVE ( 'NONE', #43823, #49722, #69367, .T. ) ;
#65641=VERTEX_POINT ( 'NONE', #61418 ) ;
#65643=CARTESIAN_POINT ( 'NONE',  ( 15.50000000000000000, -0.1999999999999999556, 22.50000000000000000 ) ) ;
#65644=AXIS2_PLACEMENT_3D ( 'NONE', #33671, #7132, #60877 ) ;
#65645=ORIENTED_EDGE ( 'NONE', *, *, #18502, .F. ) ;
#65652=VERTEX_POINT ( 'NONE', #28557 ) ;
#65665=ORIENTED_EDGE ( 'NONE', *, *, #54165, .F. ) ;
#65669=DIRECTION ( 'NONE',  ( 0.000000000000000000, -1.000000000000000000, 3.989863994748342081E-13 ) ) ;
#65671=ORIENTED_EDGE ( 'NONE', *, *, #13303, .T. ) ;
#65672=VECTOR ( 'NONE', #23431, 1000.000000000000000 ) ;
#65674=DIRECTION ( 'NONE',  ( -1.000000000000000000, 0.000000000000000000, 0.000000000000000000 ) ) ;
#65690=DIRECTION ( 'NONE',  ( 1.000000000000000000, -0.000000000000000000, -0.000000000000000000 ) ) ;
#65697=DIRECTION ( 'NONE',  ( 0.000000000000000000, 3.989863994748342081E-13, 1.000000000000000000 ) ) ;
#65698=DIRECTION ( 'NONE',  ( 0.000000000000000000, 1.000000000000000000, 0.000000000000000000 ) ) ;
#65702=CARTESIAN_POINT ( 'NONE',  ( -29.50000000000000355, -11.50000000000000000, 15.00000000000000000 ) ) ;
#65704=LINE ( 'NONE', #65369, #45129 ) ;
#65713=CARTESIAN_POINT ( 'NONE',  ( -11.00000000000000000, -16.28999999999999915, 14.50000000000000000 ) ) ;
#65723=DIRECTION ( 'NONE',  ( 0.000000000000000000, 0.000000000000000000, 1.000000000000000000 ) ) ;
#65731=CARTESIAN_POINT ( 'NONE',  ( 17.24945551514599984, -15.50000000000000000, 25.53140320652400064 ) ) ;
#65734=VERTEX_POINT ( 'NONE', #44470 ) ;
#65740=ORIENTED_EDGE ( 'NONE', *, *, #63392, .F. ) ;
#65748=ORIENTED_EDGE ( 'NONE', *, *, #53036, .F. ) ;
#65751=FACE_OUTER_BOUND ( 'NONE', #68350, .T. ) ;
#65756=DIRECTION ( 'NONE',  ( 0.000000000000000000, 1.000000000000000000, 0.000000000000000000 ) ) ;
#65765=DIRECTION ( 'NONE',  ( -0.000000000000000000, 1.000000000000000000, -0.000000000000000000 ) ) ;
#65766=CARTESIAN_POINT ( 'NONE',  ( -16.75000000000000000, -0.2038245569916330158, -21.77831216351300014 ) ) ;
#65767=CARTESIAN_POINT ( 'NONE',  ( -28.00000000000000000, -15.50000000000000000, -14.50000000000000000 ) ) ;
#65768=LINE ( 'NONE', #21268, #30125 ) ;
#65770=DIRECTION ( 'NONE',  ( -1.000000000000000000, 0.000000000000000000, 0.000000000000000000 ) ) ;
#65772=FACE_OUTER_BOUND ( 'NONE', #61010, .T. ) ;
#65781=ORIENTED_EDGE ( 'NONE', *, *, #49140, .F. ) ;
#65783=EDGE_CURVE ( 'NONE', #42614, #61558, #29601, .T. ) ;
#65784=CARTESIAN_POINT ( 'NONE',  ( 16.75000000000000000, -2.500000000000000000, -21.77831216351300014 ) ) ;
#65785=AXIS2_PLACEMENT_3D ( 'NONE', #7945, #29521, #44725 ) ;
#65791=EDGE_CURVE ( 'NONE', #54299, #51332, #62468, .T. ) ;
#65794=LINE ( 'NONE', #7077, #45143 ) ;
#65798=CARTESIAN_POINT ( 'NONE',  ( -11.75000000000000000, -5.000000000000000000, 23.89194109070750116 ) ) ;
#65804=DIRECTION ( 'NONE',  ( 0.000000000000000000, 1.000000000000000000, 0.000000000000000000 ) ) ;
#65809=ORIENTED_EDGE ( 'NONE', *, *, #24236, .T. ) ;
#65812=DIRECTION ( 'NONE',  ( 0.000000000000000000, 0.000000000000000000, 1.000000000000000000 ) ) ;
#65814=VECTOR ( 'NONE', #28810, 1000.000000000000000 ) ;
#65819=DIRECTION ( 'NONE',  ( 0.000000000000000000, -1.000000000000000000, 0.000000000000000000 ) ) ;
#65826=EDGE_CURVE ( 'NONE', #58012, #4367, #55669, .T. ) ;
#65836=AXIS2_PLACEMENT_3D ( 'NONE', #28736, #1877, #44999 ) ;
#65839=EDGE_LOOP ( 'NONE', ( #13899, #67674, #49120, #22995 ) ) ;
#65850=CARTESIAN_POINT ( 'NONE',  ( 11.50000000000000000, -11.50000000000100009, -19.50000000000103739 ) ) ;
#65856=EDGE_CURVE ( 'NONE', #67811, #64214, #56825, .T. ) ;
#65857=FACE_OUTER_BOUND ( 'NONE', #10900, .T. ) ;
#65860=FACE_BOUND ( 'NONE', #9115, .T. ) ;
#65863=CARTESIAN_POINT ( 'NONE',  ( 11.75000000000000000, -5.200000000000001066, 26.25000000000000000 ) ) ;
#65865=ORIENTED_EDGE ( 'NONE', *, *, #23293, .T. ) ;
#65867=CARTESIAN_POINT ( 'NONE',  ( 30.00000000000000000, -17.14999999999999858, -27.00000000000000000 ) ) ;
#65868=AXIS2_PLACEMENT_3D ( 'NONE', #49006, #22132, #65279 ) ;
#65875=ORIENTED_EDGE ( 'NONE', *, *, #40865, .F. ) ;
#65878=ORIENTED_EDGE ( 'NONE', *, *, #45588, .F. ) ;
#65880=AXIS2_PLACEMENT_3D ( 'NONE', #35609, #62849, #46571 ) ;
#65881=CARTESIAN_POINT ( 'NONE',  ( 29.50000000000000355, -11.50000000000100009, -19.50000000000103739 ) ) ;
#65892=DIRECTION ( 'NONE',  ( 0.000000000000000000, 1.000000000000000000, 0.000000000000000000 ) ) ;
#65894=ORIENTED_EDGE ( 'NONE', *, *, #13623, .F. ) ;
#65901=ORIENTED_EDGE ( 'NONE', *, *, #54207, .T. ) ;
#65902=ORIENTED_EDGE ( 'NONE', *, *, #23833, .T. ) ;
#65911=ORIENTED_EDGE ( 'NONE', *, *, #60978, .F. ) ;
#65915=AXIS2_PLACEMENT_3D ( 'NONE', #3928, #14887, #30796 ) ;
#65918=DIRECTION ( 'NONE',  ( 0.000000000000000000, -1.000000000000000000, 0.000000000000000000 ) ) ;
#65919=DIRECTION ( 'NONE',  ( 0.000000000000000000, 0.000000000000000000, -1.000000000000000000 ) ) ;
#65921=ORIENTED_EDGE ( 'NONE', *, *, #11983, .F. ) ;
#65932=DIRECTION ( 'NONE',  ( -1.000000000000000000, 0.000000000000000000, 0.000000000000000000 ) ) ;
#65933=LINE ( 'NONE', #17857, #42072 ) ;
#65944=ORIENTED_EDGE ( 'NONE', *, *, #44100, .T. ) ;
#65945=DIRECTION ( 'NONE',  ( -1.000000000000000000, 0.000000000000000000, 0.000000000000000000 ) ) ;
#65950=VECTOR ( 'NONE', #873, 1000.000000000000000 ) ;
#65959=AXIS2_PLACEMENT_3D ( 'NONE', #36792, #3911, #14151 ) ;
#65961=ADVANCED_FACE ( 'NONE', ( #32422 ), #69194, .T. ) ;
#65964=EDGE_CURVE ( 'NONE', #39751, #58695, #52594, .T. ) ;
#65965=AXIS2_PLACEMENT_3D ( 'NONE', #8354, #55761, #51149 ) ;
#65982=DIRECTION ( 'NONE',  ( 0.000000000000000000, 0.000000000000000000, -1.000000000000000000 ) ) ;
#65996=ORIENTED_EDGE ( 'NONE', *, *, #31973, .F. ) ;
#65997=ORIENTED_EDGE ( 'NONE', *, *, #43462, .F. ) ;
#66001=AXIS2_PLACEMENT_3D ( 'NONE', #69169, #20724, #46892 ) ;
#66005=DIRECTION ( 'NONE',  ( 1.000000000000000000, 0.000000000000000000, 0.000000000000000000 ) ) ;
#66013=ORIENTED_EDGE ( 'NONE', *, *, #49645, .F. ) ;
#66026=EDGE_CURVE ( 'NONE', #59384, #1121, #38748, .T. ) ;
#66038=PLANE ( 'NONE',  #3931 ) ;
#66041=CARTESIAN_POINT ( 'NONE',  ( 11.50000000000000000, -11.50000000000100009, 15.00000000000084910 ) ) ;
#66044=CIRCLE ( 'NONE', #26549, 2.250000000000001776 ) ;
#66050=CIRCLE ( 'NONE', #35564, 0.5000000000001362244 ) ;
#66054=DIRECTION ( 'NONE',  ( 0.4998444328988824181, 0.000000000000000000, -0.8661152018640445593 ) ) ;
#66059=VERTEX_POINT ( 'NONE', #49026 ) ;
#66063=B_SPLINE_CURVE_WITH_KNOTS ( 'NONE', 3,
 ( #9621, #30828, #10315, #42485, #64082, #52404 ),
 .UNSPECIFIED., .F., .F.,
 ( 4, 2, 4 ),
 ( 1.820537833122031213, 2.555393473688635453, 3.290249114255239693 ),
 .UNSPECIFIED. ) ;
#66066=VECTOR ( 'NONE', #67253, 1000.000000000000000 ) ;
#66068=DIRECTION ( 'NONE',  ( 0.000000000000000000, 0.7046037717862339012, -0.7096009616570518874 ) ) ;
#66072=ORIENTED_EDGE ( 'NONE', *, *, #56999, .F. ) ;
#66085=AXIS2_PLACEMENT_3D ( 'NONE', #33534, #60746, #42146 ) ;
#66089=VECTOR ( 'NONE', #42754, 1000.000000000000000 ) ;
#66096=LINE ( 'NONE', #45217, #58406 ) ;
#66100=ORIENTED_EDGE ( 'NONE', *, *, #34107, .T. ) ;
#66102=EDGE_LOOP ( 'NONE', ( #59338, #35060, #30277, #14983 ) ) ;
#66111=EDGE_CURVE ( 'NONE', #57822, #50308, #45556, .T. ) ;
#66119=FACE_OUTER_BOUND ( 'NONE', #11012, .T. ) ;
#66125=DIRECTION ( 'NONE',  ( 0.000000000000000000, 0.000000000000000000, 1.000000000000000000 ) ) ;
#66143=FACE_OUTER_BOUND ( 'NONE', #14985, .T. ) ;
#66145=VECTOR ( 'NONE', #43366, 1000.000000000000000 ) ;
#66168=ORIENTED_EDGE ( 'NONE', *, *, #19385, .T. ) ;
#66171=DIRECTION ( 'NONE',  ( 0.000000000000000000, 1.000000000000000000, -1.500535806722257514E-12 ) ) ;
#66182=LINE ( 'NONE', #1472, #40147 ) ;
#66188=ADVANCED_FACE ( 'NONE', ( #45789 ), #13615, .F. ) ;
#66207=CARTESIAN_POINT ( 'NONE',  ( 11.00000000000000000, -16.28999999999710369, -14.50000000000000000 ) ) ;
#66211=VECTOR ( 'NONE', #54117, 1000.000000000000000 ) ;
#66212=LINE ( 'NONE', #61577, #54721 ) ;
#66214=DIRECTION ( 'NONE',  ( 0.000000000000000000, 0.000000000000000000, -1.000000000000000000 ) ) ;
#66215=DIRECTION ( 'NONE',  ( 0.000000000000000000, 0.7046037717862339012, -0.7096009616570518874 ) ) ;
#66226=CARTESIAN_POINT ( 'NONE',  ( 23.48000000000000043, -15.50000000000000000, 26.00000000000000355 ) ) ;
#66230=EDGE_CURVE ( 'NONE', #67811, #22061, #11698, .T. ) ;
#66234=ORIENTED_EDGE ( 'NONE', *, *, #9425, .F. ) ;
#66235=PLANE ( 'NONE',  #59291 ) ;
#66249=VECTOR ( 'NONE', #11911, 1000.000000000000000 ) ;
#66251=VERTEX_POINT ( 'NONE', #30934 ) ;
#66255=DIRECTION ( 'NONE',  ( -1.000000000000000000, 0.000000000000000000, 0.000000000000000000 ) ) ;
#66262=ORIENTED_EDGE ( 'NONE', *, *, #41913, .T. ) ;
#66270=EDGE_CURVE ( 'NONE', #64180, #9560, #68134, .T. ) ;
#66275=ADVANCED_FACE ( 'NONE', ( #20321 ), #36578, .T. ) ;
#66281=AXIS2_PLACEMENT_3D ( 'NONE', #20625, #46450, #35846 ) ;
#66285=CARTESIAN_POINT ( 'NONE',  ( 11.00000000000000000, -11.10796162543699950, -9.102987789146602893 ) ) ;
#66287=LINE ( 'NONE', #28784, #32841 ) ;
#66296=VERTEX_POINT ( 'NONE', #53223 ) ;
#66301=AXIS2_PLACEMENT_3D ( 'NONE', #11579, #6295, #38481 ) ;
#66302=AXIS2_PLACEMENT_3D ( 'NONE', #27162, #31782, #21848 ) ;
#66307=CIRCLE ( 'NONE', #34696, 4.000000000000000888 ) ;
#66310=CARTESIAN_POINT ( 'NONE',  ( 30.00000000000000000, -11.50000000000000000, -15.00000000000000000 ) ) ;
#66311=DIRECTION ( 'NONE',  ( 0.000000000000000000, 0.000000000000000000, -1.000000000000000000 ) ) ;
#66316=VECTOR ( 'NONE', #50022, 1000.000000000000000 ) ;
#66332=EDGE_LOOP ( 'NONE', ( #56, #22325, #30419, #27184 ) ) ;
#66340=DIRECTION ( 'NONE',  ( -1.000000000000000000, 0.000000000000000000, 0.000000000000000000 ) ) ;
#66341=CARTESIAN_POINT ( 'NONE',  ( -13.00000000000000178, -17.50000000000000000, 20.05051025721700242 ) ) ;
#66370=DIRECTION ( 'NONE',  ( 8.659560562354963673E-17, 0.7071067811865450192, -0.7071067811865500152 ) ) ;
#66372=VECTOR ( 'NONE', #25341, 1000.000000000000000 ) ;
#66373=CARTESIAN_POINT ( 'NONE',  ( 14.25000000000000000, -0.2038245569916330158, 23.22168783648699986 ) ) ;
#66375=CARTESIAN_POINT ( 'NONE',  ( 11.00000000000000000, -17.50000000000000000, 15.70499999999969809 ) ) ;
#66376=VERTEX_POINT ( 'NONE', #59555 ) ;
#66384=FACE_OUTER_BOUND ( 'NONE', #61335, .T. ) ;
#66387=DIRECTION ( 'NONE',  ( 0.000000000000000000, 0.000000000000000000, -1.000000000000000000 ) ) ;
#66391=CARTESIAN_POINT ( 'NONE',  ( 11.00000000000000000, -12.00000000000000000, 12.19999999999999929 ) ) ;
#66396=PLANE ( 'NONE',  #15363 ) ;
#66398=EDGE_CURVE ( 'NONE', #50592, #14101, #38856, .T. ) ;
#66399=DIRECTION ( 'NONE',  ( 0.8660254037844482555, 0.000000000000000000, -0.4999999999999831801 ) ) ;
#66408=CARTESIAN_POINT ( 'NONE',  ( -14.25000000000000000, -0.2038245569916330158, -23.22168783648699986 ) ) ;
#66409=AXIS2_PLACEMENT_3D ( 'NONE', #38537, #44167, #60088 ) ;
#66413=EDGE_CURVE ( 'NONE', #35470, #24440, #34041, .T. ) ;
#66416=ORIENTED_EDGE ( 'NONE', *, *, #55984, .T. ) ;
#66417=LINE ( 'NONE', #7352, #27215 ) ;
#66432=EDGE_CURVE ( 'NONE', #24441, #8384, #38675, .T. ) ;
#66446=EDGE_CURVE ( 'NONE', #48776, #57629, #54603, .T. ) ;
#66448=ORIENTED_EDGE ( 'NONE', *, *, #58766, .T. ) ;
#66456=ORIENTED_EDGE ( 'NONE', *, *, #48970, .F. ) ;
#66465=LINE ( 'NONE', #33599, #7360 ) ;
#66472=EDGE_LOOP ( 'NONE', ( #1234, #3565, #20802, #16078 ) ) ;
#66480=CARTESIAN_POINT ( 'NONE',  ( 28.00000000000000000, -17.50000000000000000, -15.70500000000000362 ) ) ;
#66483=ORIENTED_EDGE ( 'NONE', *, *, #7168, .F. ) ;
#66488=LINE ( 'NONE', #50585, #27955 ) ;
#66494=ORIENTED_EDGE ( 'NONE', *, *, #41204, .F. ) ;
#66501=EDGE_CURVE ( 'NONE', #54584, #29722, #51012, .T. ) ;
#66509=EDGE_CURVE ( 'NONE', #1941, #15054, #19623, .T. ) ;
#66517=VECTOR ( 'NONE', #57518, 1000.000000000000000 ) ;
#66520=EDGE_CURVE ( 'NONE', #56741, #20459, #46057, .T. ) ;
#66522=ORIENTED_EDGE ( 'NONE', *, *, #19836, .F. ) ;
#66527=DIRECTION ( 'NONE',  ( -1.000000000000000000, 0.000000000000000000, 0.000000000000000000 ) ) ;
#66529=ORIENTED_EDGE ( 'NONE', *, *, #20714, .F. ) ;
#66534=ADVANCED_FACE ( 'NONE', ( #34742 ), #39698, .F. ) ;
#66537=VERTEX_POINT ( 'NONE', #8569 ) ;
#66557=AXIS2_PLACEMENT_3D ( 'NONE', #69712, #15263, #37189 ) ;
#66564=CIRCLE ( 'NONE', #50759, 2.250000000000001776 ) ;
#66568=DIRECTION ( 'NONE',  ( 0.000000000000000000, 0.000000000000000000, 1.000000000000000000 ) ) ;
#66574=FACE_BOUND ( 'NONE', #65379, .T. ) ;
#66578=CARTESIAN_POINT ( 'NONE',  ( -17.00000000000000000, -16.28999999999999915, 14.50000000000000000 ) ) ;
#66581=ORIENTED_EDGE ( 'NONE', *, *, #32529, .T. ) ;
#66582=CARTESIAN_POINT ( 'NONE',  ( -11.00000000000000000, -8.959999999999999076, 17.04524521594300523 ) ) ;
#66585=LINE ( 'NONE', #23099, #9007 ) ;
#66587=AXIS2_PLACEMENT_3D ( 'NONE', #43673, #26363, #5148 ) ;
#66588=CARTESIAN_POINT ( 'NONE',  ( 11.00000000000000000, -17.50000000000000000, 26.64999999999999858 ) ) ;
#66591=VERTEX_POINT ( 'NONE', #69739 ) ;
#66610=AXIS2_PLACEMENT_3D ( 'NONE', #3189, #40998, #62929 ) ;
#66612=CARTESIAN_POINT ( 'NONE',  ( 11.75000000000000000, -5.000000000000000000, 23.89194109070750116 ) ) ;
#66613=CIRCLE ( 'NONE', #4557, 0.5000000000079362072 ) ;
#66627=CARTESIAN_POINT ( 'NONE',  ( 30.00000000000000000, -12.00000000000000000, 11.00000000000000000 ) ) ;
#66628=DIRECTION ( 'NONE',  ( 0.000000000000000000, 0.000000000000000000, 1.000000000000000000 ) ) ;
#66640=VECTOR ( 'NONE', #41051, 1000.000000000000000 ) ;
#66649=VECTOR ( 'NONE', #20040, 1000.000000000000000 ) ;
#66672=VECTOR ( 'NONE', #12842, 1000.000000000000000 ) ;
#66686=FACE_OUTER_BOUND ( 'NONE', #22954, .T. ) ;
#66694=EDGE_CURVE ( 'NONE', #63027, #8802, #2762, .T. ) ;
#66697=EDGE_CURVE ( 'NONE', #36899, #13975, #52454, .T. ) ;
#66702=VECTOR ( 'NONE', #46141, 1000.000000000000000 ) ;
#66708=CARTESIAN_POINT ( 'NONE',  ( -30.00000000000000000, -17.50000000000000000, 26.64999999999999858 ) ) ;
#66710=FACE_OUTER_BOUND ( 'NONE', #55062, .T. ) ;
#66719=CARTESIAN_POINT ( 'NONE',  ( 30.00000000000000000, -17.00000000000000000, 15.70499999999969809 ) ) ;
#66724=FACE_BOUND ( 'NONE', #53788, .T. ) ;
#66726=CARTESIAN_POINT ( 'NONE',  ( 29.50000000000000355, -15.97213595500069871, 14.50000000000000000 ) ) ;
#66727=EDGE_LOOP ( 'NONE', ( #30547, #44920, #53093, #16436 ) ) ;
#66730=ORIENTED_EDGE ( 'NONE', *, *, #53027, .T. ) ;
#66731=FACE_BOUND ( 'NONE', #18391, .T. ) ;
#66736=EDGE_CURVE ( 'NONE', #14932, #22707, #36641, .T. ) ;
#66743=LINE ( 'NONE', #2738, #57060 ) ;
#66744=VERTEX_POINT ( 'NONE', #12048 ) ;
#66753=CARTESIAN_POINT ( 'NONE',  ( -11.50000000000000000, -11.70000000000000284, 11.00000000000000000 ) ) ;
#66756=CONICAL_SURFACE ( 'NONE', #48713, 2.000000000000001776, 0.7853981633974503884 ) ;
#66780=ADVANCED_FACE ( 'NONE', ( #55199 ), #6421, .T. ) ;
#66781=PLANE ( 'NONE',  #25691 ) ;
#66784=AXIS2_PLACEMENT_3D ( 'NONE', #22302, #4648, #26211 ) ;
#66786=AXIS2_PLACEMENT_3D ( 'NONE', #65426, #16284, #37861 ) ;
#66801=LINE ( 'NONE', #18352, #15006 ) ;
#66803=DIRECTION ( 'NONE',  ( -0.3479852726768751237, 0.000000000000000000, -0.9375000000000004441 ) ) ;
#66807=EDGE_LOOP ( 'NONE', ( #26061, #54980, #9696, #2950 ) ) ;
#66808=FACE_OUTER_BOUND ( 'NONE', #34272, .T. ) ;
#66824=CARTESIAN_POINT ( 'NONE',  ( 30.00000000000000000, -11.85423089348099879, 9.852125413066602277 ) ) ;
#66828=DIRECTION ( 'NONE',  ( 0.000000000000000000, 1.000000000000000000, 0.000000000000000000 ) ) ;
#66835=ORIENTED_EDGE ( 'NONE', *, *, #66509, .F. ) ;
#66860=ORIENTED_EDGE ( 'NONE', *, *, #12770, .F. ) ;
#66876=DIRECTION ( 'NONE',  ( -1.000000000000000000, 0.000000000000000000, 0.000000000000000000 ) ) ;
#66877=CIRCLE ( 'NONE', #60129, 4.500000000000190958 ) ;
#66879=LINE ( 'NONE', #61570, #28956 ) ;
#66881=ADVANCED_FACE ( 'NONE', ( #7086 ), #23702, .F. ) ;
#66883=CONICAL_SURFACE ( 'NONE', #57862, 1.621000000000000885, 0.7853981633974518317 ) ;
#66893=CARTESIAN_POINT ( 'NONE',  ( 15.50000000000000000, -5.000000000000000000, 22.50000000000000000 ) ) ;
#66895=EDGE_CURVE ( 'NONE', #31751, #19212, #2483, .T. ) ;
#66900=FACE_OUTER_BOUND ( 'NONE', #53210, .T. ) ;
#66917=DIRECTION ( 'NONE',  ( -0.000000000000000000, 1.000000000000000000, -0.000000000000000000 ) ) ;
#66923=ORIENTED_EDGE ( 'NONE', *, *, #18153, .T. ) ;
#66937=ORIENTED_EDGE ( 'NONE', *, *, #53948, .T. ) ;
#66941=CARTESIAN_POINT ( 'NONE',  ( 28.00000000000000000, -17.50000000000000000, 20.05051025721700242 ) ) ;
#66943=CARTESIAN_POINT ( 'NONE',  ( -15.70366306705060033, -0.2717122460100995229, 23.82579074638835692 ) ) ;
#66947=LINE ( 'NONE', #19217, #66672 ) ;
#66957=LINE ( 'NONE', #39392, #7461 ) ;
#66963=VERTEX_POINT ( 'NONE', #14503 ) ;
#66969=CARTESIAN_POINT ( 'NONE',  ( 11.00000000000000000, -9.199999999999999289, -12.69999999999986073 ) ) ;
#66977=CARTESIAN_POINT ( 'NONE',  ( 15.50000000000000000, -0.4000000000005274892, 25.79999999999946780 ) ) ;
#66986=ADVANCED_FACE ( 'NONE', ( #53393 ), #42421, .F. ) ;
#66987=ORIENTED_EDGE ( 'NONE', *, *, #46392, .F. ) ;
#66990=VECTOR ( 'NONE', #60376, 1000.000000000000000 ) ;
#67001=CARTESIAN_POINT ( 'NONE',  ( -17.24945551514599984, -15.50000000000000000, -25.53140320652400064 ) ) ;
#67021=CARTESIAN_POINT ( 'NONE',  ( -14.24999999999999822, -0.3152037684892585179, -22.74589050208021135 ) ) ;
#67026=DIRECTION ( 'NONE',  ( -0.000000000000000000, 1.000000000000000000, -0.000000000000000000 ) ) ;
#67040=B_SPLINE_CURVE_WITH_KNOTS ( 'NONE', 3,
 ( #56692, #13555, #36167, #8594, #66943, #3297 ),
 .UNSPECIFIED., .F., .F.,
 ( 4, 2, 4 ),
 ( 0.0002380763768113913770, 0.7291065797294570272, 1.457975083082102774 ),
 .UNSPECIFIED. ) ;
#67046=EDGE_CURVE ( 'NONE', #24537, #67547, #64343, .T. ) ;
#67059=CARTESIAN_POINT ( 'NONE',  ( 30.00000000000000000, -11.10796162543699950, 9.102987789146602893 ) ) ;
#67065=DIRECTION ( 'NONE',  ( 0.000000000000000000, 0.000000000000000000, 1.000000000000000000 ) ) ;
#67068=VECTOR ( 'NONE', #62582, 1000.000000000000000 ) ;
#67071=DIRECTION ( 'NONE',  ( 0.000000000000000000, 1.000000000000000000, 0.000000000000000000 ) ) ;
#67080=CARTESIAN_POINT ( 'NONE',  ( 30.00000000000000000, -12.00000000000000000, -10.20500000000000007 ) ) ;
#67085=FACE_OUTER_BOUND ( 'NONE', #59400, .T. ) ;
#67088=VERTEX_POINT ( 'NONE', #687 ) ;
#67099=EDGE_CURVE ( 'NONE', #47170, #26707, #49113, .T. ) ;
#67100=EDGE_CURVE ( 'NONE', #63611, #28340, #25390, .T. ) ;
#67113=ORIENTED_EDGE ( 'NONE', *, *, #68670, .F. ) ;
#67115=PLANE ( 'NONE',  #20867 ) ;
#67116=CARTESIAN_POINT ( 'NONE',  ( -29.50000000000000355, -11.70000000000012008, -10.70000000000011831 ) ) ;
#67120=ORIENTED_EDGE ( 'NONE', *, *, #7498, .F. ) ;
#67133=AXIS2_PLACEMENT_3D ( 'NONE', #29715, #7795, #28676 ) ;
#67135=DIRECTION ( 'NONE',  ( 0.000000000000000000, 0.000000000000000000, 1.000000000000000000 ) ) ;
#67136=ORIENTED_EDGE ( 'NONE', *, *, #27261, .F. ) ;
#67151=DIRECTION ( 'NONE',  ( -0.9375000000000006661, 0.000000000000000000, -0.3479852726768744020 ) ) ;
#67159=CARTESIAN_POINT ( 'NONE',  ( 11.50000000000000000, -11.50000000000100009, 15.00000000000084910 ) ) ;
#67166=ORIENTED_EDGE ( 'NONE', *, *, #49141, .T. ) ;
#67168=EDGE_LOOP ( 'NONE', ( #14076, #4378, #24009, #39050 ) ) ;
#67178=FACE_OUTER_BOUND ( 'NONE', #64321, .T. ) ;
#67185=DIRECTION ( 'NONE',  ( 1.000000000000000000, -0.000000000000000000, -0.000000000000000000 ) ) ;
#67195=DIRECTION ( 'NONE',  ( 0.000000000000000000, 0.000000000000000000, 1.000000000000000000 ) ) ;
#67198=CARTESIAN_POINT ( 'NONE',  ( -15.50000000000000000, -0.4000000000005236034, 22.50000000000000000 ) ) ;
#67199=VERTEX_POINT ( 'NONE', #61804 ) ;
#67202=DIRECTION ( 'NONE',  ( 0.000000000000000000, -0.7084617869623469621, -0.7057491738671168857 ) ) ;
#67206=AXIS2_PLACEMENT_3D ( 'NONE', #30146, #61964, #46056 ) ;
#67210=CARTESIAN_POINT ( 'NONE',  ( -11.00000000000000000, -5.599999999999379696, 26.60000000000059828 ) ) ;
#67212=AXIS2_PLACEMENT_3D ( 'NONE', #21521, #48745, #43083 ) ;
#67213=VECTOR ( 'NONE', #10023, 1000.000000000000000 ) ;
#67222=FACE_OUTER_BOUND ( 'NONE', #35710, .T. ) ;
#67228=ORIENTED_EDGE ( 'NONE', *, *, #5792, .F. ) ;
#67237=VECTOR ( 'NONE', #31882, 1000.000000000000000 ) ;
#67238=ORIENTED_EDGE ( 'NONE', *, *, #58715, .F. ) ;
#67239=CARTESIAN_POINT ( 'NONE',  ( 11.00000000000000000, -11.50000000000000000, 19.00000000000000000 ) ) ;
#67240=CARTESIAN_POINT ( 'NONE',  ( 30.00000000000000000, -11.50000000000100009, 19.50000000000103739 ) ) ;
#67243=CARTESIAN_POINT ( 'NONE',  ( 16.75000000000000000, -2.500000000000000000, 23.22168783648699986 ) ) ;
#67250=CARTESIAN_POINT ( 'NONE',  ( -15.50000000000000000, -1.037157890325000054, -22.50000000000000000 ) ) ;
#67253=DIRECTION ( 'NONE',  ( 0.000000000000000000, -1.000000000000000000, 0.000000000000000000 ) ) ;
#67259=DIRECTION ( 'NONE',  ( -1.000000000000000000, 0.000000000000000000, 0.000000000000000000 ) ) ;
#67276=FACE_BOUND ( 'NONE', #23063, .T. ) ;
#67280=CARTESIAN_POINT ( 'NONE',  ( 13.00000000000000178, -17.50000000000000000, 15.70500000000000007 ) ) ;
#67282=DIRECTION ( 'NONE',  ( 0.7142857142857395036, 0.000000000000000000, 0.6998542122237394469 ) ) ;
#67283=CARTESIAN_POINT ( 'NONE',  ( 25.50000000000000355, 0.000000000000000000, 22.50000000000000000 ) ) ;
#67285=ORIENTED_EDGE ( 'NONE', *, *, #30136, .F. ) ;
#67291=DIRECTION ( 'NONE',  ( 0.000000000000000000, -0.1111111111108836896, 0.9938079899999319178 ) ) ;
#67299=VERTEX_POINT ( 'NONE', #33873 ) ;
#67300=ORIENTED_EDGE ( 'NONE', *, *, #50200, .F. ) ;
#67304=DIRECTION ( 'NONE',  ( -1.000000000000000000, 0.000000000000000000, 0.000000000000000000 ) ) ;
#67305=DIRECTION ( 'NONE',  ( -1.000000000000000000, 0.000000000000000000, 0.000000000000000000 ) ) ;
#67309=VECTOR ( 'NONE', #28449, 1000.000000000000000 ) ;
#67310=VERTEX_POINT ( 'NONE', #10427 ) ;
#67313=VECTOR ( 'NONE', #17186, 1000.000000000000000 ) ;
#67315=FACE_OUTER_BOUND ( 'NONE', #39458, .T. ) ;
#67324=DIRECTION ( 'NONE',  ( 0.000000000000000000, 0.000000000000000000, -1.000000000000000000 ) ) ;
#67332=VERTEX_POINT ( 'NONE', #38003 ) ;
#67333=ORIENTED_EDGE ( 'NONE', *, *, #55542, .F. ) ;
#67355=EDGE_LOOP ( 'NONE', ( #55373, #37798, #16247, #51554, #14340, #7787, #50178, #23399, #57263, #23969, #45445, #45045, #55408, #45680, #42741, #61242, #35894, #27124 ) ) ;
#67357=CARTESIAN_POINT ( 'NONE',  ( 13.00000000000000178, -15.50000000000000000, -20.05051025721700242 ) ) ;
#67359=DIRECTION ( 'NONE',  ( 1.000000000000000000, -0.000000000000000000, -0.000000000000000000 ) ) ;
#67374=ADVANCED_FACE ( 'NONE', ( #42946 ), #58169, .T. ) ;
#67377=AXIS2_PLACEMENT_3D ( 'NONE', #43060, #69931, #26118 ) ;
#67380=ORIENTED_EDGE ( 'NONE', *, *, #28786, .F. ) ;
#67381=EDGE_CURVE ( 'NONE', #47223, #37085, #59216, .T. ) ;
#67385=ORIENTED_EDGE ( 'NONE', *, *, #19477, .F. ) ;
#67387=CARTESIAN_POINT ( 'NONE',  ( -14.25000000000000000, -0.3156864504677185379, -22.25638000318209109 ) ) ;
#67390=ORIENTED_EDGE ( 'NONE', *, *, #54552, .F. ) ;
#67399=DIRECTION ( 'NONE',  ( 0.000000000000000000, -1.000000000000000000, 0.000000000000000000 ) ) ;
#67403=EDGE_CURVE ( 'NONE', #55252, #36470, #59903, .T. ) ;
#67406=EDGE_CURVE ( 'NONE', #26198, #32897, #64971, .T. ) ;
#67419=VECTOR ( 'NONE', #15871, 1000.000000000000000 ) ;
#67420=CIRCLE ( 'NONE', #15499, 4.000000000000000888 ) ;
#67421=ADVANCED_FACE ( 'NONE', ( #12150, #28753 ), #44662, .F. ) ;
#67425=VECTOR ( 'NONE', #4807, 1000.000000000000000 ) ;
#67429=VERTEX_POINT ( 'NONE', #54614 ) ;
#67430=VERTEX_POINT ( 'NONE', #517 ) ;
#67437=VERTEX_POINT ( 'NONE', #49974 ) ;
#67444=FACE_BOUND ( 'NONE', #65627, .T. ) ;
#67447=ORIENTED_EDGE ( 'NONE', *, *, #41913, .F. ) ;
#67451=DIRECTION ( 'NONE',  ( 0.000000000000000000, 0.000000000000000000, 1.000000000000000000 ) ) ;
#67452=LINE ( 'NONE', #46912, #15292 ) ;
#67454=DIRECTION ( 'NONE',  ( -1.000000000000000000, 0.000000000000000000, 0.000000000000000000 ) ) ;
#67455=FACE_OUTER_BOUND ( 'NONE', #65310, .T. ) ;
#67459=ORIENTED_EDGE ( 'NONE', *, *, #22037, .F. ) ;
#67461=DIRECTION ( 'NONE',  ( 0.000000000000000000, 0.000000000000000000, -1.000000000000000000 ) ) ;
#67464=EDGE_CURVE ( 'NONE', #48929, #65032, #43502, .T. ) ;
#67472=EDGE_CURVE ( 'NONE', #4926, #19062, #65559, .T. ) ;
#67476=ORIENTED_EDGE ( 'NONE', *, *, #46646, .F. ) ;
#67485=VECTOR ( 'NONE', #58839, 1000.000000000000000 ) ;
#67487=DIRECTION ( 'NONE',  ( 0.000000000000000000, 0.000000000000000000, 1.000000000000000000 ) ) ;
#67489=ORIENTED_EDGE ( 'NONE', *, *, #27486, .F. ) ;
#67491=EDGE_LOOP ( 'NONE', ( #6466, #4987, #11053, #93 ) ) ;
#67492=ORIENTED_EDGE ( 'NONE', *, *, #67046, .T. ) ;
#67497=AXIS2_PLACEMENT_3D ( 'NONE', #2370, #23932, #46192 ) ;
#67498=LINE ( 'NONE', #62881, #18968 ) ;
#67508=EDGE_CURVE ( 'NONE', #58770, #4599, #1210, .T. ) ;
#67517=CARTESIAN_POINT ( 'NONE',  ( -24.00000000000000000, -16.64230188589299786, 14.64519951917100116 ) ) ;
#67521=DIRECTION ( 'NONE',  ( 0.000000000000000000, 0.000000000000000000, -1.000000000000000000 ) ) ;
#67530=ORIENTED_EDGE ( 'NONE', *, *, #43445, .F. ) ;
#67533=VECTOR ( 'NONE', #18703, 1000.000000000000000 ) ;
#67545=PLANE ( 'NONE',  #22472 ) ;
#67546=DIRECTION ( 'NONE',  ( 0.000000000000000000, -0.7057491738665938596, 0.7084617869628679898 ) ) ;
#67547=VERTEX_POINT ( 'NONE', #18848 ) ;
#67568=CARTESIAN_POINT ( 'NONE',  ( -11.50000000000000000, -11.50000000000000000, -11.00000000000000000 ) ) ;
#67570=DIRECTION ( 'NONE',  ( 0.000000000000000000, 1.000000000000000000, 0.000000000000000000 ) ) ;
#67572=ORIENTED_EDGE ( 'NONE', *, *, #19402, .T. ) ;
#67585=DIRECTION ( 'NONE',  ( 0.000000000000000000, 0.000000000000000000, -1.000000000000000000 ) ) ;
#67586=DIRECTION ( 'NONE',  ( 0.000000000000000000, -0.1111111111108840643, -0.9938079899999319178 ) ) ;
#67588=AXIS2_PLACEMENT_3D ( 'NONE', #67612, #35414, #61944 ) ;
#67593=ORIENTED_EDGE ( 'NONE', *, *, #10328, .F. ) ;
#67601=ADVANCED_FACE ( 'NONE', ( #67995 ), #62676, .T. ) ;
#67611=CARTESIAN_POINT ( 'NONE',  ( -11.75000000000000000, -5.000000000000000000, 26.25000000000000000 ) ) ;
#67612=CARTESIAN_POINT ( 'NONE',  ( -11.75000000000000000, -5.000000000000000000, 60.00000000000000000 ) ) ;
#67621=CARTESIAN_POINT ( 'NONE',  ( 23.48000000000000043, -15.50000000000000000, 26.00000000000000355 ) ) ;
#67624=AXIS2_PLACEMENT_3D ( 'NONE', #19944, #41512, #63080 ) ;
#67636=VERTEX_POINT ( 'NONE', #26261 ) ;
#67640=EDGE_CURVE ( 'NONE', #37912, #5159, #36758, .T. ) ;
#67643=EDGE_CURVE ( 'NONE', #37614, #9113, #41813, .T. ) ;
#67647=ORIENTED_EDGE ( 'NONE', *, *, #21207, .T. ) ;
#67657=DIRECTION ( 'NONE',  ( 0.3479852726768751237, 0.000000000000000000, -0.9375000000000004441 ) ) ;
#67674=ORIENTED_EDGE ( 'NONE', *, *, #55280, .F. ) ;
#67682=LINE ( 'NONE', #62017, #65365 ) ;
#67685=DIRECTION ( 'NONE',  ( 0.000000000000000000, -1.000000000000000000, 0.000000000000000000 ) ) ;
#67694=DIRECTION ( 'NONE',  ( -1.000000000000000000, 0.000000000000000000, 0.000000000000000000 ) ) ;
#67697=DIRECTION ( 'NONE',  ( 1.000000000000000000, 0.000000000000000000, 0.000000000000000000 ) ) ;
#67701=ORIENTED_EDGE ( 'NONE', *, *, #20696, .T. ) ;
#67704=DIRECTION ( 'NONE',  ( -1.000000000000000000, 0.000000000000000000, 0.000000000000000000 ) ) ;
#67714=EDGE_CURVE ( 'NONE', #2702, #60441, #31231, .T. ) ;
#67723=CONICAL_SURFACE ( 'NONE', #24830, 2.000000000000001776, 0.7853981633974503884 ) ;
#67726=CARTESIAN_POINT ( 'NONE',  ( -25.50000000000000355, -15.50000000000000000, 22.50000000000000000 ) ) ;
#67738=EDGE_LOOP ( 'NONE', ( #2433, #18573, #47730, #63416 ) ) ;
#67767=VECTOR ( 'NONE', #59020, 1000.000000000000000 ) ;
#67773=AXIS2_PLACEMENT_3D ( 'NONE', #54990, #17137, #44004 ) ;
#67807=VERTEX_POINT ( 'NONE', #65478 ) ;
#67808=CIRCLE ( 'NONE', #64451, 4.000000000000000888 ) ;
#67811=VERTEX_POINT ( 'NONE', #32615 ) ;
#67816=VERTEX_POINT ( 'NONE', #39963 ) ;
#67819=DIRECTION ( 'NONE',  ( 0.000000000000000000, 0.000000000000000000, -1.000000000000000000 ) ) ;
#67821=DIRECTION ( 'NONE',  ( 0.000000000000000000, 0.7096009616570518874, -0.7046037717862339012 ) ) ;
#67822=ORIENTED_EDGE ( 'NONE', *, *, #57799, .F. ) ;
#67825=DIRECTION ( 'NONE',  ( 0.000000000000000000, 0.7046037717862339012, 0.7096009616570518874 ) ) ;
#67830=VERTEX_POINT ( 'NONE', #57297 ) ;
#67840=CIRCLE ( 'NONE', #28313, 1.620999999999997332 ) ;
#67844=CARTESIAN_POINT ( 'NONE',  ( -29.50000000000000355, -12.00000000000000000, -10.69999999999999929 ) ) ;
#67853=DIRECTION ( 'NONE',  ( 0.000000000000000000, 1.000000000000000000, 0.000000000000000000 ) ) ;
#67856=DIRECTION ( 'NONE',  ( -0.000000000000000000, 1.000000000000000000, -0.000000000000000000 ) ) ;
#67865=DIRECTION ( 'NONE',  ( 0.000000000000000000, -1.000000000000000000, 0.000000000000000000 ) ) ;
#67866=CIRCLE ( 'NONE', #36213, 3.499999999999040323 ) ;
#67884=DIRECTION ( 'NONE',  ( 0.000000000000000000, -0.7071067811865455743, 0.7071067811865495711 ) ) ;
#67895=CARTESIAN_POINT ( 'NONE',  ( 29.50000000000000355, -11.50000000000100009, 15.00000000000084910 ) ) ;
#67896=CYLINDRICAL_SURFACE ( 'NONE', #25370, 0.5000000000001374456 ) ;
#67898=EDGE_LOOP ( 'NONE', ( #50735, #23412, #33997, #42228 ) ) ;
#67899=FACE_OUTER_BOUND ( 'NONE', #32956, .T. ) ;
#67901=VERTEX_POINT ( 'NONE', #61182 ) ;
#67905=FACE_OUTER_BOUND ( 'NONE', #67898, .T. ) ;
#67907=AXIS2_PLACEMENT_3D ( 'NONE', #64555, #52548, #42625 ) ;
#67914=DIRECTION ( 'NONE',  ( -1.000000000000000000, 0.000000000000000000, 0.000000000000000000 ) ) ;
#67917=VERTEX_POINT ( 'NONE', #7450 ) ;
#67925=DIRECTION ( 'NONE',  ( 0.000000000000000000, 0.7057491738665938596, 0.7084617869628679898 ) ) ;
#67931=LINE ( 'NONE', #58019, #66640 ) ;
#67936=LINE ( 'NONE', #34700, #42984 ) ;
#67940=ADVANCED_FACE ( 'NONE', ( #45273 ), #35015, .F. ) ;
#67947=EDGE_CURVE ( 'NONE', #38194, #51551, #8495, .T. ) ;
#67949=CARTESIAN_POINT ( 'NONE',  ( 30.00000000000000000, -9.487228132326899654, 12.50000000000000000 ) ) ;
#67956=ORIENTED_EDGE ( 'NONE', *, *, #40224, .F. ) ;
#67957=DIRECTION ( 'NONE',  ( 0.000000000000000000, 0.000000000000000000, 1.000000000000000000 ) ) ;
#67960=VECTOR ( 'NONE', #15686, 1000.000000000000000 ) ;
#67963=ORIENTED_EDGE ( 'NONE', *, *, #31422, .F. ) ;
#67965=DIRECTION ( 'NONE',  ( 0.000000000000000000, 0.000000000000000000, 1.000000000000000000 ) ) ;
#67966=ORIENTED_EDGE ( 'NONE', *, *, #6899, .T. ) ;
#67970=EDGE_LOOP ( 'NONE', ( #28639, #20972, #53386, #63915 ) ) ;
#67971=DIRECTION ( 'NONE',  ( -1.000000000000000000, 0.000000000000000000, 0.000000000000000000 ) ) ;
#67983=DIRECTION ( 'NONE',  ( 0.000000000000000000, 0.000000000000000000, -1.000000000000000000 ) ) ;
#67995=FACE_OUTER_BOUND ( 'NONE', #60795, .T. ) ;
#67996=DIRECTION ( 'NONE',  ( 0.000000000000000000, 0.7084617869628681008, -0.7057491738665939707 ) ) ;
#67999=EDGE_CURVE ( 'NONE', #1121, #13935, #40156, .T. ) ;
#68002=DIRECTION ( 'NONE',  ( 0.000000000000000000, 0.000000000000000000, -1.000000000000000000 ) ) ;
#68004=CARTESIAN_POINT ( 'NONE',  ( 15.50000000000000000, -0.2000000000000000111, 25.80000000297970075 ) ) ;
#68010=ORIENTED_EDGE ( 'NONE', *, *, #33394, .F. ) ;
#68014=ORIENTED_EDGE ( 'NONE', *, *, #40090, .F. ) ;
#68030=DIRECTION ( 'NONE',  ( 0.000000000000000000, 0.000000000000000000, 1.000000000000000000 ) ) ;
#68034=DIRECTION ( 'NONE',  ( 1.000000000000000000, -0.000000000000000000, -0.000000000000000000 ) ) ;
#68037=CARTESIAN_POINT ( 'NONE',  ( -11.75000000000000000, -5.200000000000001066, -11.75000000000000000 ) ) ;
#68052=CARTESIAN_POINT ( 'NONE',  ( -11.50000000000000000, -11.50000000000000000, -19.00000000000000000 ) ) ;
#68057=ORIENTED_EDGE ( 'NONE', *, *, #42758, .F. ) ;
#68063=CARTESIAN_POINT ( 'NONE',  ( -30.00000000000000000, -14.04000000000000092, 14.80000000000000071 ) ) ;
#68066=CARTESIAN_POINT ( 'NONE',  ( -15.50000000000000000, -5.000000000000000000, -22.50000000000000000 ) ) ;
#68071=ORIENTED_EDGE ( 'NONE', *, *, #62743, .T. ) ;
#68075=ADVANCED_FACE ( 'NONE', ( #47043 ), #25125, .T. ) ;
#68094=DIRECTION ( 'NONE',  ( 0.000000000000000000, 1.000000000000000000, 0.000000000000000000 ) ) ;
#68102=EDGE_LOOP ( 'NONE', ( #28486, #30752, #7254, #20606 ) ) ;
#68104=DIRECTION ( 'NONE',  ( -1.000000000000000000, 0.000000000000000000, 0.000000000000000000 ) ) ;
#68112=ORIENTED_EDGE ( 'NONE', *, *, #55194, .T. ) ;
#68113=AXIS2_PLACEMENT_3D ( 'NONE', #21915, #44163, #59746 ) ;
#68116=CARTESIAN_POINT ( 'NONE',  ( -11.00000000000000000, -8.959999999999999076, 17.04524521594300523 ) ) ;
#68117=ADVANCED_FACE ( 'NONE', ( #59047 ), #53064, .T. ) ;
#68120=EDGE_CURVE ( 'NONE', #35525, #11608, #43470, .T. ) ;
#68126=EDGE_CURVE ( 'NONE', #24168, #57618, #52663, .T. ) ;
#68130=LINE ( 'NONE', #14399, #66517 ) ;
#68134=CIRCLE ( 'NONE', #7147, 0.2000000000005226763 ) ;
#68137=CARTESIAN_POINT ( 'NONE',  ( 15.29633693294940500, -0.2717122460100945269, 23.82579074638835692 ) ) ;
#68140=CARTESIAN_POINT ( 'NONE',  ( 22.14589803375000088, -17.50000000000000000, -21.50000000000000000 ) ) ;
#68142=DIRECTION ( 'NONE',  ( -1.000000000000000000, 0.000000000000000000, 0.000000000000000000 ) ) ;
#68144=DIRECTION ( 'NONE',  ( -0.8660254037844482555, 0.000000000000000000, 0.4999999999999831801 ) ) ;
#68154=EDGE_LOOP ( 'NONE', ( #5042, #36607, #58505, #17995 ) ) ;
#68159=ORIENTED_EDGE ( 'NONE', *, *, #67403, .T. ) ;
#68160=EDGE_LOOP ( 'NONE', ( #14628, #46339, #69678, #6436 ) ) ;
#68162=CARTESIAN_POINT ( 'NONE',  ( 16.75000000000000000, -0.2038245569916320166, 23.22168783648699986 ) ) ;
#68165=AXIS2_PLACEMENT_3D ( 'NONE', #13605, #50036, #51082 ) ;
#68170=VERTEX_POINT ( 'NONE', #5324 ) ;
#68175=EDGE_CURVE ( 'NONE', #414, #36899, #1380, .T. ) ;
#68177=CARTESIAN_POINT ( 'NONE',  ( 16.75000000000000000, -0.2714405302574892098, -22.98746066354537376 ) ) ;
#68181=CARTESIAN_POINT ( 'NONE',  ( -11.00000000000000000, -11.50000000000000000, -15.00000000000000000 ) ) ;
#68185=VECTOR ( 'NONE', #48944, 1000.000000000000000 ) ;
#68190=CARTESIAN_POINT ( 'NONE',  ( 11.00000000000000000, -5.599999999999999645, -9.000000000000001776 ) ) ;
#68193=VECTOR ( 'NONE', #35804, 1000.000000000000000 ) ;
#68195=CARTESIAN_POINT ( 'NONE',  ( 30.00000000000000000, -8.959999999999999076, -17.04524521594300523 ) ) ;
#68199=LINE ( 'NONE', #55840, #67533 ) ;
#68200=CARTESIAN_POINT ( 'NONE',  ( -29.50000000000000355, -11.50000000000100009, 19.50000000000103739 ) ) ;
#68205=CARTESIAN_POINT ( 'NONE',  ( 13.00000000000000178, -15.50000000000000000, 14.50000000000000000 ) ) ;
#68209=CARTESIAN_POINT ( 'NONE',  ( -11.00000000000000000, -8.959999999999999076, -17.04524521594300523 ) ) ;
#68213=DIRECTION ( 'NONE',  ( -1.000000000000000000, 0.000000000000000000, 0.000000000000000000 ) ) ;
#68216=LINE ( 'NONE', #46642, #607 ) ;
#68227=DIRECTION ( 'NONE',  ( 0.000000000000000000, -0.7071067811865495711, -0.7071067811865455743 ) ) ;
#68229=DIRECTION ( 'NONE',  ( -1.000000000000000000, 0.000000000000000000, 0.000000000000000000 ) ) ;
#68230=AXIS2_PLACEMENT_3D ( 'NONE', #67080, #40206, #34891 ) ;
#68236=VERTEX_POINT ( 'NONE', #11624 ) ;
#68244=ORIENTED_EDGE ( 'NONE', *, *, #20427, .T. ) ;
#68253=DIRECTION ( 'NONE',  ( 0.000000000000000000, 0.000000000000000000, -1.000000000000000000 ) ) ;
#68254=ORIENTED_EDGE ( 'NONE', *, *, #17890, .T. ) ;
#68255=EDGE_CURVE ( 'NONE', #56239, #39495, #21565, .T. ) ;
#68257=DIRECTION ( 'NONE',  ( -1.000000000000000000, 0.000000000000000000, 0.000000000000000000 ) ) ;
#68263=ORIENTED_EDGE ( 'NONE', *, *, #2425, .T. ) ;
#68265=EDGE_CURVE ( 'NONE', #903, #28244, #60561, .T. ) ;
#68269=EDGE_LOOP ( 'NONE', ( #5497, #34413, #58482, #68506, #45085, #57628, #63496, #11371 ) ) ;
#68273=DIRECTION ( 'NONE',  ( 0.000000000000000000, 0.000000000000000000, 1.000000000000000000 ) ) ;
#68280=LINE ( 'NONE', #62611, #34159 ) ;
#68292=EDGE_CURVE ( 'NONE', #40989, #10852, #3127, .T. ) ;
#68297=CIRCLE ( 'NONE', #58109, 3.499999999999054534 ) ;
#68298=CARTESIAN_POINT ( 'NONE',  ( 30.00000000000000000, -12.00000000000000000, 10.20500000000000007 ) ) ;
#68304=ORIENTED_EDGE ( 'NONE', *, *, #22177, .F. ) ;
#68305=CARTESIAN_POINT ( 'NONE',  ( 30.00000000000000000, -11.50000000000082068, 10.20500000000000007 ) ) ;
#68309=LINE ( 'NONE', #30826, #28452 ) ;
#68311=DIRECTION ( 'NONE',  ( -1.000000000000000000, 0.000000000000000000, 0.000000000000000000 ) ) ;
#68316=CARTESIAN_POINT ( 'NONE',  ( -28.00000000000000000, -16.64230188589299786, -14.64519951917100116 ) ) ;
#68317=EDGE_LOOP ( 'NONE', ( #36554, #50972, #18401, #735, #1519, #44977, #38132, #20408, #43511, #21142, #58909, #69822, #61106, #59687 ) ) ;
#68320=ORIENTED_EDGE ( 'NONE', *, *, #1899, .T. ) ;
#68327=CARTESIAN_POINT ( 'NONE',  ( 13.00000000000000178, -16.28999999999710369, 14.50000000000000000 ) ) ;
#68332=ORIENTED_EDGE ( 'NONE', *, *, #60971, .T. ) ;
#68337=DIRECTION ( 'NONE',  ( 0.000000000000000000, 0.000000000000000000, 1.000000000000000000 ) ) ;
#68344=AXIS2_PLACEMENT_3D ( 'NONE', #25570, #42518, #15656 ) ;
#68350=EDGE_LOOP ( 'NONE', ( #43170, #60237, #25733, #69721 ) ) ;
#68351=AXIS2_PLACEMENT_3D ( 'NONE', #3878, #41697, #36393 ) ;
#68362=AXIS2_PLACEMENT_3D ( 'NONE', #27275, #748, #21275 ) ;
#68371=ORIENTED_EDGE ( 'NONE', *, *, #52133, .T. ) ;
#68376=EDGE_LOOP ( 'NONE', ( #54693, #43591, #45046, #50756 ) ) ;
#68377=ORIENTED_EDGE ( 'NONE', *, *, #5404, .F. ) ;
#68379=VECTOR ( 'NONE', #14047, 1000.000000000000000 ) ;
#68385=EDGE_CURVE ( 'NONE', #7056, #23202, #40594, .T. ) ;
#68386=AXIS2_PLACEMENT_3D ( 'NONE', #22457, #37677, #53595 ) ;
#68389=CARTESIAN_POINT ( 'NONE',  ( -15.50000000000000000, -15.50000000000000000, -22.50000000000000000 ) ) ;
#68399=ORIENTED_EDGE ( 'NONE', *, *, #40001, .T. ) ;
#68401=DIRECTION ( 'NONE',  ( 0.000000000000000000, 0.000000000000000000, -1.000000000000000000 ) ) ;
#68406=CARTESIAN_POINT ( 'NONE',  ( 11.00000000000000000, -5.599999999999999645, -27.00000000000000000 ) ) ;
#68412=CARTESIAN_POINT ( 'NONE',  ( 24.00000000000000000, -16.28999999999710369, 15.00000000000794920 ) ) ;
#68413=CARTESIAN_POINT ( 'NONE',  ( -15.50000000000000000, -1.037157890325000054, -22.50000000000000000 ) ) ;
#68415=DIRECTION ( 'NONE',  ( -1.000000000000000000, 0.000000000000000000, 0.000000000000000000 ) ) ;
#68421=DIRECTION ( 'NONE',  ( 0.000000000000000000, -1.000000000000000000, 0.000000000000000000 ) ) ;
#68433=ORIENTED_EDGE ( 'NONE', *, *, #13542, .T. ) ;
#68434=DIRECTION ( 'NONE',  ( 0.000000000000000000, 0.000000000000000000, 1.000000000000000000 ) ) ;
#68445=VERTEX_POINT ( 'NONE', #41290 ) ;
#68449=VECTOR ( 'NONE', #9219, 1000.000000000000000 ) ;
#68453=ORIENTED_EDGE ( 'NONE', *, *, #24806, .F. ) ;
#68458=DIRECTION ( 'NONE',  ( 0.000000000000000000, 0.000000000000000000, 1.000000000000000000 ) ) ;
#68462=CARTESIAN_POINT ( 'NONE',  ( 25.50000000000000355, 0.000000000000000000, 22.50000000000000000 ) ) ;
#68477=CARTESIAN_POINT ( 'NONE',  ( 18.85410196625000268, -15.50000000000000000, 21.50000000000000000 ) ) ;
#68483=ORIENTED_EDGE ( 'NONE', *, *, #42725, .F. ) ;
#68484=LINE ( 'NONE', #30997, #62926 ) ;
#68494=DIRECTION ( 'NONE',  ( 0.000000000000000000, 1.000000000000000000, 0.000000000000000000 ) ) ;
#68497=ORIENTED_EDGE ( 'NONE', *, *, #16812, .F. ) ;
#68498=DIRECTION ( 'NONE',  ( -1.000000000000000000, 0.000000000000000000, 0.000000000000000000 ) ) ;
#68501=DIRECTION ( 'NONE',  ( 0.000000000000000000, 1.000000000000000000, 0.000000000000000000 ) ) ;
#68505=DIRECTION ( 'NONE',  ( 0.000000000000000000, 0.000000000000000000, 1.000000000000000000 ) ) ;
#68506=ORIENTED_EDGE ( 'NONE', *, *, #53998, .T. ) ;
#68510=CARTESIAN_POINT ( 'NONE',  ( -29.50000000000000355, -12.00000000000000000, -10.52786404500095863 ) ) ;
#68528=VERTEX_POINT ( 'NONE', #31042 ) ;
#68532=EDGE_LOOP ( 'NONE', ( #30450, #8044, #11461, #7972 ) ) ;
#68537=ORIENTED_EDGE ( 'NONE', *, *, #60827, .F. ) ;
#68539=AXIS2_PLACEMENT_3D ( 'NONE', #16201, #59336, #38470 ) ;
#68543=LINE ( 'NONE', #69590, #39870 ) ;
#68554=DIRECTION ( 'NONE',  ( 0.000000000000000000, 1.000000000000000000, 0.000000000000000000 ) ) ;
#68561=DIRECTION ( 'NONE',  ( 0.000000000000000000, 0.000000000000000000, -1.000000000000000000 ) ) ;
#68562=EDGE_LOOP ( 'NONE', ( #66072, #21039, #29443, #23870 ) ) ;
#68568=DIRECTION ( 'NONE',  ( 0.000000000000000000, 1.000000000000000000, 0.000000000000000000 ) ) ;
#68571=ORIENTED_EDGE ( 'NONE', *, *, #44387, .T. ) ;
#68573=DIRECTION ( 'NONE',  ( -1.000000000000000000, 0.000000000000000000, 0.000000000000000000 ) ) ;
#68575=DIRECTION ( 'NONE',  ( 0.000000000000000000, 0.000000000000000000, 1.000000000000000000 ) ) ;
#68592=DIRECTION ( 'NONE',  ( 0.000000000000000000, 0.000000000000000000, 1.000000000000000000 ) ) ;
#68600=ORIENTED_EDGE ( 'NONE', *, *, #67046, .F. ) ;
#68602=AXIS2_PLACEMENT_3D ( 'NONE', #30215, #8277, #57074 ) ;
#68612=CIRCLE ( 'NONE', #38133, 4.500000000000191847 ) ;
#68621=ORIENTED_EDGE ( 'NONE', *, *, #15718, .F. ) ;
#68623=EDGE_CURVE ( 'NONE', #44169, #26101, #27134, .T. ) ;
#68630=ORIENTED_EDGE ( 'NONE', *, *, #59380, .F. ) ;
#68633=LINE ( 'NONE', #9230, #26414 ) ;
#68649=EDGE_LOOP ( 'NONE', ( #44063, #69742, #28955, #50081 ) ) ;
#68662=FACE_OUTER_BOUND ( 'NONE', #47936, .T. ) ;
#68670=EDGE_CURVE ( 'NONE', #26198, #7905, #54701, .T. ) ;
#68672=CARTESIAN_POINT ( 'NONE',  ( 30.00000000000000000, -12.00000000000000000, -10.20500000000000007 ) ) ;
#68677=EDGE_CURVE ( 'NONE', #6775, #52725, #64967, .T. ) ;
#68681=ORIENTED_EDGE ( 'NONE', *, *, #31878, .T. ) ;
#68682=EDGE_CURVE ( 'NONE', #14586, #23311, #49733, .T. ) ;
#68684=ADVANCED_FACE ( 'NONE', ( #37402 ), #32090, .T. ) ;
#68688=ADVANCED_FACE ( 'NONE', ( #50764 ), #35190, .F. ) ;
#68692=CARTESIAN_POINT ( 'NONE',  ( 11.00000000000000000, -17.50000000000000000, 26.64999999999999858 ) ) ;
#68693=ORIENTED_EDGE ( 'NONE', *, *, #7498, .T. ) ;
#68695=DIRECTION ( 'NONE',  ( 0.000000000000000000, 0.000000000000000000, 1.000000000000000000 ) ) ;
#68696=ORIENTED_EDGE ( 'NONE', *, *, #62333, .F. ) ;
#68704=ADVANCED_FACE ( 'NONE', ( #60689 ), #12924, .F. ) ;
#68705=VECTOR ( 'NONE', #30357, 1000.000000000000000 ) ;
#68709=ORIENTED_EDGE ( 'NONE', *, *, #22090, .F. ) ;
#68712=VERTEX_POINT ( 'NONE', #40151 ) ;
#68713=FACE_OUTER_BOUND ( 'NONE', #38211, .T. ) ;
#68714=EDGE_CURVE ( 'NONE', #21845, #23827, #7974, .T. ) ;
#68720=VERTEX_POINT ( 'NONE', #51119 ) ;
#68723=ORIENTED_EDGE ( 'NONE', *, *, #27842, .F. ) ;
#68725=LINE ( 'NONE', #63767, #46873 ) ;
#68734=CARTESIAN_POINT ( 'NONE',  ( 11.50000000000000000, -12.00000000000000000, 10.69999999999999929 ) ) ;
#68742=DIRECTION ( 'NONE',  ( 0.000000000000000000, -1.000000000000000000, 0.000000000000000000 ) ) ;
#68744=EDGE_CURVE ( 'NONE', #1475, #69663, #45922, .T. ) ;
#68747=DIRECTION ( 'NONE',  ( -1.000000000000000000, 0.000000000000000000, 0.000000000000000000 ) ) ;
#68754=CARTESIAN_POINT ( 'NONE',  ( 11.75000000000000000, -5.200000000000001066, -11.75000000000000000 ) ) ;
#68759=ORIENTED_EDGE ( 'NONE', *, *, #3509, .F. ) ;
#68761=DIRECTION ( 'NONE',  ( -1.000000000000000000, 0.000000000000000000, 0.000000000000000000 ) ) ;
#68764=CARTESIAN_POINT ( 'NONE',  ( 11.50000000000000000, -11.50000000000000000, -15.00000000000000000 ) ) ;
#68769=ADVANCED_FACE ( 'NONE', ( #61730 ), #39797, .F. ) ;
#68775=DIRECTION ( 'NONE',  ( 1.000000000000000000, -0.000000000000000000, -0.000000000000000000 ) ) ;
#68778=EDGE_LOOP ( 'NONE', ( #67489, #64990, #21399, #30142 ) ) ;
#68781=ORIENTED_EDGE ( 'NONE', *, *, #5823, .F. ) ;
#68785=EDGE_CURVE ( 'NONE', #37150, #38571, #47106, .T. ) ;
#68791=EDGE_LOOP ( 'NONE', ( #57639, #45994, #11957, #51283 ) ) ;
#68792=ORIENTED_EDGE ( 'NONE', *, *, #17125, .T. ) ;
#68796=DIRECTION ( 'NONE',  ( 0.000000000000000000, -0.8206518066484758123, -0.5714285714283042772 ) ) ;
#68799=ORIENTED_EDGE ( 'NONE', *, *, #33302, .T. ) ;
#68818=CARTESIAN_POINT ( 'NONE',  ( 29.25000000000000000, -5.000000000000000000, 26.25000000000000000 ) ) ;
#68826=ADVANCED_FACE ( 'NONE', ( #9393 ), #13989, .F. ) ;
#68831=CYLINDRICAL_SURFACE ( 'NONE', #4246, 4.000000000000000000 ) ;
#68832=ADVANCED_FACE ( 'NONE', ( #51827 ), #52177, .F. ) ;
#68838=ADVANCED_FACE ( 'NONE', ( #30266 ), #36258, .T. ) ;
#68841=AXIS2_PLACEMENT_3D ( 'NONE', #38566, #18016, #60119 ) ;
#68853=VERTEX_POINT ( 'NONE', #62780 ) ;
#68857=DIRECTION ( 'NONE',  ( 0.000000000000000000, 0.000000000000000000, 1.000000000000000000 ) ) ;
#68865=VERTEX_POINT ( 'NONE', #14357 ) ;
#68873=ORIENTED_EDGE ( 'NONE', *, *, #37129, .T. ) ;
#68893=ORIENTED_EDGE ( 'NONE', *, *, #33929, .T. ) ;
#68909=DIRECTION ( 'NONE',  ( 0.000000000000000000, 1.000000000000000000, 0.000000000000000000 ) ) ;
#68918=ADVANCED_FACE ( 'NONE', ( #67905 ), #17762, .F. ) ;
#68926=FACE_OUTER_BOUND ( 'NONE', #16661, .T. ) ;
#68927=EDGE_LOOP ( 'NONE', ( #58063, #27137, #40409, #7859 ) ) ;
#68928=DIRECTION ( 'NONE',  ( -1.000000000000000000, 0.000000000000000000, 0.000000000000000000 ) ) ;
#68933=CARTESIAN_POINT ( 'NONE',  ( -11.00000000000000000, -16.28999999999710369, 15.00000000000794920 ) ) ;
#68937=LINE ( 'NONE', #14496, #42143 ) ;
#68942=ORIENTED_EDGE ( 'NONE', *, *, #45904, .T. ) ;
#68949=DIRECTION ( 'NONE',  ( 0.000000000000000000, 0.000000000000000000, 1.000000000000000000 ) ) ;
#68950=ORIENTED_EDGE ( 'NONE', *, *, #32697, .T. ) ;
#68954=EDGE_LOOP ( 'NONE', ( #58289, #32834, #58094, #64265 ) ) ;
#68966=CARTESIAN_POINT ( 'NONE',  ( 29.25000000000000000, -5.200000000000001066, 26.25000000000000000 ) ) ;
#68967=EDGE_LOOP ( 'NONE', ( #64133, #23992, #12848, #51990 ) ) ;
#68970=DIRECTION ( 'NONE',  ( 0.000000000000000000, 0.000000000000000000, 1.000000000000000000 ) ) ;
#68975=VERTEX_POINT ( 'NONE', #9212 ) ;
#68978=EDGE_CURVE ( 'NONE', #58887, #20965, #19455, .T. ) ;
#68981=ORIENTED_EDGE ( 'NONE', *, *, #44533, .T. ) ;
#68985=CARTESIAN_POINT ( 'NONE',  ( -11.00000000000000000, -11.85423089348099879, -9.852125413066602277 ) ) ;
#68987=FACE_OUTER_BOUND ( 'NONE', #37205, .T. ) ;
#68990=DIRECTION ( 'NONE',  ( 0.000000000000000000, 0.000000000000000000, 1.000000000000000000 ) ) ;
#69002=DIRECTION ( 'NONE',  ( 0.000000000000000000, 0.000000000000000000, -1.000000000000000000 ) ) ;
#69003=CARTESIAN_POINT ( 'NONE',  ( 15.50000000000000000, -0.4000000000005274892, -22.50000000000000000 ) ) ;
#69011=CYLINDRICAL_SURFACE ( 'NONE', #28295, 3.499999999999999556 ) ;
#69012=ORIENTED_EDGE ( 'NONE', *, *, #27655, .F. ) ;
#69016=DIRECTION ( 'NONE',  ( -1.000000000000000000, 0.000000000000000000, 0.000000000000000000 ) ) ;
#69034=CARTESIAN_POINT ( 'NONE',  ( -30.00000000000000000, -14.04000000000000092, 17.04524521594300523 ) ) ;
#69035=PLANE ( 'NONE',  #51226 ) ;
#69046=EDGE_CURVE ( 'NONE', #32181, #43574, #57283, .T. ) ;
#69047=CARTESIAN_POINT ( 'NONE',  ( 15.50000000000000000, -15.50000000000000000, 22.50000000000000000 ) ) ;
#69055=DIRECTION ( 'NONE',  ( 0.000000000000000000, 0.000000000000000000, 1.000000000000000000 ) ) ;
#69056=ORIENTED_EDGE ( 'NONE', *, *, #62946, .T. ) ;
#69063=PLANE ( 'NONE',  #26654 ) ;
#69070=DIRECTION ( 'NONE',  ( 0.000000000000000000, 1.000000000000000000, 0.000000000000000000 ) ) ;
#69075=EDGE_CURVE ( 'NONE', #6765, #62987, #42429, .T. ) ;
#69077=EDGE_CURVE ( 'NONE', #27404, #4441, #40316, .T. ) ;
#69081=ORIENTED_EDGE ( 'NONE', *, *, #34961, .T. ) ;
#69090=EDGE_CURVE ( 'NONE', #4292, #61558, #5656, .T. ) ;
#69093=AXIS2_PLACEMENT_3D ( 'NONE', #8313, #29887, #24598 ) ;
#69097=EDGE_CURVE ( 'NONE', #22061, #46013, #47385, .T. ) ;
#69103=DIRECTION ( 'NONE',  ( 0.000000000000000000, 0.000000000000000000, 1.000000000000000000 ) ) ;
#69111=LINE ( 'NONE', #42585, #17003 ) ;
#69114=DIRECTION ( 'NONE',  ( 0.000000000000000000, 0.000000000000000000, 1.000000000000000000 ) ) ;
#69117=DIRECTION ( 'NONE',  ( -1.000000000000000000, 0.000000000000000000, 0.000000000000000000 ) ) ;
#69120=CARTESIAN_POINT ( 'NONE',  ( -25.50000000000000355, -5.200000000000001066, -24.50000000000000000 ) ) ;
#69130=AXIS2_PLACEMENT_3D ( 'NONE', #51236, #2794, #24374 ) ;
#69139=VERTEX_POINT ( 'NONE', #20862 ) ;
#69143=ORIENTED_EDGE ( 'NONE', *, *, #46134, .T. ) ;
#69145=CARTESIAN_POINT ( 'NONE',  ( -15.50000000000000000, -1.037157890325000054, 22.50000000000000000 ) ) ;
#69152=DIRECTION ( 'NONE',  ( 0.000000000000000000, 0.000000000000000000, 1.000000000000000000 ) ) ;
#69156=ORIENTED_EDGE ( 'NONE', *, *, #27261, .T. ) ;
#69162=LINE ( 'NONE', #37000, #6696 ) ;
#69169=CARTESIAN_POINT ( 'NONE',  ( -30.00000000000000000, -9.199999999999999289, -12.69999999999986073 ) ) ;
#69172=DIRECTION ( 'NONE',  ( 0.000000000000000000, 0.5000000000000199840, 0.8660254037844271613 ) ) ;
#69180=DIRECTION ( 'NONE',  ( 0.000000000000000000, 1.000000000000000000, 0.000000000000000000 ) ) ;
#69194=PLANE ( 'NONE',  #42147 ) ;
#69202=FACE_OUTER_BOUND ( 'NONE', #7466, .T. ) ;
#69207=CARTESIAN_POINT ( 'NONE',  ( 30.00000000000000000, -11.85423089348099879, 9.852125413066602277 ) ) ;
#69212=ORIENTED_EDGE ( 'NONE', *, *, #21743, .T. ) ;
#69215=CARTESIAN_POINT ( 'NONE',  ( -30.00000000000000000, -11.85423089348099879, 9.852125413066602277 ) ) ;
#69218=ORIENTED_EDGE ( 'NONE', *, *, #3664, .F. ) ;
#69229=ORIENTED_EDGE ( 'NONE', *, *, #40090, .T. ) ;
#69231=EDGE_CURVE ( 'NONE', #60253, #6765, #49477, .T. ) ;
#69242=EDGE_LOOP ( 'NONE', ( #68792, #29377, #18624, #64562 ) ) ;
#69243=PLANE ( 'NONE',  #48295 ) ;
#69258=VECTOR ( 'NONE', #58093, 1000.000000000000000 ) ;
#69263=CARTESIAN_POINT ( 'NONE',  ( -25.50000000000000355, -17.50000000000000000, -22.50000000000000000 ) ) ;
#69264=ORIENTED_EDGE ( 'NONE', *, *, #30593, .T. ) ;
#69274=CARTESIAN_POINT ( 'NONE',  ( -29.50000000000000355, -11.50000000000100009, 15.00000000000084910 ) ) ;
#69276=CARTESIAN_POINT ( 'NONE',  ( 17.51999999999999957, -15.50000000000000000, -26.00000000000000355 ) ) ;
#69277=CARTESIAN_POINT ( 'NONE',  ( 28.00000000000000000, -15.50000000000000000, -20.05051025721700242 ) ) ;
#69297=VERTEX_POINT ( 'NONE', #55132 ) ;
#69306=CARTESIAN_POINT ( 'NONE',  ( 15.50000000000129852, -15.50000000000000000, -22.50000000000000000 ) ) ;
#69313=ORIENTED_EDGE ( 'NONE', *, *, #47924, .T. ) ;
#69325=ORIENTED_EDGE ( 'NONE', *, *, #35712, .F. ) ;
#69327=LINE ( 'NONE', #30542, #782 ) ;
#69331=DIRECTION ( 'NONE',  ( 1.000000000000000000, -0.000000000000000000, -0.000000000000000000 ) ) ;
#69334=ORIENTED_EDGE ( 'NONE', *, *, #9308, .T. ) ;
#69335=DIRECTION ( 'NONE',  ( 0.000000000000000000, 0.000000000000000000, 1.000000000000000000 ) ) ;
#69343=DIRECTION ( 'NONE',  ( 0.000000000000000000, -0.7278708115916149302, -0.6857142857145122061 ) ) ;
#69350=CIRCLE ( 'NONE', #8348, 0.5000000000001392220 ) ;
#69354=EDGE_CURVE ( 'NONE', #50308, #3316, #56501, .T. ) ;
#69360=CARTESIAN_POINT ( 'NONE',  ( -11.75000000000000000, -5.000000000000000000, -23.89194109070750116 ) ) ;
#69361=DIRECTION ( 'NONE',  ( 0.000000000000000000, 0.000000000000000000, 1.000000000000000000 ) ) ;
#69363=ORIENTED_EDGE ( 'NONE', *, *, #59440, .F. ) ;
#69367=LINE ( 'NONE', #20921, #37722 ) ;
#69368=ORIENTED_EDGE ( 'NONE', *, *, #41589, .F. ) ;
#69377=VERTEX_POINT ( 'NONE', #68162 ) ;
#69378=ORIENTED_EDGE ( 'NONE', *, *, #43401, .T. ) ;
#69382=DIRECTION ( 'NONE',  ( 0.000000000000000000, 3.989863994748342081E-13, 1.000000000000000000 ) ) ;
#69388=FACE_OUTER_BOUND ( 'NONE', #9257, .T. ) ;
#69392=VERTEX_POINT ( 'NONE', #41284 ) ;
#69414=ORIENTED_EDGE ( 'NONE', *, *, #40892, .F. ) ;
#69416=CIRCLE ( 'NONE', #16366, 0.3500000000002722600 ) ;
#69418=CARTESIAN_POINT ( 'NONE',  ( -13.00000000000000178, -17.50000000000000000, 20.05051025721700242 ) ) ;
#69425=CARTESIAN_POINT ( 'NONE',  ( -25.50000000000000355, 0.000000000000000000, 20.24999999999999645 ) ) ;
#69429=CARTESIAN_POINT ( 'NONE',  ( 11.75000000000000000, -5.200000000000001066, 11.75000000000000000 ) ) ;
#69431=CARTESIAN_POINT ( 'NONE',  ( 30.00000000000000000, -17.50000000000000000, 26.64999999999999858 ) ) ;
#69433=CARTESIAN_POINT ( 'NONE',  ( -30.00000000000000000, -15.46862696659690073, 14.50000000000000000 ) ) ;
#69443=VERTEX_POINT ( 'NONE', #45892 ) ;
#69446=CIRCLE ( 'NONE', #41218, 3.499999999999999556 ) ;
#69457=ADVANCED_FACE ( 'NONE', ( #30693 ), #35988, .T. ) ;
#69458=ORIENTED_EDGE ( 'NONE', *, *, #7813, .T. ) ;
#69462=CIRCLE ( 'NONE', #38965, 0.5000000000001386669 ) ;
#69469=CARTESIAN_POINT ( 'NONE',  ( 29.50000000000000355, -11.70000000000012008, -10.70000000000011831 ) ) ;
#69473=ORIENTED_EDGE ( 'NONE', *, *, #62909, .T. ) ;
#69485=ORIENTED_EDGE ( 'NONE', *, *, #48259, .F. ) ;
#69486=DIRECTION ( 'NONE',  ( 0.000000000000000000, 0.000000000000000000, 1.000000000000000000 ) ) ;
#69492=AXIS2_PLACEMENT_3D ( 'NONE', #56569, #18735, #40301 ) ;
#69495=CYLINDRICAL_SURFACE ( 'NONE', #6251, 0.3499999999999302558 ) ;
#69498=DIRECTION ( 'NONE',  ( 1.000000000000000000, -0.000000000000000000, -0.000000000000000000 ) ) ;
#69504=EDGE_LOOP ( 'NONE', ( #43524, #34362, #69906, #62488 ) ) ;
#69505=ORIENTED_EDGE ( 'NONE', *, *, #19813, .T. ) ;
#69523=ADVANCED_FACE ( 'NONE', ( #20771 ), #9911, .F. ) ;
#69544=DIRECTION ( 'NONE',  ( 0.000000000000000000, -1.000000000000000000, 0.000000000000000000 ) ) ;
#69553=VERTEX_POINT ( 'NONE', #31747 ) ;
#69555=LINE ( 'NONE', #31021, #26590 ) ;
#69568=AXIS2_PLACEMENT_3D ( 'NONE', #910, #16807, #65587 ) ;
#69589=EDGE_CURVE ( 'NONE', #1690, #46397, #26791, .T. ) ;
#69590=CARTESIAN_POINT ( 'NONE',  ( 30.00000000000000000, -16.28999999999999915, 14.50000000000000000 ) ) ;
#69594=DIRECTION ( 'NONE',  ( 0.000000000000000000, 1.000000000000000000, 0.000000000000000000 ) ) ;
#69597=ORIENTED_EDGE ( 'NONE', *, *, #28044, .T. ) ;
#69603=AXIS2_PLACEMENT_3D ( 'NONE', #9723, #31304, #36953 ) ;
#69604=DIRECTION ( 'NONE',  ( 0.4285714285711672566, 0.000000000000000000, 0.9035079029053751931 ) ) ;
#69607=AXIS2_PLACEMENT_3D ( 'NONE', #44551, #49533, #13070 ) ;
#69612=EDGE_LOOP ( 'NONE', ( #67136, #69745, #10505, #49452, #28403, #7283, #487, #61684, #30002, #25295, #53040, #9209, #6595, #40172 ) ) ;
#69627=DIRECTION ( 'NONE',  ( 0.000000000000000000, -0.9938079899998859545, -0.1111111111112941946 ) ) ;
#69631=DIRECTION ( 'NONE',  ( 0.000000000000000000, 0.000000000000000000, 1.000000000000000000 ) ) ;
#69633=DIRECTION ( 'NONE',  ( 0.000000000000000000, 0.000000000000000000, 1.000000000000000000 ) ) ;
#69640=ORIENTED_EDGE ( 'NONE', *, *, #58729, .T. ) ;
#69657=VECTOR ( 'NONE', #34625, 1000.000000000000000 ) ;
#69659=FACE_OUTER_BOUND ( 'NONE', #43201, .T. ) ;
#69663=VERTEX_POINT ( 'NONE', #66341 ) ;
#69667=CARTESIAN_POINT ( 'NONE',  ( 14.45366306705349402, -0.2717122460102546766, -23.33927276307431598 ) ) ;
#69669=DIRECTION ( 'NONE',  ( 0.000000000000000000, 1.000000000000000000, 0.000000000000000000 ) ) ;
#69672=DIRECTION ( 'NONE',  ( 0.000000000000000000, 1.000000000000000000, 0.000000000000000000 ) ) ;
#69678=ORIENTED_EDGE ( 'NONE', *, *, #29330, .F. ) ;
#69687=ADVANCED_FACE ( 'NONE', ( #49400 ), #50072, .F. ) ;
#69689=DIRECTION ( 'NONE',  ( -0.4999999999989361843, 0.000000000000000000, 0.8660254037850529940 ) ) ;
#69690=ORIENTED_EDGE ( 'NONE', *, *, #9894, .T. ) ;
#69694=CARTESIAN_POINT ( 'NONE',  ( 30.00000000000000000, -5.599999999999379696, 26.60000000000059828 ) ) ;
#69701=DIRECTION ( 'NONE',  ( 0.000000000000000000, 1.000000000000000000, 0.000000000000000000 ) ) ;
#69703=DIRECTION ( 'NONE',  ( -1.000000000000000000, 0.000000000000000000, 0.000000000000000000 ) ) ;
#69712=CARTESIAN_POINT ( 'NONE',  ( 25.50000000000000355, -17.50000000000000000, 22.50000000000000000 ) ) ;
#69714=ORIENTED_EDGE ( 'NONE', *, *, #65102, .T. ) ;
#69718=CARTESIAN_POINT ( 'NONE',  ( 16.75000000000000000, -2.500000000000000000, -23.22168783648699986 ) ) ;
#69721=ORIENTED_EDGE ( 'NONE', *, *, #861, .F. ) ;
#69727=DIRECTION ( 'NONE',  ( 1.000000000000000000, -0.000000000000000000, -0.000000000000000000 ) ) ;
#69732=EDGE_CURVE ( 'NONE', #66744, #54664, #53967, .T. ) ;
#69736=ORIENTED_EDGE ( 'NONE', *, *, #18235, .F. ) ;
#69737=DIRECTION ( 'NONE',  ( 0.000000000000000000, 0.000000000000000000, 1.000000000000000000 ) ) ;
#69738=DIRECTION ( 'NONE',  ( 0.000000000000000000, -0.8206518066484758123, -0.5714285714283042772 ) ) ;
#69739=CARTESIAN_POINT ( 'NONE',  ( 30.00000000000000000, -5.000000000000000000, 27.00000000000000000 ) ) ;
#69742=ORIENTED_EDGE ( 'NONE', *, *, #40522, .F. ) ;
#69745=ORIENTED_EDGE ( 'NONE', *, *, #62743, .F. ) ;
#69759=AXIS2_PLACEMENT_3D ( 'NONE', #47598, #31361, #42286 ) ;
#69763=AXIS2_PLACEMENT_3D ( 'NONE', #31606, #4031, #20278 ) ;
#69771=AXIS2_PLACEMENT_3D ( 'NONE', #10051, #52853, #31623 ) ;
#69773=VERTEX_POINT ( 'NONE', #6250 ) ;
#69778=EDGE_LOOP ( 'NONE', ( #36844, #52539, #23123, #19449 ) ) ;
#69779=DIRECTION ( 'NONE',  ( -1.000000000000000000, 0.000000000000000000, 0.000000000000000000 ) ) ;
#69785=DIRECTION ( 'NONE',  ( 0.000000000000000000, 1.000000000000000000, 0.000000000000000000 ) ) ;
#69811=ORIENTED_EDGE ( 'NONE', *, *, #13824, .T. ) ;
#69821=FACE_OUTER_BOUND ( 'NONE', #26163, .T. ) ;
#69822=ORIENTED_EDGE ( 'NONE', *, *, #38573, .F. ) ;
#69826=CYLINDRICAL_SURFACE ( 'NONE', #17691, 0.3999999999993835154 ) ;
#69827=CARTESIAN_POINT ( 'NONE',  ( -29.25000000000000000, -5.200000000000001066, -26.25000000000000000 ) ) ;
#69829=DIRECTION ( 'NONE',  ( 0.000000000000000000, 1.000000000000000000, 0.000000000000000000 ) ) ;
#69836=ORIENTED_EDGE ( 'NONE', *, *, #14716, .T. ) ;
#69840=ORIENTED_EDGE ( 'NONE', *, *, #46233, .F. ) ;
#69842=VERTEX_POINT ( 'NONE', #7970 ) ;
#69844=CYLINDRICAL_SURFACE ( 'NONE', #45121, 4.000000000000000000 ) ;
#69848=VECTOR ( 'NONE', #2740, 999.9999999999998863 ) ;
#69871=CARTESIAN_POINT ( 'NONE',  ( 15.50000000000000000, -5.000000000000000000, 18.50000000000000000 ) ) ;
#69874=ORIENTED_EDGE ( 'NONE', *, *, #26038, .T. ) ;
#69876=EDGE_CURVE ( 'NONE', #44054, #3700, #33499, .T. ) ;
#69880=ORIENTED_EDGE ( 'NONE', *, *, #63197, .F. ) ;
#69889=ADVANCED_FACE ( 'NONE', ( #61362 ), #31411, .F. ) ;
#69899=DIRECTION ( 'NONE',  ( 0.000000000000000000, 1.000000000000000000, 0.000000000000000000 ) ) ;
#69905=CARTESIAN_POINT ( 'NONE',  ( 29.50000000000000355, -11.50000000000000000, -11.00000000000000000 ) ) ;
#69906=ORIENTED_EDGE ( 'NONE', *, *, #16797, .T. ) ;
#69907=DIRECTION ( 'NONE',  ( -1.000000000000000000, 0.000000000000000000, 0.000000000000000000 ) ) ;
#69909=CIRCLE ( 'NONE', #14589, 2.250000000000001776 ) ;
#69922=ORIENTED_EDGE ( 'NONE', *, *, #46255, .F. ) ;
#69931=DIRECTION ( 'NONE',  ( 0.000000000000000000, 1.000000000000000000, 0.000000000000000000 ) ) ;
#69939=VECTOR ( 'NONE', #10258, 1000.000000000000000 ) ;
#69940=DIRECTION ( 'NONE',  ( -1.000000000000000000, 0.000000000000000000, 0.000000000000000000 ) ) ;
#69942=EDGE_CURVE ( 'NONE', #8802, #4926, #53581, .T. ) ;
#69949=LINE ( 'NONE', #4909, #43182 ) ;
#69959=DIRECTION ( 'NONE',  ( -1.000000000000000000, 0.000000000000000000, 0.000000000000000000 ) ) ;
#69963=PLANE ( 'NONE',  #67212 ) ;
#69973=CARTESIAN_POINT ( 'NONE',  ( 11.50000000000000000, -11.50000000000000000, -15.00000000000000000 ) ) ;
ENDSEC;
END-ISO-10303-21;
